ISO-10303-21;
HEADER;
/* Generated by software containing ST-Developer
 * from STEP Tools, Inc. (www.steptools.com) 
 */

FILE_DESCRIPTION(
/* description */ ('Independent30mm screw-fed quill/spindle unit with16mm straight tool s
ocket, radial set screw, native reusable open ball bearings, retained 
inner/outer race stacks, keyed quill guide and M12x1.75 fine feed. Ext
ernal moving drive and tool not included. Ideal cage orbital links; in
dividual ball spin, force and preload not simulated. No drilling capac
ity, runout, speed, torque, load, life or machine safety rating.'),
/* implementation_level */ '2;1');

FILE_NAME(
/* name */ 'Socket head cap screw M4x12.step',
/* time_stamp */ '2026-11-08T18:59:42-08:00',
/* author */ (''),
/* organization */ (''),
/* preprocessor_version */ 'ST-DEVELOPER v20.2',
/* originating_system */ 'Autodesk Translation Framework v15.17.0.0',
/* authorisation */ '');

FILE_SCHEMA (('AUTOMOTIVE_DESIGN { 1 0 10303 214 3 1 1 }'));
ENDSEC;

DATA;
#10=MECHANICAL_DESIGN_GEOMETRIC_PRESENTATION_REPRESENTATION('',(#1609),#63898);
#239=CONICAL_SURFACE('',#16787,1.5,0.785398163397449);
#264=B_SPLINE_SURFACE_WITH_KNOTS('',3,3,((#62683,#62684,#62685,#62686,#62687,
#62688,#62689,#62690,#62691,#62692,#62693,#62694,#62695,#62696,#62697,#62698,
#62699,#62700,#62701,#62702,#62703,#62704,#62705,#62706,#62707,#62708,#62709,
#62710,#62711,#62712,#62713,#62714,#62715,#62716,#62717,#62718,#62719,#62720,
#62721,#62722,#62723,#62724,#62725,#62726,#62727,#62728,#62729,#62730,#62731,
#62732,#62733,#62734,#62735,#62736,#62737,#62738,#62739,#62740,#62741,#62742,
#62743,#62744,#62745,#62746,#62747,#62748,#62749,#62750,#62751,#62752,#62753,
#62754,#62755,#62756,#62757,#62758,#62759,#62760,#62761,#62762,#62763,#62764,
#62765,#62766,#62767,#62768,#62769,#62770,#62771,#62772,#62773,#62774,#62775,
#62776,#62777,#62778,#62779,#62780,#62781,#62782,#62783,#62784,#62785,#62786,
#62787,#62788),(#62789,#62790,#62791,#62792,#62793,#62794,#62795,#62796,
#62797,#62798,#62799,#62800,#62801,#62802,#62803,#62804,#62805,#62806,#62807,
#62808,#62809,#62810,#62811,#62812,#62813,#62814,#62815,#62816,#62817,#62818,
#62819,#62820,#62821,#62822,#62823,#62824,#62825,#62826,#62827,#62828,#62829,
#62830,#62831,#62832,#62833,#62834,#62835,#62836,#62837,#62838,#62839,#62840,
#62841,#62842,#62843,#62844,#62845,#62846,#62847,#62848,#62849,#62850,#62851,
#62852,#62853,#62854,#62855,#62856,#62857,#62858,#62859,#62860,#62861,#62862,
#62863,#62864,#62865,#62866,#62867,#62868,#62869,#62870,#62871,#62872,#62873,
#62874,#62875,#62876,#62877,#62878,#62879,#62880,#62881,#62882,#62883,#62884,
#62885,#62886,#62887,#62888,#62889,#62890,#62891,#62892,#62893,#62894),
(#62895,#62896,#62897,#62898,#62899,#62900,#62901,#62902,#62903,#62904,
#62905,#62906,#62907,#62908,#62909,#62910,#62911,#62912,#62913,#62914,#62915,
#62916,#62917,#62918,#62919,#62920,#62921,#62922,#62923,#62924,#62925,#62926,
#62927,#62928,#62929,#62930,#62931,#62932,#62933,#62934,#62935,#62936,#62937,
#62938,#62939,#62940,#62941,#62942,#62943,#62944,#62945,#62946,#62947,#62948,
#62949,#62950,#62951,#62952,#62953,#62954,#62955,#62956,#62957,#62958,#62959,
#62960,#62961,#62962,#62963,#62964,#62965,#62966,#62967,#62968,#62969,#62970,
#62971,#62972,#62973,#62974,#62975,#62976,#62977,#62978,#62979,#62980,#62981,
#62982,#62983,#62984,#62985,#62986,#62987,#62988,#62989,#62990,#62991,#62992,
#62993,#62994,#62995,#62996,#62997,#62998,#62999,#63000),(#63001,#63002,
#63003,#63004,#63005,#63006,#63007,#63008,#63009,#63010,#63011,#63012,#63013,
#63014,#63015,#63016,#63017,#63018,#63019,#63020,#63021,#63022,#63023,#63024,
#63025,#63026,#63027,#63028,#63029,#63030,#63031,#63032,#63033,#63034,#63035,
#63036,#63037,#63038,#63039,#63040,#63041,#63042,#63043,#63044,#63045,#63046,
#63047,#63048,#63049,#63050,#63051,#63052,#63053,#63054,#63055,#63056,#63057,
#63058,#63059,#63060,#63061,#63062,#63063,#63064,#63065,#63066,#63067,#63068,
#63069,#63070,#63071,#63072,#63073,#63074,#63075,#63076,#63077,#63078,#63079,
#63080,#63081,#63082,#63083,#63084,#63085,#63086,#63087,#63088,#63089,#63090,
#63091,#63092,#63093,#63094,#63095,#63096,#63097,#63098,#63099,#63100,#63101,
#63102,#63103,#63104,#63105,#63106)),.UNSPECIFIED.,.F.,.F.,.F.,(4,4),(4,
1,1,1,1,1,1,1,1,1,1,1,1,1,1,1,1,1,1,1,1,1,1,1,1,1,1,1,1,1,1,1,1,1,1,1,1,
1,1,1,1,1,1,1,1,1,1,1,1,1,1,1,1,1,1,1,1,1,1,1,1,1,1,1,1,1,1,1,1,1,1,1,1,
1,1,1,1,1,1,1,1,1,1,1,1,1,1,1,1,1,1,1,1,1,1,1,1,1,1,1,1,1,1,4),(0.,0.0460148164544132),
(11.6154215191105,12.6127573616628,13.610093204215,14.6074290467673,15.6047648893195,
16.6021007318718,17.599436574424,18.5967724169762,19.5941082595285,20.5914441020807,
21.588779944633,22.5861157871852,23.5834516297375,24.5807874722897,25.5781233148419,
26.5754591573942,27.5727949999464,28.5701308424987,29.5674666850509,30.5648025276032,
31.5621383701554,32.5594742127077,33.5568100552599,34.5541458978121,35.5514817403644,
36.5488175829166,37.5461534254689,38.5434892680211,39.5408251105734,40.5381609531256,
41.5354967956779,42.5328326382301,43.5301684807823,44.5275043233346,45.5248401658868,
46.5221760084391,47.5195118509913,48.5168476935436,49.5141835360958,50.5115193786481,
51.5088552212003,52.5061910637525,53.5035269063048,54.500862748857,55.4981985914093,
56.4955344339615,57.4928702765138,58.490206119066,59.4875419616182,60.4848778041705,
61.4822136467227,62.479549489275,63.4768853318272,64.4742211743795,65.4715570169317,
66.468892859484,67.4662287020362,68.4635645445884,69.4609003871407,70.4582362296929,
71.4555720722452,72.4529079147974,73.4502437573497,74.4475795999019,75.4449154424541,
76.4422512850064,77.4395871275586,78.4369229701109,79.4342588126631,80.4315946552154,
81.4289304977676,82.4262663403199,83.4236021828721,84.4209380254243,85.4182738679766,
86.4156097105288,87.4129455530811,88.4102813956333,89.4076172381856,90.4049530807378,
91.4022889232901,92.3996247658423,93.3969606083945,94.3942964509468,95.391632293499,
96.3889681360513,97.3863039786035,98.3836398211558,99.380975663708,100.37831150626,
101.375647348812,102.372983191365,103.370319033917,104.367654876469,105.364990719021,
106.362326561574,107.359662404126,108.356998246678,109.35433408923,110.351669931783,
111.349005774335,112.346341616887,113.343677459439,114.341013301992),
 .UNSPECIFIED.);
#265=B_SPLINE_SURFACE_WITH_KNOTS('',3,3,((#63226,#63227,#63228,#63229,#63230,
#63231,#63232,#63233,#63234,#63235,#63236,#63237,#63238,#63239,#63240,#63241,
#63242,#63243,#63244,#63245,#63246,#63247,#63248,#63249,#63250,#63251,#63252,
#63253,#63254,#63255,#63256,#63257,#63258,#63259,#63260,#63261,#63262,#63263,
#63264,#63265,#63266,#63267,#63268,#63269,#63270,#63271,#63272,#63273,#63274,
#63275,#63276,#63277,#63278,#63279,#63280,#63281,#63282,#63283,#63284,#63285,
#63286,#63287,#63288,#63289,#63290,#63291,#63292,#63293,#63294,#63295,#63296,
#63297,#63298,#63299,#63300,#63301,#63302,#63303,#63304,#63305,#63306,#63307,
#63308,#63309,#63310,#63311,#63312,#63313,#63314,#63315,#63316,#63317,#63318,
#63319,#63320,#63321,#63322,#63323,#63324,#63325,#63326,#63327,#63328,#63329,
#63330,#63331,#63332,#63333),(#63334,#63335,#63336,#63337,#63338,#63339,
#63340,#63341,#63342,#63343,#63344,#63345,#63346,#63347,#63348,#63349,#63350,
#63351,#63352,#63353,#63354,#63355,#63356,#63357,#63358,#63359,#63360,#63361,
#63362,#63363,#63364,#63365,#63366,#63367,#63368,#63369,#63370,#63371,#63372,
#63373,#63374,#63375,#63376,#63377,#63378,#63379,#63380,#63381,#63382,#63383,
#63384,#63385,#63386,#63387,#63388,#63389,#63390,#63391,#63392,#63393,#63394,
#63395,#63396,#63397,#63398,#63399,#63400,#63401,#63402,#63403,#63404,#63405,
#63406,#63407,#63408,#63409,#63410,#63411,#63412,#63413,#63414,#63415,#63416,
#63417,#63418,#63419,#63420,#63421,#63422,#63423,#63424,#63425,#63426,#63427,
#63428,#63429,#63430,#63431,#63432,#63433,#63434,#63435,#63436,#63437,#63438,
#63439,#63440,#63441),(#63442,#63443,#63444,#63445,#63446,#63447,#63448,
#63449,#63450,#63451,#63452,#63453,#63454,#63455,#63456,#63457,#63458,#63459,
#63460,#63461,#63462,#63463,#63464,#63465,#63466,#63467,#63468,#63469,#63470,
#63471,#63472,#63473,#63474,#63475,#63476,#63477,#63478,#63479,#63480,#63481,
#63482,#63483,#63484,#63485,#63486,#63487,#63488,#63489,#63490,#63491,#63492,
#63493,#63494,#63495,#63496,#63497,#63498,#63499,#63500,#63501,#63502,#63503,
#63504,#63505,#63506,#63507,#63508,#63509,#63510,#63511,#63512,#63513,#63514,
#63515,#63516,#63517,#63518,#63519,#63520,#63521,#63522,#63523,#63524,#63525,
#63526,#63527,#63528,#63529,#63530,#63531,#63532,#63533,#63534,#63535,#63536,
#63537,#63538,#63539,#63540,#63541,#63542,#63543,#63544,#63545,#63546,#63547,
#63548,#63549),(#63550,#63551,#63552,#63553,#63554,#63555,#63556,#63557,
#63558,#63559,#63560,#63561,#63562,#63563,#63564,#63565,#63566,#63567,#63568,
#63569,#63570,#63571,#63572,#63573,#63574,#63575,#63576,#63577,#63578,#63579,
#63580,#63581,#63582,#63583,#63584,#63585,#63586,#63587,#63588,#63589,#63590,
#63591,#63592,#63593,#63594,#63595,#63596,#63597,#63598,#63599,#63600,#63601,
#63602,#63603,#63604,#63605,#63606,#63607,#63608,#63609,#63610,#63611,#63612,
#63613,#63614,#63615,#63616,#63617,#63618,#63619,#63620,#63621,#63622,#63623,
#63624,#63625,#63626,#63627,#63628,#63629,#63630,#63631,#63632,#63633,#63634,
#63635,#63636,#63637,#63638,#63639,#63640,#63641,#63642,#63643,#63644,#63645,
#63646,#63647,#63648,#63649,#63650,#63651,#63652,#63653,#63654,#63655,#63656,
#63657)),.UNSPECIFIED.,.F.,.F.,.F.,(4,4),(4,1,1,1,1,1,1,1,1,1,1,1,1,1,1,
1,1,1,1,1,1,1,1,1,1,1,1,1,1,1,1,1,1,1,1,1,1,1,1,1,1,1,1,1,1,1,1,1,1,1,1,
1,1,1,1,1,1,1,1,1,1,1,1,1,1,1,1,1,1,1,1,1,1,1,1,1,1,1,1,1,1,1,1,1,1,1,1,
1,1,1,1,1,1,1,1,1,1,1,1,1,1,1,1,1,1,4),(0.,0.0460148164544132),(8.31058692273969,
9.30859389336977,10.3066008639999,11.30460783463,12.30261480526,13.3006217758901,
14.2986287465202,15.2966357171503,16.2946426877804,17.2926496584105,18.2906566290406,
19.2886635996707,20.2866705703008,21.2846775409308,22.2826845115609,23.280691482191,
24.2786984528211,25.2767054234512,26.2747123940813,27.2727193647114,28.2707263353415,
29.2687333059716,30.2667402766016,31.2647472472317,32.2627542178618,33.2607611884919,
34.258768159122,35.2567751297521,36.2547821003822,37.2527890710123,38.2507960416424,
39.2488030122724,40.2468099829025,41.2448169535326,42.2428239241627,43.2408308947928,
44.2388378654229,45.236844836053,46.2348518066831,47.2328587773132,48.2308657479432,
49.2288727185733,50.2268796892034,51.2248866598335,52.2228936304636,53.2209006010937,
54.2189075717238,55.2169145423539,56.214921512984,57.212928483614,58.2109354542441,
59.2089424248742,60.2069493955043,61.2049563661344,62.2029633367645,63.2009703073946,
64.1989772780247,65.1969842486548,66.1949912192848,67.1929981899149,68.191005160545,
69.1890121311751,70.1870191018052,71.1850260724353,72.1830330430654,73.1810400136955,
74.1790469843256,75.1770539549557,76.1750609255857,77.1730678962158,78.1710748668459,
79.169081837476,80.1670888081061,81.1650957787362,82.1631027493663,83.1611097199964,
84.1591166906264,85.1571236612565,86.1551306318866,87.1531376025167,88.1511445731468,
89.1491515437769,90.147158514407,91.1451654850371,92.1431724556672,93.1411794262973,
94.1391863969273,95.1371933675574,96.1352003381875,97.1332073088176,98.1312142794477,
99.1292212500778,100.127228220708,101.125235191338,102.123242161968,103.121249132598,
104.119256103228,105.117263073858,106.115270044488,107.113277015118,108.111283985749,
109.109290956379,110.107297927009,111.105304897639,112.103311868269,113.101318838899),
 .UNSPECIFIED.);
#1483=B_SPLINE_CURVE_WITH_KNOTS('',3,(#61234,#61235,#61236,#61237,#61238,
#61239,#61240,#61241,#61242,#61243),.UNSPECIFIED.,.F.,.F.,(4,3,3,4),(-4.09254174883833,
-3.98934337020898,-2.99200752765673,-2.06514013327813),.UNSPECIFIED.);
#1484=B_SPLINE_CURVE_WITH_KNOTS('',3,(#61246,#61247,#61248,#61249,#61250,
#61251,#61252),.UNSPECIFIED.,.F.,.F.,(4,3,4),(0.,0.998006970630082,1.11419103802948),
 .UNSPECIFIED.);
#1485=B_SPLINE_CURVE_WITH_KNOTS('',3,(#61257,#61258,#61259,#61260,#61261,
#61262,#61263,#61264,#61265,#61266,#61267,#61268,#61269,#61270,#61271,#61272,
#61273,#61274,#61275,#61276,#61277,#61278),.UNSPECIFIED.,.F.,.F.,(4,3,3,
3,3,3,3,4),(-10.3757270560179,-9.97335842552244,-8.9760225829702,-7.97868674041795,
-6.9813508978657,-5.98401505531347,-4.98667921276122,-4.09254174883833),
 .UNSPECIFIED.);
#1486=B_SPLINE_CURVE_WITH_KNOTS('',3,(#61279,#61280,#61281,#61282,#61283,
#61284,#61285,#61286,#61287,#61288,#61289,#61290,#61291,#61292,#61293,#61294,
#61295,#61296,#61297,#61298,#61299,#61300),.UNSPECIFIED.,.F.,.F.,(4,3,3,
3,3,3,3,4),(1.11419103802948,1.99601394126018,2.99402091189026,3.99202788252035,
4.99003485315045,5.98804182378054,6.98604879441062,7.39737634520907),
 .UNSPECIFIED.);
#1487=B_SPLINE_CURVE_WITH_KNOTS('',3,(#61305,#61306,#61307,#61308,#61309,
#61310,#61311,#61312,#61313,#61314,#61315,#61316,#61317,#61318,#61319,#61320,
#61321,#61322,#61323,#61324,#61325,#61326),.UNSPECIFIED.,.F.,.F.,(4,3,3,
3,3,3,3,4),(-16.6589123631975,-15.9573734808359,-14.9600376382837,-13.9627017957314,
-12.9653659531792,-11.9680301106269,-10.9706942680747,-10.3757270560179),
 .UNSPECIFIED.);
#1488=B_SPLINE_CURVE_WITH_KNOTS('',3,(#61327,#61328,#61329,#61330,#61331,
#61332,#61333,#61334,#61335,#61336,#61337,#61338,#61339,#61340,#61341,#61342,
#61343,#61344,#61345,#61346,#61347,#61348),.UNSPECIFIED.,.F.,.F.,(4,3,3,
3,3,3,3,4),(7.39737634520907,7.98405576504071,8.9820627356708,9.98006970630089,
10.978076676931,11.9760836475611,12.9740906181912,13.6805616523887),
 .UNSPECIFIED.);
#1489=B_SPLINE_CURVE_WITH_KNOTS('',3,(#61353,#61354,#61355,#61356,#61357,
#61358,#61359,#61360,#61361,#61362,#61363,#61364,#61365,#61366,#61367,#61368,
#61369,#61370,#61371,#61372,#61373,#61374,#61375,#61376,#61377),
 .UNSPECIFIED.,.F.,.F.,(4,3,3,3,3,3,3,3,4),(-22.9420976703771,-22.9387243787016,
-21.9413885361494,-20.9440526935971,-19.9467168510449,-18.9493810084926,
-17.9520451659404,-16.9547093233881,-16.6589123631975),.UNSPECIFIED.);
#1490=B_SPLINE_CURVE_WITH_KNOTS('',3,(#61378,#61379,#61380,#61381,#61382,
#61383,#61384,#61385,#61386,#61387,#61388,#61389,#61390,#61391,#61392,#61393,
#61394,#61395,#61396,#61397,#61398,#61399,#61400,#61401,#61402),
 .UNSPECIFIED.,.F.,.F.,(4,3,3,3,3,3,3,3,4),(13.6805616523887,13.9720975888212,
14.9701045594513,15.9681115300814,16.9661185007115,17.9641254713416,18.9621324419717,
19.9601394126018,19.9637469595682),.UNSPECIFIED.);
#1491=B_SPLINE_CURVE_WITH_KNOTS('',3,(#61407,#61408,#61409,#61410,#61411,
#61412,#61413,#61414,#61415,#61416,#61417,#61418,#61419,#61420,#61421,#61422,
#61423,#61424,#61425,#61426,#61427,#61428),.UNSPECIFIED.,.F.,.F.,(4,3,3,
3,3,3,3,4),(-29.2252829775567,-28.9227394340151,-27.9254035914628,-26.9280677489106,
-25.9307319063583,-24.9333960638061,-23.9360602212539,-22.9420976703771),
 .UNSPECIFIED.);
#1492=B_SPLINE_CURVE_WITH_KNOTS('',3,(#61429,#61430,#61431,#61432,#61433,
#61434,#61435,#61436,#61437,#61438,#61439,#61440,#61441,#61442,#61443,#61444,
#61445,#61446,#61447,#61448,#61449,#61450),.UNSPECIFIED.,.F.,.F.,(4,3,3,
3,3,3,3,4),(19.9637469595682,20.9581463832319,21.956153353862,22.954160324492,
23.9521672951221,24.9501742657522,25.9481812363823,26.2469322667478),
 .UNSPECIFIED.);
#1493=B_SPLINE_CURVE_WITH_KNOTS('',3,(#61455,#61456,#61457,#61458,#61459,
#61460,#61461,#61462,#61463,#61464,#61465,#61466,#61467,#61468,#61469,#61470,
#61471,#61472,#61473,#61474,#61475,#61476),.UNSPECIFIED.,.F.,.F.,(4,3,3,
3,3,3,3,4),(-35.5084682847363,-34.9067544893285,-33.9094186467763,-32.9120828042241,
-31.9147469616718,-30.9174111191196,-29.9200752765673,-29.2252829775567),
 .UNSPECIFIED.);
#1494=B_SPLINE_CURVE_WITH_KNOTS('',3,(#61477,#61478,#61479,#61480,#61481,
#61482,#61483,#61484,#61485,#61486,#61487,#61488,#61489,#61490,#61491,#61492,
#61493,#61494,#61495,#61496,#61497,#61498),.UNSPECIFIED.,.F.,.F.,(4,3,3,
3,3,3,3,4),(26.2469322667478,26.9461882070124,27.9441951776425,28.9422021482726,
29.9402091189027,30.9382160895327,31.9362230601628,32.5301175739274),
 .UNSPECIFIED.);
#1495=B_SPLINE_CURVE_WITH_KNOTS('',3,(#61503,#61504,#61505,#61506,#61507,
#61508,#61509,#61510,#61511,#61512,#61513,#61514,#61515,#61516,#61517,#61518,
#61519,#61520,#61521,#61522,#61523,#61524),.UNSPECIFIED.,.F.,.F.,(4,3,3,
3,3,3,3,4),(-41.7916535919159,-40.890769544642,-39.8934337020898,-38.8960978595375,
-37.8987620169853,-36.901426174433,-35.9040903318808,-35.5084682847363),
 .UNSPECIFIED.);
#1496=B_SPLINE_CURVE_WITH_KNOTS('',3,(#61525,#61526,#61527,#61528,#61529,
#61530,#61531,#61532,#61533,#61534,#61535,#61536,#61537,#61538,#61539,#61540,
#61541,#61542,#61543,#61544,#61545,#61546),.UNSPECIFIED.,.F.,.F.,(4,3,3,
3,3,3,3,4),(32.5301175739274,32.9342300307929,33.932237001423,34.9302439720531,
35.9282509426832,36.9262579133133,37.9242648839434,38.813302881107),
 .UNSPECIFIED.);
#1497=B_SPLINE_CURVE_WITH_KNOTS('',3,(#61551,#61552,#61553,#61554,#61555,
#61556,#61557,#61558,#61559,#61560,#61561,#61562,#61563,#61564,#61565,#61566,
#61567,#61568,#61569,#61570,#61571,#61572,#61573,#61574,#61575),
 .UNSPECIFIED.,.F.,.F.,(4,3,3,3,3,3,3,3,4),(-48.0748388990955,-47.8721204425077,
-46.8747845999555,-45.8774487574032,-44.880112914851,-43.8827770722987,
-42.8854412297465,-41.8881053871943,-41.7916535919159),.UNSPECIFIED.);
#1498=B_SPLINE_CURVE_WITH_KNOTS('',3,(#61576,#61577,#61578,#61579,#61580,
#61581,#61582,#61583,#61584,#61585,#61586,#61587,#61588,#61589,#61590,#61591,
#61592,#61593,#61594,#61595,#61596,#61597,#61598,#61599,#61600),
 .UNSPECIFIED.,.F.,.F.,(4,3,3,3,3,3,3,3,4),(38.813302881107,38.9222718545735,
39.9202788252036,40.9182857958337,41.9162927664637,42.9142997370938,43.9123067077239,
44.910313678354,45.0964881882866),.UNSPECIFIED.);
#1499=B_SPLINE_CURVE_WITH_KNOTS('',3,(#61605,#61606,#61607,#61608,#61609,
#61610,#61611,#61612,#61613,#61614,#61615,#61616,#61617,#61618,#61619,#61620,
#61621,#61622,#61623,#61624,#61625,#61626),.UNSPECIFIED.,.F.,.F.,(4,3,3,
3,3,3,3,4),(-54.3580242062751,-53.8561354978212,-52.8587996552689,-51.8614638127167,
-50.8641279701645,-49.8667921276122,-48.86945628506,-48.0748388990955),
 .UNSPECIFIED.);
#1500=B_SPLINE_CURVE_WITH_KNOTS('',3,(#61627,#61628,#61629,#61630,#61631,
#61632,#61633,#61634,#61635,#61636,#61637,#61638,#61639,#61640,#61641,#61642,
#61643,#61644,#61645,#61646,#61647,#61648),.UNSPECIFIED.,.F.,.F.,(4,3,3,
3,3,3,3,4),(45.0964881882866,45.9083206489841,46.9063276196142,47.9043345902443,
48.9023415608744,49.9003485315045,50.8983555021345,51.3796734954662),
 .UNSPECIFIED.);
#1501=B_SPLINE_CURVE_WITH_KNOTS('',3,(#61653,#61654,#61655,#61656,#61657,
#61658,#61659,#61660,#61661,#61662,#61663,#61664,#61665,#61666,#61667,#61668,
#61669,#61670,#61671,#61672,#61673,#61674),.UNSPECIFIED.,.F.,.F.,(4,3,3,
3,3,3,3,4),(-60.6412095134546,-59.8401505531347,-58.8428147105824,-57.8454788680302,
-56.8481430254779,-55.8508071829257,-54.8534713403734,-54.3580242062751),
 .UNSPECIFIED.);
#1502=B_SPLINE_CURVE_WITH_KNOTS('',3,(#61675,#61676,#61677,#61678,#61679,
#61680,#61681,#61682,#61683,#61684,#61685,#61686,#61687,#61688,#61689,#61690,
#61691,#61692,#61693,#61694,#61695,#61696),.UNSPECIFIED.,.F.,.F.,(4,3,3,
3,3,3,3,4),(51.3796734954662,51.8963624727646,52.8943694433947,53.8923764140248,
54.8903833846549,55.888390355285,56.8863973259151,57.6628588026458),
 .UNSPECIFIED.);
#1503=B_SPLINE_CURVE_WITH_KNOTS('',3,(#61701,#61702,#61703,#61704,#61705,
#61706,#61707,#61708,#61709,#61710,#61711,#61712,#61713,#61714,#61715,#61716,
#61717,#61718,#61719,#61720,#61721,#61722,#61723,#61724,#61725),
 .UNSPECIFIED.,.F.,.F.,(4,3,3,3,3,3,3,3,4),(-66.9243948206342,-66.8215014510004,
-65.8241656084481,-64.8268297658959,-63.8294939233436,-62.8321580807914,
-61.8348222382391,-60.8374863956869,-60.6412095134546),.UNSPECIFIED.);
#1504=B_SPLINE_CURVE_WITH_KNOTS('',3,(#61726,#61727,#61728,#61729,#61730,
#61731,#61732,#61733,#61734,#61735,#61736,#61737,#61738,#61739,#61740,#61741,
#61742,#61743,#61744,#61745,#61746,#61747,#61748,#61749,#61750),
 .UNSPECIFIED.,.F.,.F.,(4,3,3,3,3,3,3,3,4),(57.6628588026458,57.8844042965452,
58.8824112671752,59.8804182378054,60.8784252084354,61.8764321790655,62.8744391496956,
63.8724461203257,63.9460441098254),.UNSPECIFIED.);
#1505=B_SPLINE_CURVE_WITH_KNOTS('',3,(#61755,#61756,#61757,#61758,#61759,
#61760,#61761,#61762,#61763,#61764,#61765,#61766,#61767,#61768,#61769,#61770,
#61771,#61772,#61773,#61774,#61775,#61776),.UNSPECIFIED.,.F.,.F.,(4,3,3,
3,3,3,3,4),(-73.2075801278138,-72.8055165063138,-71.8081806637616,-70.8108448212093,
-69.8135089786571,-68.8161731361048,-67.8188372935526,-66.9243948206342),
 .UNSPECIFIED.);
#1506=B_SPLINE_CURVE_WITH_KNOTS('',3,(#61777,#61778,#61779,#61780,#61781,
#61782,#61783,#61784,#61785,#61786,#61787,#61788,#61789,#61790,#61791,#61792,
#61793,#61794,#61795,#61796,#61797,#61798),.UNSPECIFIED.,.F.,.F.,(4,3,3,
3,3,3,3,4),(63.9460441098254,64.8704530909558,65.8684600615859,66.866467032216,
67.8644740028461,68.8624809734761,69.8604879441062,70.229229417005),
 .UNSPECIFIED.);
#1507=B_SPLINE_CURVE_WITH_KNOTS('',3,(#61803,#61804,#61805,#61806,#61807,
#61808,#61809,#61810,#61811,#61812,#61813,#61814,#61815,#61816,#61817,#61818,
#61819,#61820,#61821,#61822,#61823,#61824),.UNSPECIFIED.,.F.,.F.,(4,3,3,
3,3,3,3,4),(-79.4907654349934,-78.7895315616273,-77.792195719075,-76.7948598765228,
-75.7975240339705,-74.8001881914183,-73.802852348866,-73.2075801278138),
 .UNSPECIFIED.);
#1508=B_SPLINE_CURVE_WITH_KNOTS('',3,(#61825,#61826,#61827,#61828,#61829,
#61830,#61831,#61832,#61833,#61834,#61835,#61836,#61837,#61838,#61839,#61840,
#61841,#61842,#61843,#61844,#61845,#61846),.UNSPECIFIED.,.F.,.F.,(4,3,3,
3,3,3,3,4),(70.229229417005,70.8584949147363,71.8565018853664,72.8545088559965,
73.8525158266266,74.8505227972567,75.8485297678868,76.5124147241846),
 .UNSPECIFIED.);
#1509=B_SPLINE_CURVE_WITH_KNOTS('',3,(#61851,#61852,#61853,#61854,#61855,
#61856,#61857,#61858,#61859,#61860,#61861,#61862,#61863,#61864,#61865,#61866,
#61867,#61868,#61869,#61870,#61871,#61872,#61873,#61874,#61875),
 .UNSPECIFIED.,.F.,.F.,(4,3,3,3,3,3,3,3,4),(-85.773950742173,-85.770882459493,
-84.7735466169407,-83.7762107743885,-82.7788749318363,-81.781539089284,
-80.7842032467318,-79.7868674041795,-79.4907654349934),.UNSPECIFIED.);
#1510=B_SPLINE_CURVE_WITH_KNOTS('',3,(#61876,#61877,#61878,#61879,#61880,
#61881,#61882,#61883,#61884,#61885,#61886,#61887,#61888,#61889,#61890,#61891,
#61892,#61893,#61894,#61895,#61896,#61897),.UNSPECIFIED.,.F.,.F.,(4,3,3,
3,3,3,3,4),(76.5124147241846,76.8465367385169,77.8445437091469,78.842550679777,
79.8405576504071,80.8385646210372,81.8365715916673,82.7956000313642),
 .UNSPECIFIED.);
#1511=B_SPLINE_CURVE_WITH_KNOTS('',3,(#61902,#61903,#61904,#61905,#61906,
#61907,#61908,#61909,#61910,#61911,#61912,#61913,#61914,#61915,#61916,#61917,
#61918,#61919,#61920,#61921,#61922,#61923),.UNSPECIFIED.,.F.,.F.,(4,3,3,
3,3,3,3,4),(-92.0571360493526,-91.7548975148065,-90.7575616722542,-89.760225829702,
-88.7628899871497,-87.7655541445975,-86.7682183020452,-85.773950742173),
 .UNSPECIFIED.);
#1512=B_SPLINE_CURVE_WITH_KNOTS('',3,(#61924,#61925,#61926,#61927,#61928,
#61929,#61930,#61931,#61932,#61933,#61934,#61935,#61936,#61937,#61938,#61939,
#61940,#61941,#61942,#61943,#61944,#61945,#61946,#61947,#61948),
 .UNSPECIFIED.,.F.,.F.,(4,3,3,3,3,3,3,3,4),(82.7956000313642,82.8345785622974,
83.8325855329275,84.8305925035576,85.8285994741877,86.8266064448178,87.8246134154479,
88.822620386078,89.0787853385438),.UNSPECIFIED.);
#1513=B_SPLINE_CURVE_WITH_KNOTS('',3,(#61953,#61954,#61955,#61956,#61957,
#61958,#61959,#61960,#61961,#61962,#61963,#61964,#61965,#61966,#61967,#61968,
#61969,#61970,#61971,#61972,#61973,#61974),.UNSPECIFIED.,.F.,.F.,(4,3,3,
3,3,3,3,4),(-98.3403213565322,-97.7389125701199,-96.7415767275677,-95.7442408850154,
-94.7469050424632,-93.7495691999109,-92.7522333573587,-92.0571360493526),
 .UNSPECIFIED.);
#1514=B_SPLINE_CURVE_WITH_KNOTS('',3,(#61975,#61976,#61977,#61978,#61979,
#61980,#61981,#61982,#61983,#61984,#61985,#61986,#61987,#61988,#61989,#61990,
#61991,#61992,#61993,#61994,#61995,#61996),.UNSPECIFIED.,.F.,.F.,(4,3,3,
3,3,3,3,4),(89.0787853385438,89.820627356708,90.8186343273381,91.8166412979682,
92.8146482685983,93.8126552392284,94.8106622098585,95.3619706457233),
 .UNSPECIFIED.);
#1515=B_SPLINE_CURVE_WITH_KNOTS('',3,(#62002,#62003,#62004,#62005,#62006,
#62007,#62008,#62009),.UNSPECIFIED.,.F.,.F.,(4,1,1,1,1,4),(109.955742875643,
110.351669931783,111.349005774335,112.346341616887,113.343677459439,114.341013301992),
 .UNSPECIFIED.);
#1516=B_SPLINE_CURVE_WITH_KNOTS('',3,(#62012,#62013,#62014,#62015,#62016,
#62017,#62018),.UNSPECIFIED.,.F.,.F.,(4,1,1,1,4),(109.955742875643,110.107297927009,
111.105304897639,112.103311868269,113.101318838899),.UNSPECIFIED.);
#1517=B_SPLINE_CURVE_WITH_KNOTS('',3,(#62023,#62024,#62025,#62026,#62027,
#62028,#62029,#62030,#62031,#62032),.UNSPECIFIED.,.F.,.F.,(4,1,1,1,1,1,
1,4),(103.672557568463,104.367654876469,105.364990719021,106.362326561574,
107.359662404126,108.356998246678,109.35433408923,109.955742875643),
 .UNSPECIFIED.);
#1518=B_SPLINE_CURVE_WITH_KNOTS('',3,(#62033,#62034,#62035,#62036,#62037,
#62038,#62039,#62040,#62041,#62042),.UNSPECIFIED.,.F.,.F.,(4,1,1,1,1,1,
1,4),(103.672557568463,104.119256103228,105.117263073858,106.115270044488,
107.113277015118,108.111283985749,109.109290956379,109.955742875643),
 .UNSPECIFIED.);
#1519=B_SPLINE_CURVE_WITH_KNOTS('',3,(#62047,#62048,#62049,#62050,#62051,
#62052,#62053,#62054,#62055,#62056),.UNSPECIFIED.,.F.,.F.,(4,1,1,1,1,1,
1,4),(97.3893722612836,98.3836398211558,99.380975663708,100.37831150626,
101.375647348812,102.372983191365,103.370319033917,103.672557568463),
 .UNSPECIFIED.);
#1520=B_SPLINE_CURVE_WITH_KNOTS('',3,(#62057,#62058,#62059,#62060,#62061,
#62062,#62063,#62064,#62065,#62066),.UNSPECIFIED.,.F.,.F.,(4,1,1,1,1,1,
1,4),(97.3893722612836,98.1312142794477,99.1292212500778,100.127228220708,
101.125235191338,102.123242161968,103.121249132598,103.672557568463),
 .UNSPECIFIED.);
#1521=B_SPLINE_CURVE_WITH_KNOTS('',3,(#62071,#62072,#62073,#62074,#62075,
#62076,#62077,#62078,#62079,#62080,#62081),.UNSPECIFIED.,.F.,.F.,(4,1,1,
1,1,1,1,1,4),(91.106186954104,91.4022889232901,92.3996247658423,93.3969606083945,
94.3942964509468,95.391632293499,96.3889681360513,97.3863039786035,97.3893722612836),
 .UNSPECIFIED.);
#1522=B_SPLINE_CURVE_WITH_KNOTS('',3,(#62082,#62083,#62084,#62085,#62086,
#62087,#62088,#62089,#62090,#62091,#62092),.UNSPECIFIED.,.F.,.F.,(4,1,1,
1,1,1,1,1,4),(91.106186954104,91.1451654850371,92.1431724556672,93.1411794262973,
94.1391863969273,95.1371933675574,96.1352003381875,97.1332073088176,97.3893722612836),
 .UNSPECIFIED.);
#1523=B_SPLINE_CURVE_WITH_KNOTS('',3,(#62097,#62098,#62099,#62100,#62101,
#62102,#62103,#62104,#62105,#62106),.UNSPECIFIED.,.F.,.F.,(4,1,1,1,1,1,
1,4),(84.8230016469244,85.4182738679766,86.4156097105288,87.4129455530811,
88.4102813956333,89.4076172381856,90.4049530807378,91.106186954104),
 .UNSPECIFIED.);
#1524=B_SPLINE_CURVE_WITH_KNOTS('',3,(#62107,#62108,#62109,#62110,#62111,
#62112,#62113,#62114,#62115,#62116),.UNSPECIFIED.,.F.,.F.,(4,1,1,1,1,1,
1,4),(84.8230016469244,85.1571236612565,86.1551306318866,87.1531376025167,
88.1511445731468,89.1491515437769,90.147158514407,91.106186954104),
 .UNSPECIFIED.);
#1525=B_SPLINE_CURVE_WITH_KNOTS('',3,(#62121,#62122,#62123,#62124,#62125,
#62126,#62127,#62128,#62129,#62130),.UNSPECIFIED.,.F.,.F.,(4,1,1,1,1,1,
1,4),(78.5398163397448,79.4342588126631,80.4315946552154,81.4289304977676,
82.4262663403199,83.4236021828721,84.4209380254243,84.8230016469244),
 .UNSPECIFIED.);
#1526=B_SPLINE_CURVE_WITH_KNOTS('',3,(#62131,#62132,#62133,#62134,#62135,
#62136,#62137,#62138,#62139,#62140),.UNSPECIFIED.,.F.,.F.,(4,1,1,1,1,1,
1,4),(78.5398163397448,79.169081837476,80.1670888081061,81.1650957787362,
82.1631027493663,83.1611097199964,84.1591166906264,84.8230016469244),
 .UNSPECIFIED.);
#1527=B_SPLINE_CURVE_WITH_KNOTS('',3,(#62145,#62146,#62147,#62148,#62149,
#62150,#62151,#62152,#62153,#62154,#62155),.UNSPECIFIED.,.F.,.F.,(4,1,1,
1,1,1,1,1,4),(72.2566310325652,72.4529079147974,73.4502437573497,74.4475795999019,
75.4449154424541,76.4422512850064,77.4395871275586,78.4369229701109,78.5398163397448),
 .UNSPECIFIED.);
#1528=B_SPLINE_CURVE_WITH_KNOTS('',3,(#62156,#62157,#62158,#62159,#62160,
#62161,#62162,#62163,#62164,#62165),.UNSPECIFIED.,.F.,.F.,(4,1,1,1,1,1,
1,4),(72.2566310325652,73.1810400136955,74.1790469843256,75.1770539549557,
76.1750609255857,77.1730678962158,78.1710748668459,78.5398163397448),
 .UNSPECIFIED.);
#1529=B_SPLINE_CURVE_WITH_KNOTS('',3,(#62170,#62171,#62172,#62173,#62174,
#62175,#62176,#62177,#62178,#62179),.UNSPECIFIED.,.F.,.F.,(4,1,1,1,1,1,
1,4),(65.9734457253856,66.468892859484,67.4662287020362,68.4635645445884,
69.4609003871407,70.4582362296929,71.4555720722452,72.2566310325652),
 .UNSPECIFIED.);
#1530=B_SPLINE_CURVE_WITH_KNOTS('',3,(#62180,#62181,#62182,#62183,#62184,
#62185,#62186,#62187,#62188,#62189,#62190),.UNSPECIFIED.,.F.,.F.,(4,1,1,
1,1,1,1,1,4),(65.9734457253856,66.1949912192848,67.1929981899149,68.191005160545,
69.1890121311751,70.1870191018052,71.1850260724353,72.1830330430654,72.2566310325652),
 .UNSPECIFIED.);
#1531=B_SPLINE_CURVE_WITH_KNOTS('',3,(#62195,#62196,#62197,#62198,#62199,
#62200,#62201,#62202,#62203,#62204),.UNSPECIFIED.,.F.,.F.,(4,1,1,1,1,1,
1,4),(59.690260418206,60.4848778041705,61.4822136467227,62.479549489275,
63.4768853318272,64.4742211743795,65.4715570169317,65.9734457253856),
 .UNSPECIFIED.);
#1532=B_SPLINE_CURVE_WITH_KNOTS('',3,(#62205,#62206,#62207,#62208,#62209,
#62210,#62211,#62212,#62213,#62214),.UNSPECIFIED.,.F.,.F.,(4,1,1,1,1,1,
1,4),(59.690260418206,60.2069493955043,61.2049563661344,62.2029633367645,
63.2009703073946,64.1989772780247,65.1969842486548,65.9734457253856),
 .UNSPECIFIED.);
#1533=B_SPLINE_CURVE_WITH_KNOTS('',3,(#62219,#62220,#62221,#62222,#62223,
#62224,#62225,#62226,#62227,#62228,#62229),.UNSPECIFIED.,.F.,.F.,(4,1,1,
1,1,1,1,1,4),(53.4070751110265,53.5035269063048,54.500862748857,55.4981985914093,
56.4955344339615,57.4928702765138,58.490206119066,59.4875419616182,59.690260418206),
 .UNSPECIFIED.);
#1534=B_SPLINE_CURVE_WITH_KNOTS('',3,(#62230,#62231,#62232,#62233,#62234,
#62235,#62236,#62237,#62238,#62239),.UNSPECIFIED.,.F.,.F.,(4,1,1,1,1,1,
1,4),(53.4070751110264,54.2189075717238,55.2169145423539,56.214921512984,
57.212928483614,58.2109354542441,59.2089424248742,59.690260418206),
 .UNSPECIFIED.);
#1535=B_SPLINE_CURVE_WITH_KNOTS('',3,(#62244,#62245,#62246,#62247,#62248,
#62249,#62250,#62251,#62252,#62253),.UNSPECIFIED.,.F.,.F.,(4,1,1,1,1,1,
1,4),(47.1238898038469,47.5195118509913,48.5168476935436,49.5141835360958,
50.5115193786481,51.5088552212003,52.5061910637525,53.4070751110265),
 .UNSPECIFIED.);
#1536=B_SPLINE_CURVE_WITH_KNOTS('',3,(#62254,#62255,#62256,#62257,#62258,
#62259,#62260,#62261,#62262,#62263,#62264),.UNSPECIFIED.,.F.,.F.,(4,1,1,
1,1,1,1,1,4),(47.1238898038468,47.2328587773132,48.2308657479432,49.2288727185733,
50.2268796892034,51.2248866598335,52.2228936304636,53.2209006010937,53.4070751110264),
 .UNSPECIFIED.);
#1537=B_SPLINE_CURVE_WITH_KNOTS('',3,(#62269,#62270,#62271,#62272,#62273,
#62274,#62275,#62276,#62277,#62278),.UNSPECIFIED.,.F.,.F.,(4,1,1,1,1,1,
1,4),(40.8407044966673,41.5354967956779,42.5328326382301,43.5301684807823,
44.5275043233346,45.5248401658868,46.5221760084391,47.1238898038469),
 .UNSPECIFIED.);
#1538=B_SPLINE_CURVE_WITH_KNOTS('',3,(#62279,#62280,#62281,#62282,#62283,
#62284,#62285,#62286,#62287,#62288),.UNSPECIFIED.,.F.,.F.,(4,1,1,1,1,1,
1,4),(40.8407044966672,41.2448169535326,42.2428239241627,43.2408308947928,
44.2388378654229,45.236844836053,46.2348518066831,47.1238898038468),
 .UNSPECIFIED.);
#1539=B_SPLINE_CURVE_WITH_KNOTS('',3,(#62293,#62294,#62295,#62296,#62297,
#62298,#62299,#62300,#62301,#62302),.UNSPECIFIED.,.F.,.F.,(4,1,1,1,1,1,
1,4),(34.5575191894877,35.5514817403644,36.5488175829166,37.5461534254689,
38.5434892680211,39.5408251105734,40.5381609531256,40.8407044966673),
 .UNSPECIFIED.);
#1540=B_SPLINE_CURVE_WITH_KNOTS('',3,(#62303,#62304,#62305,#62306,#62307,
#62308,#62309,#62310,#62311,#62312),.UNSPECIFIED.,.F.,.F.,(4,1,1,1,1,1,
1,4),(34.5575191894876,35.2567751297521,36.2547821003822,37.2527890710123,
38.2507960416424,39.2488030122724,40.2468099829025,40.8407044966672),
 .UNSPECIFIED.);
#1541=B_SPLINE_CURVE_WITH_KNOTS('',3,(#62317,#62318,#62319,#62320,#62321,
#62322,#62323,#62324,#62325,#62326,#62327),.UNSPECIFIED.,.F.,.F.,(4,1,1,
1,1,1,1,1,4),(28.2743338823081,28.5701308424987,29.5674666850509,30.5648025276032,
31.5621383701554,32.5594742127077,33.5568100552599,34.5541458978121,34.5575191894877),
 .UNSPECIFIED.);
#1542=B_SPLINE_CURVE_WITH_KNOTS('',3,(#62328,#62329,#62330,#62331,#62332,
#62333,#62334,#62335,#62336,#62337),.UNSPECIFIED.,.F.,.F.,(4,1,1,1,1,1,
1,4),(28.274333882308,29.2687333059716,30.2667402766016,31.2647472472317,
32.2627542178618,33.2607611884919,34.258768159122,34.5575191894876),
 .UNSPECIFIED.);
#1543=B_SPLINE_CURVE_WITH_KNOTS('',3,(#62342,#62343,#62344,#62345,#62346,
#62347,#62348,#62349,#62350,#62351),.UNSPECIFIED.,.F.,.F.,(4,1,1,1,1,1,
1,4),(21.9911485751285,22.5861157871852,23.5834516297375,24.5807874722897,
25.5781233148419,26.5754591573942,27.5727949999464,28.2743338823081),
 .UNSPECIFIED.);
#1544=B_SPLINE_CURVE_WITH_KNOTS('',3,(#62352,#62353,#62354,#62355,#62356,
#62357,#62358,#62359,#62360,#62361,#62362),.UNSPECIFIED.,.F.,.F.,(4,1,1,
1,1,1,1,1,4),(21.9911485751285,22.2826845115609,23.280691482191,24.2786984528211,
25.2767054234512,26.2747123940813,27.2727193647114,28.2707263353415,28.274333882308),
 .UNSPECIFIED.);
#1545=B_SPLINE_CURVE_WITH_KNOTS('',3,(#62367,#62368,#62369,#62370,#62371,
#62372,#62373,#62374,#62375,#62376),.UNSPECIFIED.,.F.,.F.,(4,1,1,1,1,1,
1,4),(15.7079632679489,16.6021007318718,17.599436574424,18.5967724169762,
19.5941082595285,20.5914441020807,21.588779944633,21.9911485751285),
 .UNSPECIFIED.);
#1546=B_SPLINE_CURVE_WITH_KNOTS('',3,(#62377,#62378,#62379,#62380,#62381,
#62382,#62383,#62384,#62385,#62386),.UNSPECIFIED.,.F.,.F.,(4,1,1,1,1,1,
1,4),(15.7079632679489,16.2946426877804,17.2926496584105,18.2906566290406,
19.2886635996707,20.2866705703008,21.2846775409308,21.9911485751285),
 .UNSPECIFIED.);
#1547=B_SPLINE_CURVE_WITH_KNOTS('',3,(#62389,#62390,#62391,#62392,#62393,
#62394,#62395,#62396,#62397,#62398,#62399,#62400,#62401,#62402,#62403,#62404,
#62405,#62406,#62407,#62408,#62409,#62410,#62411,#62412,#62413,#62414,#62415,
#62416,#62417,#62418,#62419,#62420,#62421,#62422,#62423,#62424,#62425,#62426,
#62427,#62428,#62429,#62430,#62431,#62432,#62433,#62434,#62435,#62436,#62437,
#62438,#62439,#62440,#62441,#62442,#62443,#62444,#62445,#62446,#62447,#62448,
#62449,#62450,#62451,#62452,#62453,#62454,#62455,#62456,#62457,#62458,#62459,
#62460,#62461,#62462,#62463,#62464,#62465,#62466,#62467,#62468,#62469,#62470,
#62471,#62472,#62473,#62474,#62475,#62476,#62477,#62478,#62479,#62480,#62481,
#62482,#62483,#62484,#62485,#62486,#62487,#62488,#62489,#62490,#62491,#62492,
#62493,#62494,#62495,#62496,#62497,#62498,#62499,#62500,#62501,#62502,#62503,
#62504,#62505,#62506,#62507,#62508,#62509,#62510,#62511,#62512,#62513,#62514,
#62515),.UNSPECIFIED.,.F.,.F.,(4,3,3,3,3,3,3,3,3,3,3,3,3,3,3,3,3,3,3,3,
3,3,3,3,3,3,3,3,3,3,3,3,3,3,3,3,3,3,3,3,3,3,4),(-0.996917990983956,-0.978871588953361,
-0.96111138213616,-0.951572166884024,-0.94788730271085,-0.928958746515757,
-0.909876465942473,-0.904936500084987,-0.901848009849201,-0.882541837721487,
-0.863353532865677,-0.850071733640713,-0.842096384739765,-0.838733342910066,
-0.836789934415749,-0.818254783653573,-0.798902591036692,-0.782735584954257,
-0.778204258927876,-0.774298497031817,-0.75473106557298,-0.734923369072796,
-0.7185841623989,-0.712646708603056,-0.709110058221935,-0.689189804001172,
-0.669566542377212,-0.649891129487148,-0.644972000047888,-0.641670824784499,
-0.621885476350888,-0.601705353300825,-0.588427767916722,-0.579820295317846,
-0.575107459303169,-0.554609906499435,-0.53420632583291,-0.514845498030454,
-0.510394870356688,-0.506773348856668,-0.495484670227998,-0.475532816008266,
-0.468408511919796),.UNSPECIFIED.);
#1548=B_SPLINE_CURVE_WITH_KNOTS('',3,(#62517,#62518,#62519,#62520,#62521,
#62522,#62523,#62524,#62525,#62526,#62527,#62528,#62529,#62530,#62531,#62532,
#62533,#62534,#62535,#62536,#62537,#62538,#62539,#62540,#62541,#62542,#62543,
#62544,#62545,#62546,#62547,#62548,#62549,#62550,#62551,#62552,#62553,#62554,
#62555,#62556,#62557,#62558,#62559,#62560,#62561,#62562,#62563,#62564,#62565,
#62566,#62567,#62568,#62569,#62570,#62571,#62572,#62573,#62574),
 .UNSPECIFIED.,.F.,.F.,(4,3,3,3,3,3,3,3,3,3,3,3,3,3,3,3,3,3,3,4),(-0.271362855059921,
-0.249815156703991,-0.228817954605844,-0.214757059032555,-0.202695986178297,
-0.199258382274391,-0.179079040584676,-0.172574372312687,-0.151002575773601,
-0.132127253801901,-0.128545223737615,-0.108660382312346,-0.0889046320299183,
-0.0695673553379917,-0.0643976613730527,-0.0611873083345303,-0.0424332578302701,
-0.0240014673407122,-0.00610701619818059,0.),.UNSPECIFIED.);
#1549=B_SPLINE_CURVE_WITH_KNOTS('',3,(#62577,#62578,#62579,#62580,#62581,
#62582,#62583,#62584,#62585,#62586,#62587,#62588,#62589,#62590,#62591,#62592,
#62593,#62594,#62595,#62596,#62597,#62598,#62599,#62600,#62601,#62602,#62603,
#62604,#62605,#62606,#62607,#62608,#62609,#62610,#62611,#62612,#62613,#62614,
#62615,#62616,#62617,#62618,#62619,#62620,#62621,#62622,#62623,#62624,#62625,
#62626,#62627,#62628,#62629,#62630,#62631,#62632,#62633,#62634,#62635,#62636,
#62637,#62638,#62639,#62640,#62641,#62642,#62643,#62644,#62645,#62646,#62647,
#62648,#62649,#62650,#62651,#62652,#62653,#62654,#62655,#62656,#62657,#62658,
#62659,#62660,#62661,#62662,#62663,#62664,#62665,#62666,#62667,#62668,#62669,
#62670,#62671,#62672,#62673,#62674,#62675,#62676,#62677,#62678,#62679),
 .UNSPECIFIED.,.F.,.F.,(4,3,3,3,3,3,3,3,3,3,3,3,3,3,3,3,3,3,3,3,3,3,3,3,
3,3,3,3,3,3,3,3,3,3,4),(-0.468408511919796,-0.449159592277506,-0.442679572366002,
-0.439139523917826,-0.418501747794262,-0.397540534942074,-0.376759689901926,
-0.369408338867191,-0.366188435771172,-0.344993296658329,-0.324164935680159,
-0.314417154781481,-0.302674036643168,-0.298303152413865,-0.294792657786698,
-0.273759483634418,-0.252453791079512,-0.23671297526563,-0.228622459040654,
-0.22484613779528,-0.221071692886511,-0.199520974492535,-0.177947952659577,
-0.156760757052952,-0.151824997028116,-0.148277425274246,-0.12652726456846,
-0.105236270462937,-0.0835127492652271,-0.0784406535722348,-0.0733870619889256,
-0.0516031153801045,-0.029512914496819,-0.0074997402847098,0.),
 .UNSPECIFIED.);
#1550=B_SPLINE_CURVE_WITH_KNOTS('',3,(#63108,#63109,#63110,#63111,#63112,
#63113,#63114,#63115),.UNSPECIFIED.,.F.,.F.,(4,1,1,1,1,4),(11.6154215191105,
12.6127573616628,13.610093204215,14.6074290467673,15.6047648893195,15.7079632679489),
 .UNSPECIFIED.);
#1551=B_SPLINE_CURVE_WITH_KNOTS('',3,(#63116,#63117,#63118,#63119,#63120,
#63121,#63122,#63123,#63124,#63125,#63126,#63127,#63128,#63129,#63130,#63131,
#63132,#63133,#63134,#63135,#63136,#63137,#63138,#63139,#63140,#63141,#63142,
#63143,#63144,#63145,#63146,#63147,#63148,#63149,#63150,#63151,#63152,#63153,
#63154,#63155,#63156,#63157,#63158,#63159,#63160,#63161,#63162,#63163,#63164,
#63165,#63166,#63167,#63168,#63169,#63170,#63171,#63172,#63173,#63174,#63175,
#63176,#63177,#63178,#63179,#63180,#63181,#63182,#63183,#63184,#63185,#63186,
#63187,#63188,#63189,#63190,#63191,#63192,#63193,#63194,#63195,#63196,#63197,
#63198,#63199,#63200),.UNSPECIFIED.,.F.,.F.,(4,3,3,3,3,3,3,3,3,3,3,3,3,
3,3,3,3,3,3,3,3,3,3,3,3,3,3,3,4),(-0.364629307890661,-0.350885759085945,
-0.329296488089375,-0.318978386270927,-0.313741431878983,-0.309365163672801,
-0.288042901568511,-0.272809238661881,-0.264006177467146,-0.26029818106468,
-0.239567096461013,-0.219346880276472,-0.206053559786221,-0.194876880502573,
-0.191399047668888,-0.171813366976952,-0.166173598315468,-0.145401898526034,
-0.126706873608775,-0.123379860192083,-0.103925496661725,-0.0845481894111439,
-0.065567586070534,-0.0621782887363481,-0.05894467115978,-0.0403543924373443,
-0.0220984153978596,-0.00442511140790438,0.),.UNSPECIFIED.);
#1552=B_SPLINE_CURVE_WITH_KNOTS('',3,(#63201,#63202,#63203,#63204,#63205,
#63206,#63207,#63208,#63209,#63210,#63211,#63212,#63213),.UNSPECIFIED.,
 .F.,.F.,(4,3,3,3,4),(-101.213804280572,-100.730920097777,-99.7335842552244,
-98.7362484126722,-98.3403213565322),.UNSPECIFIED.);
#1553=B_SPLINE_CURVE_WITH_KNOTS('',3,(#63216,#63217,#63218,#63219,#63220,
#63221,#63222,#63223,#63224),.UNSPECIFIED.,.F.,.F.,(4,1,1,1,1,1,4),(10.3757270560178,
11.30460783463,12.30261480526,13.3006217758901,14.2986287465202,15.2966357171503,
15.7079632679489),.UNSPECIFIED.);
#1554=B_SPLINE_CURVE_WITH_KNOTS('',3,(#63658,#63659,#63660,#63661,#63662,
#63663,#63664,#63665,#63666,#63667,#63668,#63669,#63670,#63671,#63672,#63673),
 .UNSPECIFIED.,.F.,.F.,(4,3,3,3,3,4),(95.3619706457233,95.8086691804886,
96.8066761511186,97.8046831217487,98.8026900923788,99.1486641472938),
 .UNSPECIFIED.);
#1555=B_SPLINE_CURVE_WITH_KNOTS('',3,(#63674,#63675,#63676,#63677,#63678,
#63679,#63680,#63681,#63682,#63683,#63684,#63685,#63686,#63687,#63688,#63689,
#63690,#63691,#63692,#63693,#63694,#63695,#63696,#63697,#63698,#63699,#63700,
#63701,#63702,#63703,#63704,#63705,#63706,#63707,#63708,#63709,#63710,#63711,
#63712,#63713,#63714,#63715,#63716,#63717,#63718,#63719,#63720,#63721,#63722,
#63723,#63724,#63725,#63726,#63727,#63728,#63729,#63730,#63731,#63732,#63733,
#63734,#63735,#63736,#63737,#63738,#63739,#63740,#63741,#63742,#63743,#63744,
#63745,#63746,#63747,#63748,#63749,#63750,#63751,#63752,#63753,#63754,#63755,
#63756,#63757,#63758),.UNSPECIFIED.,.F.,.F.,(4,3,3,3,3,3,3,3,3,3,3,3,3,
3,3,3,3,3,3,3,3,3,3,3,3,3,3,3,4),(-0.366397579005845,-0.355461226466819,
-0.337490969642209,-0.327214164040339,-0.321649482146298,-0.302840833811487,
-0.288386907394637,-0.281257238921911,-0.277593927902022,-0.258153123971634,
-0.238335729520815,-0.225554152759783,-0.218411056976172,-0.214856426708649,
-0.194426531587897,-0.187209422476688,-0.167504451243421,-0.156894426252658,
-0.149523127563347,-0.145921626399787,-0.125494957624892,-0.104619107174947,
-0.0835512936559854,-0.0752831225832569,-0.0721648689176682,-0.0505208253811386,
-0.028827309118007,-0.00759789023731293,0.),.UNSPECIFIED.);
#1573=SHAPE_REPRESENTATION_RELATIONSHIP('SRR','None',#64012,#1591);
#1591=ADVANCED_BREP_SHAPE_REPRESENTATION('',(#1627),#63897);
#1609=STYLED_ITEM('',(#64099),#1627);
#1627=MANIFOLD_SOLID_BREP('Body1',#15495);
#1713=FACE_BOUND('',#4418,.T.);
#1714=FACE_BOUND('',#4421,.T.);
#2345=CYLINDRICAL_SURFACE('',#16753,1.954);
#2346=CYLINDRICAL_SURFACE('',#16755,1.954);
#2347=CYLINDRICAL_SURFACE('',#16756,1.954);
#2348=CYLINDRICAL_SURFACE('',#16757,1.954);
#2349=CYLINDRICAL_SURFACE('',#16758,1.954);
#2350=CYLINDRICAL_SURFACE('',#16759,1.954);
#2351=CYLINDRICAL_SURFACE('',#16760,1.954);
#2352=CYLINDRICAL_SURFACE('',#16761,1.954);
#2353=CYLINDRICAL_SURFACE('',#16762,1.954);
#2354=CYLINDRICAL_SURFACE('',#16763,1.954);
#2355=CYLINDRICAL_SURFACE('',#16764,1.954);
#2356=CYLINDRICAL_SURFACE('',#16765,1.954);
#2357=CYLINDRICAL_SURFACE('',#16766,1.954);
#2358=CYLINDRICAL_SURFACE('',#16767,1.954);
#2359=CYLINDRICAL_SURFACE('',#16768,1.954);
#2360=CYLINDRICAL_SURFACE('',#16769,1.954);
#2361=CYLINDRICAL_SURFACE('',#16770,1.5555);
#2362=CYLINDRICAL_SURFACE('',#16772,1.5555);
#2363=CYLINDRICAL_SURFACE('',#16773,1.5555);
#2364=CYLINDRICAL_SURFACE('',#16774,1.5555);
#2365=CYLINDRICAL_SURFACE('',#16775,1.5555);
#2366=CYLINDRICAL_SURFACE('',#16776,1.5555);
#2367=CYLINDRICAL_SURFACE('',#16777,1.5555);
#2368=CYLINDRICAL_SURFACE('',#16778,1.5555);
#2369=CYLINDRICAL_SURFACE('',#16779,1.5555);
#2370=CYLINDRICAL_SURFACE('',#16780,1.5555);
#2371=CYLINDRICAL_SURFACE('',#16781,1.5555);
#2372=CYLINDRICAL_SURFACE('',#16782,1.5555);
#2373=CYLINDRICAL_SURFACE('',#16783,1.5555);
#2374=CYLINDRICAL_SURFACE('',#16784,1.5555);
#2375=CYLINDRICAL_SURFACE('',#16785,1.5555);
#2376=CYLINDRICAL_SURFACE('',#16786,1.5555);
#2377=CYLINDRICAL_SURFACE('',#16790,1.5555);
#2378=CYLINDRICAL_SURFACE('',#16792,1.954);
#2379=CYLINDRICAL_SURFACE('',#16802,3.5);
#2653=CIRCLE('',#16754,1.954);
#2654=CIRCLE('',#16771,1.5555);
#2655=CIRCLE('',#16788,1.954);
#2656=CIRCLE('',#16789,1.);
#2657=CIRCLE('',#16791,1.5555);
#2658=CIRCLE('',#16801,3.5);
#2659=CIRCLE('',#16803,3.5);
#3450=FACE_OUTER_BOUND('',#4373,.T.);
#3451=FACE_OUTER_BOUND('',#4374,.T.);
#3452=FACE_OUTER_BOUND('',#4375,.T.);
#3453=FACE_OUTER_BOUND('',#4376,.T.);
#3454=FACE_OUTER_BOUND('',#4377,.T.);
#3455=FACE_OUTER_BOUND('',#4378,.T.);
#3456=FACE_OUTER_BOUND('',#4379,.T.);
#3457=FACE_OUTER_BOUND('',#4380,.T.);
#3458=FACE_OUTER_BOUND('',#4381,.T.);
#3459=FACE_OUTER_BOUND('',#4382,.T.);
#3460=FACE_OUTER_BOUND('',#4383,.T.);
#3461=FACE_OUTER_BOUND('',#4384,.T.);
#3462=FACE_OUTER_BOUND('',#4385,.T.);
#3463=FACE_OUTER_BOUND('',#4386,.T.);
#3464=FACE_OUTER_BOUND('',#4387,.T.);
#3465=FACE_OUTER_BOUND('',#4388,.T.);
#3466=FACE_OUTER_BOUND('',#4389,.T.);
#3467=FACE_OUTER_BOUND('',#4390,.T.);
#3468=FACE_OUTER_BOUND('',#4391,.T.);
#3469=FACE_OUTER_BOUND('',#4392,.T.);
#3470=FACE_OUTER_BOUND('',#4393,.T.);
#3471=FACE_OUTER_BOUND('',#4394,.T.);
#3472=FACE_OUTER_BOUND('',#4395,.T.);
#3473=FACE_OUTER_BOUND('',#4396,.T.);
#3474=FACE_OUTER_BOUND('',#4397,.T.);
#3475=FACE_OUTER_BOUND('',#4398,.T.);
#3476=FACE_OUTER_BOUND('',#4399,.T.);
#3477=FACE_OUTER_BOUND('',#4400,.T.);
#3478=FACE_OUTER_BOUND('',#4401,.T.);
#3479=FACE_OUTER_BOUND('',#4402,.T.);
#3480=FACE_OUTER_BOUND('',#4403,.T.);
#3481=FACE_OUTER_BOUND('',#4404,.T.);
#3482=FACE_OUTER_BOUND('',#4405,.T.);
#3483=FACE_OUTER_BOUND('',#4406,.T.);
#3484=FACE_OUTER_BOUND('',#4407,.T.);
#3485=FACE_OUTER_BOUND('',#4408,.T.);
#3486=FACE_OUTER_BOUND('',#4409,.T.);
#3487=FACE_OUTER_BOUND('',#4410,.T.);
#3488=FACE_OUTER_BOUND('',#4411,.T.);
#3489=FACE_OUTER_BOUND('',#4412,.T.);
#3490=FACE_OUTER_BOUND('',#4413,.T.);
#3491=FACE_OUTER_BOUND('',#4414,.T.);
#3492=FACE_OUTER_BOUND('',#4415,.T.);
#3493=FACE_OUTER_BOUND('',#4416,.T.);
#3494=FACE_OUTER_BOUND('',#4417,.T.);
#3495=FACE_OUTER_BOUND('',#4419,.T.);
#3496=FACE_OUTER_BOUND('',#4420,.T.);
#3497=FACE_OUTER_BOUND('',#4422,.T.);
#4373=EDGE_LOOP('',(#14246,#14247,#14248,#14249));
#4374=EDGE_LOOP('',(#14250,#14251,#14252,#14253));
#4375=EDGE_LOOP('',(#14254,#14255,#14256,#14257));
#4376=EDGE_LOOP('',(#14258,#14259,#14260,#14261));
#4377=EDGE_LOOP('',(#14262,#14263,#14264,#14265));
#4378=EDGE_LOOP('',(#14266,#14267,#14268,#14269));
#4379=EDGE_LOOP('',(#14270,#14271,#14272,#14273));
#4380=EDGE_LOOP('',(#14274,#14275,#14276,#14277));
#4381=EDGE_LOOP('',(#14278,#14279,#14280,#14281));
#4382=EDGE_LOOP('',(#14282,#14283,#14284,#14285));
#4383=EDGE_LOOP('',(#14286,#14287,#14288,#14289));
#4384=EDGE_LOOP('',(#14290,#14291,#14292,#14293));
#4385=EDGE_LOOP('',(#14294,#14295,#14296,#14297));
#4386=EDGE_LOOP('',(#14298,#14299,#14300,#14301));
#4387=EDGE_LOOP('',(#14302,#14303,#14304,#14305));
#4388=EDGE_LOOP('',(#14306,#14307,#14308,#14309));
#4389=EDGE_LOOP('',(#14310,#14311,#14312,#14313));
#4390=EDGE_LOOP('',(#14314,#14315,#14316,#14317));
#4391=EDGE_LOOP('',(#14318,#14319,#14320,#14321));
#4392=EDGE_LOOP('',(#14322,#14323,#14324,#14325));
#4393=EDGE_LOOP('',(#14326,#14327,#14328,#14329));
#4394=EDGE_LOOP('',(#14330,#14331,#14332,#14333));
#4395=EDGE_LOOP('',(#14334,#14335,#14336,#14337));
#4396=EDGE_LOOP('',(#14338,#14339,#14340,#14341));
#4397=EDGE_LOOP('',(#14342,#14343,#14344,#14345));
#4398=EDGE_LOOP('',(#14346,#14347,#14348,#14349));
#4399=EDGE_LOOP('',(#14350,#14351,#14352,#14353));
#4400=EDGE_LOOP('',(#14354,#14355,#14356,#14357));
#4401=EDGE_LOOP('',(#14358,#14359,#14360,#14361));
#4402=EDGE_LOOP('',(#14362,#14363,#14364,#14365));
#4403=EDGE_LOOP('',(#14366,#14367,#14368,#14369));
#4404=EDGE_LOOP('',(#14370,#14371,#14372,#14373));
#4405=EDGE_LOOP('',(#14374,#14375,#14376,#14377,#14378,#14379,#14380,#14381));
#4406=EDGE_LOOP('',(#14382,#14383,#14384,#14385,#14386,#14387,#14388,#14389,
#14390,#14391,#14392,#14393,#14394,#14395,#14396,#14397,#14398,#14399,#14400,
#14401,#14402,#14403,#14404,#14405,#14406,#14407,#14408,#14409,#14410,#14411,
#14412,#14413,#14414,#14415,#14416,#14417));
#4407=EDGE_LOOP('',(#14418,#14419,#14420,#14421));
#4408=EDGE_LOOP('',(#14422,#14423,#14424,#14425,#14426,#14427,#14428,#14429,
#14430,#14431,#14432,#14433,#14434,#14435,#14436,#14437,#14438,#14439,#14440,
#14441,#14442,#14443,#14444,#14445,#14446,#14447,#14448,#14449,#14450,#14451,
#14452,#14453,#14454,#14455,#14456,#14457,#14458));
#4409=EDGE_LOOP('',(#14459,#14460,#14461,#14462));
#4410=EDGE_LOOP('',(#14463,#14464,#14465,#14466));
#4411=EDGE_LOOP('',(#14467,#14468,#14469,#14470));
#4412=EDGE_LOOP('',(#14471,#14472,#14473,#14474));
#4413=EDGE_LOOP('',(#14475,#14476,#14477,#14478));
#4414=EDGE_LOOP('',(#14479,#14480,#14481,#14482));
#4415=EDGE_LOOP('',(#14483,#14484,#14485,#14486));
#4416=EDGE_LOOP('',(#14487,#14488,#14489,#14490,#14491,#14492));
#4417=EDGE_LOOP('',(#14493));
#4418=EDGE_LOOP('',(#14494,#14495,#14496,#14497));
#4419=EDGE_LOOP('',(#14498,#14499,#14500,#14501));
#4420=EDGE_LOOP('',(#14502));
#4421=EDGE_LOOP('',(#14503,#14504,#14505,#14506,#14507,#14508));
#4422=EDGE_LOOP('',(#14509));
#5134=LINE('',#61232,#5897);
#5135=LINE('',#61256,#5898);
#5136=LINE('',#61304,#5899);
#5137=LINE('',#61352,#5900);
#5138=LINE('',#61406,#5901);
#5139=LINE('',#61454,#5902);
#5140=LINE('',#61502,#5903);
#5141=LINE('',#61550,#5904);
#5142=LINE('',#61604,#5905);
#5143=LINE('',#61652,#5906);
#5144=LINE('',#61700,#5907);
#5145=LINE('',#61754,#5908);
#5146=LINE('',#61802,#5909);
#5147=LINE('',#61850,#5910);
#5148=LINE('',#61901,#5911);
#5149=LINE('',#61952,#5912);
#5150=LINE('',#62000,#5913);
#5151=LINE('',#62022,#5914);
#5152=LINE('',#62046,#5915);
#5153=LINE('',#62070,#5916);
#5154=LINE('',#62096,#5917);
#5155=LINE('',#62120,#5918);
#5156=LINE('',#62144,#5919);
#5157=LINE('',#62169,#5920);
#5158=LINE('',#62194,#5921);
#5159=LINE('',#62218,#5922);
#5160=LINE('',#62243,#5923);
#5161=LINE('',#62268,#5924);
#5162=LINE('',#62292,#5925);
#5163=LINE('',#62316,#5926);
#5164=LINE('',#62341,#5927);
#5165=LINE('',#62366,#5928);
#5166=LINE('',#62681,#5929);
#5167=LINE('',#63763,#5930);
#5168=LINE('',#63765,#5931);
#5169=LINE('',#63767,#5932);
#5170=LINE('',#63768,#5933);
#5171=LINE('',#63771,#5934);
#5172=LINE('',#63773,#5935);
#5173=LINE('',#63774,#5936);
#5174=LINE('',#63777,#5937);
#5175=LINE('',#63779,#5938);
#5176=LINE('',#63780,#5939);
#5177=LINE('',#63783,#5940);
#5178=LINE('',#63785,#5941);
#5179=LINE('',#63786,#5942);
#5180=LINE('',#63789,#5943);
#5181=LINE('',#63791,#5944);
#5182=LINE('',#63792,#5945);
#5183=LINE('',#63794,#5946);
#5184=LINE('',#63795,#5947);
#5185=LINE('',#63802,#5948);
#5897=VECTOR('',#19688,2.);
#5898=VECTOR('',#19693,2.);
#5899=VECTOR('',#19696,2.);
#5900=VECTOR('',#19699,2.);
#5901=VECTOR('',#19702,2.);
#5902=VECTOR('',#19705,2.);
#5903=VECTOR('',#19708,2.);
#5904=VECTOR('',#19711,2.);
#5905=VECTOR('',#19714,2.);
#5906=VECTOR('',#19717,2.);
#5907=VECTOR('',#19720,2.);
#5908=VECTOR('',#19723,2.);
#5909=VECTOR('',#19726,2.);
#5910=VECTOR('',#19729,2.);
#5911=VECTOR('',#19732,2.);
#5912=VECTOR('',#19735,2.);
#5913=VECTOR('',#19738,1.5555);
#5914=VECTOR('',#19743,1.5555);
#5915=VECTOR('',#19746,1.5555);
#5916=VECTOR('',#19749,1.5555);
#5917=VECTOR('',#19752,1.5555);
#5918=VECTOR('',#19755,1.5555);
#5919=VECTOR('',#19758,1.5555);
#5920=VECTOR('',#19761,1.5555);
#5921=VECTOR('',#19764,1.5555);
#5922=VECTOR('',#19767,1.5555);
#5923=VECTOR('',#19770,1.5555);
#5924=VECTOR('',#19773,1.5555);
#5925=VECTOR('',#19776,1.5555);
#5926=VECTOR('',#19779,1.5555);
#5927=VECTOR('',#19782,1.5555);
#5928=VECTOR('',#19785,1.5555);
#5929=VECTOR('',#19790,1.5);
#5930=VECTOR('',#19801,10.);
#5931=VECTOR('',#19802,10.);
#5932=VECTOR('',#19803,10.);
#5933=VECTOR('',#19804,10.);
#5934=VECTOR('',#19807,10.);
#5935=VECTOR('',#19808,10.);
#5936=VECTOR('',#19809,10.);
#5937=VECTOR('',#19812,10.);
#5938=VECTOR('',#19813,10.);
#5939=VECTOR('',#19814,10.);
#5940=VECTOR('',#19817,10.);
#5941=VECTOR('',#19818,10.);
#5942=VECTOR('',#19819,10.);
#5943=VECTOR('',#19822,10.);
#5944=VECTOR('',#19823,10.);
#5945=VECTOR('',#19824,10.);
#5946=VECTOR('',#19827,10.);
#5947=VECTOR('',#19828,10.);
#5948=VECTOR('',#19837,3.5);
#7423=VERTEX_POINT('',#61230);
#7424=VERTEX_POINT('',#61231);
#7425=VERTEX_POINT('',#61233);
#7426=VERTEX_POINT('',#61244);
#7427=VERTEX_POINT('',#61254);
#7428=VERTEX_POINT('',#61255);
#7429=VERTEX_POINT('',#61302);
#7430=VERTEX_POINT('',#61303);
#7431=VERTEX_POINT('',#61350);
#7432=VERTEX_POINT('',#61351);
#7433=VERTEX_POINT('',#61404);
#7434=VERTEX_POINT('',#61405);
#7435=VERTEX_POINT('',#61452);
#7436=VERTEX_POINT('',#61453);
#7437=VERTEX_POINT('',#61500);
#7438=VERTEX_POINT('',#61501);
#7439=VERTEX_POINT('',#61548);
#7440=VERTEX_POINT('',#61549);
#7441=VERTEX_POINT('',#61602);
#7442=VERTEX_POINT('',#61603);
#7443=VERTEX_POINT('',#61650);
#7444=VERTEX_POINT('',#61651);
#7445=VERTEX_POINT('',#61698);
#7446=VERTEX_POINT('',#61699);
#7447=VERTEX_POINT('',#61752);
#7448=VERTEX_POINT('',#61753);
#7449=VERTEX_POINT('',#61800);
#7450=VERTEX_POINT('',#61801);
#7451=VERTEX_POINT('',#61848);
#7452=VERTEX_POINT('',#61849);
#7453=VERTEX_POINT('',#61899);
#7454=VERTEX_POINT('',#61900);
#7455=VERTEX_POINT('',#61950);
#7456=VERTEX_POINT('',#61951);
#7457=VERTEX_POINT('',#61998);
#7458=VERTEX_POINT('',#61999);
#7459=VERTEX_POINT('',#62001);
#7460=VERTEX_POINT('',#62010);
#7461=VERTEX_POINT('',#62020);
#7462=VERTEX_POINT('',#62021);
#7463=VERTEX_POINT('',#62044);
#7464=VERTEX_POINT('',#62045);
#7465=VERTEX_POINT('',#62068);
#7466=VERTEX_POINT('',#62069);
#7467=VERTEX_POINT('',#62094);
#7468=VERTEX_POINT('',#62095);
#7469=VERTEX_POINT('',#62118);
#7470=VERTEX_POINT('',#62119);
#7471=VERTEX_POINT('',#62142);
#7472=VERTEX_POINT('',#62143);
#7473=VERTEX_POINT('',#62167);
#7474=VERTEX_POINT('',#62168);
#7475=VERTEX_POINT('',#62192);
#7476=VERTEX_POINT('',#62193);
#7477=VERTEX_POINT('',#62216);
#7478=VERTEX_POINT('',#62217);
#7479=VERTEX_POINT('',#62241);
#7480=VERTEX_POINT('',#62242);
#7481=VERTEX_POINT('',#62266);
#7482=VERTEX_POINT('',#62267);
#7483=VERTEX_POINT('',#62290);
#7484=VERTEX_POINT('',#62291);
#7485=VERTEX_POINT('',#62314);
#7486=VERTEX_POINT('',#62315);
#7487=VERTEX_POINT('',#62339);
#7488=VERTEX_POINT('',#62340);
#7489=VERTEX_POINT('',#62364);
#7490=VERTEX_POINT('',#62365);
#7491=VERTEX_POINT('',#62388);
#7492=VERTEX_POINT('',#62516);
#7493=VERTEX_POINT('',#62575);
#7494=VERTEX_POINT('',#62680);
#7495=VERTEX_POINT('',#63107);
#7496=VERTEX_POINT('',#63215);
#7497=VERTEX_POINT('',#63761);
#7498=VERTEX_POINT('',#63762);
#7499=VERTEX_POINT('',#63764);
#7500=VERTEX_POINT('',#63766);
#7501=VERTEX_POINT('',#63770);
#7502=VERTEX_POINT('',#63772);
#7503=VERTEX_POINT('',#63776);
#7504=VERTEX_POINT('',#63778);
#7505=VERTEX_POINT('',#63782);
#7506=VERTEX_POINT('',#63784);
#7507=VERTEX_POINT('',#63788);
#7508=VERTEX_POINT('',#63790);
#7509=VERTEX_POINT('',#63798);
#7510=VERTEX_POINT('',#63801);
#9712=EDGE_CURVE('',#7423,#7424,#5134,.T.);
#9713=EDGE_CURVE('',#7423,#7425,#1483,.T.);
#9714=EDGE_CURVE('',#7425,#7426,#2653,.F.);
#9715=EDGE_CURVE('',#7426,#7424,#1484,.T.);
#9716=EDGE_CURVE('',#7427,#7428,#5135,.T.);
#9717=EDGE_CURVE('',#7427,#7423,#1485,.T.);
#9718=EDGE_CURVE('',#7424,#7428,#1486,.T.);
#9719=EDGE_CURVE('',#7429,#7430,#5136,.T.);
#9720=EDGE_CURVE('',#7429,#7427,#1487,.T.);
#9721=EDGE_CURVE('',#7428,#7430,#1488,.T.);
#9722=EDGE_CURVE('',#7431,#7432,#5137,.T.);
#9723=EDGE_CURVE('',#7431,#7429,#1489,.T.);
#9724=EDGE_CURVE('',#7430,#7432,#1490,.T.);
#9725=EDGE_CURVE('',#7433,#7434,#5138,.T.);
#9726=EDGE_CURVE('',#7433,#7431,#1491,.T.);
#9727=EDGE_CURVE('',#7432,#7434,#1492,.T.);
#9728=EDGE_CURVE('',#7435,#7436,#5139,.T.);
#9729=EDGE_CURVE('',#7435,#7433,#1493,.T.);
#9730=EDGE_CURVE('',#7434,#7436,#1494,.T.);
#9731=EDGE_CURVE('',#7437,#7438,#5140,.T.);
#9732=EDGE_CURVE('',#7437,#7435,#1495,.T.);
#9733=EDGE_CURVE('',#7436,#7438,#1496,.T.);
#9734=EDGE_CURVE('',#7439,#7440,#5141,.T.);
#9735=EDGE_CURVE('',#7439,#7437,#1497,.T.);
#9736=EDGE_CURVE('',#7438,#7440,#1498,.T.);
#9737=EDGE_CURVE('',#7441,#7442,#5142,.T.);
#9738=EDGE_CURVE('',#7441,#7439,#1499,.T.);
#9739=EDGE_CURVE('',#7440,#7442,#1500,.T.);
#9740=EDGE_CURVE('',#7443,#7444,#5143,.T.);
#9741=EDGE_CURVE('',#7443,#7441,#1501,.T.);
#9742=EDGE_CURVE('',#7442,#7444,#1502,.T.);
#9743=EDGE_CURVE('',#7445,#7446,#5144,.T.);
#9744=EDGE_CURVE('',#7445,#7443,#1503,.T.);
#9745=EDGE_CURVE('',#7444,#7446,#1504,.T.);
#9746=EDGE_CURVE('',#7447,#7448,#5145,.T.);
#9747=EDGE_CURVE('',#7447,#7445,#1505,.T.);
#9748=EDGE_CURVE('',#7446,#7448,#1506,.T.);
#9749=EDGE_CURVE('',#7449,#7450,#5146,.T.);
#9750=EDGE_CURVE('',#7449,#7447,#1507,.T.);
#9751=EDGE_CURVE('',#7448,#7450,#1508,.T.);
#9752=EDGE_CURVE('',#7451,#7452,#5147,.T.);
#9753=EDGE_CURVE('',#7451,#7449,#1509,.T.);
#9754=EDGE_CURVE('',#7450,#7452,#1510,.T.);
#9755=EDGE_CURVE('',#7453,#7454,#5148,.T.);
#9756=EDGE_CURVE('',#7453,#7451,#1511,.T.);
#9757=EDGE_CURVE('',#7452,#7454,#1512,.T.);
#9758=EDGE_CURVE('',#7455,#7456,#5149,.T.);
#9759=EDGE_CURVE('',#7455,#7453,#1513,.T.);
#9760=EDGE_CURVE('',#7454,#7456,#1514,.T.);
#9761=EDGE_CURVE('',#7457,#7458,#5150,.T.);
#9762=EDGE_CURVE('',#7457,#7459,#1515,.T.);
#9763=EDGE_CURVE('',#7459,#7460,#2654,.T.);
#9764=EDGE_CURVE('',#7458,#7460,#1516,.T.);
#9765=EDGE_CURVE('',#7461,#7462,#5151,.T.);
#9766=EDGE_CURVE('',#7461,#7457,#1517,.T.);
#9767=EDGE_CURVE('',#7462,#7458,#1518,.T.);
#9768=EDGE_CURVE('',#7463,#7464,#5152,.T.);
#9769=EDGE_CURVE('',#7463,#7461,#1519,.T.);
#9770=EDGE_CURVE('',#7464,#7462,#1520,.T.);
#9771=EDGE_CURVE('',#7465,#7466,#5153,.T.);
#9772=EDGE_CURVE('',#7465,#7463,#1521,.T.);
#9773=EDGE_CURVE('',#7466,#7464,#1522,.T.);
#9774=EDGE_CURVE('',#7467,#7468,#5154,.T.);
#9775=EDGE_CURVE('',#7467,#7465,#1523,.T.);
#9776=EDGE_CURVE('',#7468,#7466,#1524,.T.);
#9777=EDGE_CURVE('',#7469,#7470,#5155,.T.);
#9778=EDGE_CURVE('',#7469,#7467,#1525,.T.);
#9779=EDGE_CURVE('',#7470,#7468,#1526,.T.);
#9780=EDGE_CURVE('',#7471,#7472,#5156,.T.);
#9781=EDGE_CURVE('',#7471,#7469,#1527,.T.);
#9782=EDGE_CURVE('',#7472,#7470,#1528,.T.);
#9783=EDGE_CURVE('',#7473,#7474,#5157,.T.);
#9784=EDGE_CURVE('',#7473,#7471,#1529,.T.);
#9785=EDGE_CURVE('',#7474,#7472,#1530,.T.);
#9786=EDGE_CURVE('',#7475,#7476,#5158,.T.);
#9787=EDGE_CURVE('',#7475,#7473,#1531,.T.);
#9788=EDGE_CURVE('',#7476,#7474,#1532,.T.);
#9789=EDGE_CURVE('',#7477,#7478,#5159,.T.);
#9790=EDGE_CURVE('',#7477,#7475,#1533,.T.);
#9791=EDGE_CURVE('',#7478,#7476,#1534,.T.);
#9792=EDGE_CURVE('',#7479,#7480,#5160,.T.);
#9793=EDGE_CURVE('',#7479,#7477,#1535,.T.);
#9794=EDGE_CURVE('',#7480,#7478,#1536,.T.);
#9795=EDGE_CURVE('',#7481,#7482,#5161,.T.);
#9796=EDGE_CURVE('',#7481,#7479,#1537,.T.);
#9797=EDGE_CURVE('',#7482,#7480,#1538,.T.);
#9798=EDGE_CURVE('',#7483,#7484,#5162,.T.);
#9799=EDGE_CURVE('',#7483,#7481,#1539,.T.);
#9800=EDGE_CURVE('',#7484,#7482,#1540,.T.);
#9801=EDGE_CURVE('',#7485,#7486,#5163,.T.);
#9802=EDGE_CURVE('',#7485,#7483,#1541,.T.);
#9803=EDGE_CURVE('',#7486,#7484,#1542,.T.);
#9804=EDGE_CURVE('',#7487,#7488,#5164,.T.);
#9805=EDGE_CURVE('',#7487,#7485,#1543,.T.);
#9806=EDGE_CURVE('',#7488,#7486,#1544,.T.);
#9807=EDGE_CURVE('',#7489,#7490,#5165,.T.);
#9808=EDGE_CURVE('',#7489,#7487,#1545,.T.);
#9809=EDGE_CURVE('',#7490,#7488,#1546,.T.);
#9810=EDGE_CURVE('',#7460,#7491,#1547,.T.);
#9811=EDGE_CURVE('',#7492,#7459,#1548,.T.);
#9812=EDGE_CURVE('',#7493,#7492,#2655,.T.);
#9813=EDGE_CURVE('',#7491,#7493,#1549,.T.);
#9814=EDGE_CURVE('',#7491,#7494,#5166,.T.);
#9815=EDGE_CURVE('',#7494,#7494,#2656,.T.);
#9816=EDGE_CURVE('',#7495,#7489,#1550,.T.);
#9817=EDGE_CURVE('',#7425,#7495,#1551,.T.);
#9818=EDGE_CURVE('',#7492,#7455,#1552,.T.);
#9819=EDGE_CURVE('',#7496,#7490,#1553,.T.);
#9820=EDGE_CURVE('',#7495,#7496,#2657,.T.);
#9821=EDGE_CURVE('',#7456,#7493,#1554,.T.);
#9822=EDGE_CURVE('',#7496,#7426,#1555,.T.);
#9823=EDGE_CURVE('',#7497,#7498,#5167,.T.);
#9824=EDGE_CURVE('',#7497,#7499,#5168,.T.);
#9825=EDGE_CURVE('',#7499,#7500,#5169,.T.);
#9826=EDGE_CURVE('',#7498,#7500,#5170,.T.);
#9827=EDGE_CURVE('',#7501,#7497,#5171,.T.);
#9828=EDGE_CURVE('',#7501,#7502,#5172,.T.);
#9829=EDGE_CURVE('',#7502,#7499,#5173,.T.);
#9830=EDGE_CURVE('',#7503,#7501,#5174,.T.);
#9831=EDGE_CURVE('',#7503,#7504,#5175,.T.);
#9832=EDGE_CURVE('',#7504,#7502,#5176,.T.);
#9833=EDGE_CURVE('',#7505,#7503,#5177,.T.);
#9834=EDGE_CURVE('',#7505,#7506,#5178,.T.);
#9835=EDGE_CURVE('',#7506,#7504,#5179,.T.);
#9836=EDGE_CURVE('',#7507,#7505,#5180,.T.);
#9837=EDGE_CURVE('',#7507,#7508,#5181,.T.);
#9838=EDGE_CURVE('',#7508,#7506,#5182,.T.);
#9839=EDGE_CURVE('',#7498,#7507,#5183,.T.);
#9840=EDGE_CURVE('',#7500,#7508,#5184,.T.);
#9841=EDGE_CURVE('',#7509,#7509,#2658,.T.);
#9842=EDGE_CURVE('',#7509,#7510,#5185,.T.);
#9843=EDGE_CURVE('',#7510,#7510,#2659,.T.);
#14246=ORIENTED_EDGE('',*,*,#9712,.F.);
#14247=ORIENTED_EDGE('',*,*,#9713,.T.);
#14248=ORIENTED_EDGE('',*,*,#9714,.T.);
#14249=ORIENTED_EDGE('',*,*,#9715,.T.);
#14250=ORIENTED_EDGE('',*,*,#9716,.F.);
#14251=ORIENTED_EDGE('',*,*,#9717,.T.);
#14252=ORIENTED_EDGE('',*,*,#9712,.T.);
#14253=ORIENTED_EDGE('',*,*,#9718,.T.);
#14254=ORIENTED_EDGE('',*,*,#9719,.F.);
#14255=ORIENTED_EDGE('',*,*,#9720,.T.);
#14256=ORIENTED_EDGE('',*,*,#9716,.T.);
#14257=ORIENTED_EDGE('',*,*,#9721,.T.);
#14258=ORIENTED_EDGE('',*,*,#9722,.F.);
#14259=ORIENTED_EDGE('',*,*,#9723,.T.);
#14260=ORIENTED_EDGE('',*,*,#9719,.T.);
#14261=ORIENTED_EDGE('',*,*,#9724,.T.);
#14262=ORIENTED_EDGE('',*,*,#9725,.F.);
#14263=ORIENTED_EDGE('',*,*,#9726,.T.);
#14264=ORIENTED_EDGE('',*,*,#9722,.T.);
#14265=ORIENTED_EDGE('',*,*,#9727,.T.);
#14266=ORIENTED_EDGE('',*,*,#9728,.F.);
#14267=ORIENTED_EDGE('',*,*,#9729,.T.);
#14268=ORIENTED_EDGE('',*,*,#9725,.T.);
#14269=ORIENTED_EDGE('',*,*,#9730,.T.);
#14270=ORIENTED_EDGE('',*,*,#9731,.F.);
#14271=ORIENTED_EDGE('',*,*,#9732,.T.);
#14272=ORIENTED_EDGE('',*,*,#9728,.T.);
#14273=ORIENTED_EDGE('',*,*,#9733,.T.);
#14274=ORIENTED_EDGE('',*,*,#9734,.F.);
#14275=ORIENTED_EDGE('',*,*,#9735,.T.);
#14276=ORIENTED_EDGE('',*,*,#9731,.T.);
#14277=ORIENTED_EDGE('',*,*,#9736,.T.);
#14278=ORIENTED_EDGE('',*,*,#9737,.F.);
#14279=ORIENTED_EDGE('',*,*,#9738,.T.);
#14280=ORIENTED_EDGE('',*,*,#9734,.T.);
#14281=ORIENTED_EDGE('',*,*,#9739,.T.);
#14282=ORIENTED_EDGE('',*,*,#9740,.F.);
#14283=ORIENTED_EDGE('',*,*,#9741,.T.);
#14284=ORIENTED_EDGE('',*,*,#9737,.T.);
#14285=ORIENTED_EDGE('',*,*,#9742,.T.);
#14286=ORIENTED_EDGE('',*,*,#9743,.F.);
#14287=ORIENTED_EDGE('',*,*,#9744,.T.);
#14288=ORIENTED_EDGE('',*,*,#9740,.T.);
#14289=ORIENTED_EDGE('',*,*,#9745,.T.);
#14290=ORIENTED_EDGE('',*,*,#9746,.F.);
#14291=ORIENTED_EDGE('',*,*,#9747,.T.);
#14292=ORIENTED_EDGE('',*,*,#9743,.T.);
#14293=ORIENTED_EDGE('',*,*,#9748,.T.);
#14294=ORIENTED_EDGE('',*,*,#9749,.F.);
#14295=ORIENTED_EDGE('',*,*,#9750,.T.);
#14296=ORIENTED_EDGE('',*,*,#9746,.T.);
#14297=ORIENTED_EDGE('',*,*,#9751,.T.);
#14298=ORIENTED_EDGE('',*,*,#9752,.F.);
#14299=ORIENTED_EDGE('',*,*,#9753,.T.);
#14300=ORIENTED_EDGE('',*,*,#9749,.T.);
#14301=ORIENTED_EDGE('',*,*,#9754,.T.);
#14302=ORIENTED_EDGE('',*,*,#9755,.F.);
#14303=ORIENTED_EDGE('',*,*,#9756,.T.);
#14304=ORIENTED_EDGE('',*,*,#9752,.T.);
#14305=ORIENTED_EDGE('',*,*,#9757,.T.);
#14306=ORIENTED_EDGE('',*,*,#9758,.F.);
#14307=ORIENTED_EDGE('',*,*,#9759,.T.);
#14308=ORIENTED_EDGE('',*,*,#9755,.T.);
#14309=ORIENTED_EDGE('',*,*,#9760,.T.);
#14310=ORIENTED_EDGE('',*,*,#9761,.F.);
#14311=ORIENTED_EDGE('',*,*,#9762,.T.);
#14312=ORIENTED_EDGE('',*,*,#9763,.T.);
#14313=ORIENTED_EDGE('',*,*,#9764,.F.);
#14314=ORIENTED_EDGE('',*,*,#9765,.F.);
#14315=ORIENTED_EDGE('',*,*,#9766,.T.);
#14316=ORIENTED_EDGE('',*,*,#9761,.T.);
#14317=ORIENTED_EDGE('',*,*,#9767,.F.);
#14318=ORIENTED_EDGE('',*,*,#9768,.F.);
#14319=ORIENTED_EDGE('',*,*,#9769,.T.);
#14320=ORIENTED_EDGE('',*,*,#9765,.T.);
#14321=ORIENTED_EDGE('',*,*,#9770,.F.);
#14322=ORIENTED_EDGE('',*,*,#9771,.F.);
#14323=ORIENTED_EDGE('',*,*,#9772,.T.);
#14324=ORIENTED_EDGE('',*,*,#9768,.T.);
#14325=ORIENTED_EDGE('',*,*,#9773,.F.);
#14326=ORIENTED_EDGE('',*,*,#9774,.F.);
#14327=ORIENTED_EDGE('',*,*,#9775,.T.);
#14328=ORIENTED_EDGE('',*,*,#9771,.T.);
#14329=ORIENTED_EDGE('',*,*,#9776,.F.);
#14330=ORIENTED_EDGE('',*,*,#9777,.F.);
#14331=ORIENTED_EDGE('',*,*,#9778,.T.);
#14332=ORIENTED_EDGE('',*,*,#9774,.T.);
#14333=ORIENTED_EDGE('',*,*,#9779,.F.);
#14334=ORIENTED_EDGE('',*,*,#9780,.F.);
#14335=ORIENTED_EDGE('',*,*,#9781,.T.);
#14336=ORIENTED_EDGE('',*,*,#9777,.T.);
#14337=ORIENTED_EDGE('',*,*,#9782,.F.);
#14338=ORIENTED_EDGE('',*,*,#9783,.F.);
#14339=ORIENTED_EDGE('',*,*,#9784,.T.);
#14340=ORIENTED_EDGE('',*,*,#9780,.T.);
#14341=ORIENTED_EDGE('',*,*,#9785,.F.);
#14342=ORIENTED_EDGE('',*,*,#9786,.F.);
#14343=ORIENTED_EDGE('',*,*,#9787,.T.);
#14344=ORIENTED_EDGE('',*,*,#9783,.T.);
#14345=ORIENTED_EDGE('',*,*,#9788,.F.);
#14346=ORIENTED_EDGE('',*,*,#9789,.F.);
#14347=ORIENTED_EDGE('',*,*,#9790,.T.);
#14348=ORIENTED_EDGE('',*,*,#9786,.T.);
#14349=ORIENTED_EDGE('',*,*,#9791,.F.);
#14350=ORIENTED_EDGE('',*,*,#9792,.F.);
#14351=ORIENTED_EDGE('',*,*,#9793,.T.);
#14352=ORIENTED_EDGE('',*,*,#9789,.T.);
#14353=ORIENTED_EDGE('',*,*,#9794,.F.);
#14354=ORIENTED_EDGE('',*,*,#9795,.F.);
#14355=ORIENTED_EDGE('',*,*,#9796,.T.);
#14356=ORIENTED_EDGE('',*,*,#9792,.T.);
#14357=ORIENTED_EDGE('',*,*,#9797,.F.);
#14358=ORIENTED_EDGE('',*,*,#9798,.F.);
#14359=ORIENTED_EDGE('',*,*,#9799,.T.);
#14360=ORIENTED_EDGE('',*,*,#9795,.T.);
#14361=ORIENTED_EDGE('',*,*,#9800,.F.);
#14362=ORIENTED_EDGE('',*,*,#9801,.F.);
#14363=ORIENTED_EDGE('',*,*,#9802,.T.);
#14364=ORIENTED_EDGE('',*,*,#9798,.T.);
#14365=ORIENTED_EDGE('',*,*,#9803,.F.);
#14366=ORIENTED_EDGE('',*,*,#9804,.F.);
#14367=ORIENTED_EDGE('',*,*,#9805,.T.);
#14368=ORIENTED_EDGE('',*,*,#9801,.T.);
#14369=ORIENTED_EDGE('',*,*,#9806,.F.);
#14370=ORIENTED_EDGE('',*,*,#9807,.F.);
#14371=ORIENTED_EDGE('',*,*,#9808,.T.);
#14372=ORIENTED_EDGE('',*,*,#9804,.T.);
#14373=ORIENTED_EDGE('',*,*,#9809,.F.);
#14374=ORIENTED_EDGE('',*,*,#9810,.F.);
#14375=ORIENTED_EDGE('',*,*,#9763,.F.);
#14376=ORIENTED_EDGE('',*,*,#9811,.F.);
#14377=ORIENTED_EDGE('',*,*,#9812,.F.);
#14378=ORIENTED_EDGE('',*,*,#9813,.F.);
#14379=ORIENTED_EDGE('',*,*,#9814,.T.);
#14380=ORIENTED_EDGE('',*,*,#9815,.F.);
#14381=ORIENTED_EDGE('',*,*,#9814,.F.);
#14382=ORIENTED_EDGE('',*,*,#9811,.T.);
#14383=ORIENTED_EDGE('',*,*,#9762,.F.);
#14384=ORIENTED_EDGE('',*,*,#9766,.F.);
#14385=ORIENTED_EDGE('',*,*,#9769,.F.);
#14386=ORIENTED_EDGE('',*,*,#9772,.F.);
#14387=ORIENTED_EDGE('',*,*,#9775,.F.);
#14388=ORIENTED_EDGE('',*,*,#9778,.F.);
#14389=ORIENTED_EDGE('',*,*,#9781,.F.);
#14390=ORIENTED_EDGE('',*,*,#9784,.F.);
#14391=ORIENTED_EDGE('',*,*,#9787,.F.);
#14392=ORIENTED_EDGE('',*,*,#9790,.F.);
#14393=ORIENTED_EDGE('',*,*,#9793,.F.);
#14394=ORIENTED_EDGE('',*,*,#9796,.F.);
#14395=ORIENTED_EDGE('',*,*,#9799,.F.);
#14396=ORIENTED_EDGE('',*,*,#9802,.F.);
#14397=ORIENTED_EDGE('',*,*,#9805,.F.);
#14398=ORIENTED_EDGE('',*,*,#9808,.F.);
#14399=ORIENTED_EDGE('',*,*,#9816,.F.);
#14400=ORIENTED_EDGE('',*,*,#9817,.F.);
#14401=ORIENTED_EDGE('',*,*,#9713,.F.);
#14402=ORIENTED_EDGE('',*,*,#9717,.F.);
#14403=ORIENTED_EDGE('',*,*,#9720,.F.);
#14404=ORIENTED_EDGE('',*,*,#9723,.F.);
#14405=ORIENTED_EDGE('',*,*,#9726,.F.);
#14406=ORIENTED_EDGE('',*,*,#9729,.F.);
#14407=ORIENTED_EDGE('',*,*,#9732,.F.);
#14408=ORIENTED_EDGE('',*,*,#9735,.F.);
#14409=ORIENTED_EDGE('',*,*,#9738,.F.);
#14410=ORIENTED_EDGE('',*,*,#9741,.F.);
#14411=ORIENTED_EDGE('',*,*,#9744,.F.);
#14412=ORIENTED_EDGE('',*,*,#9747,.F.);
#14413=ORIENTED_EDGE('',*,*,#9750,.F.);
#14414=ORIENTED_EDGE('',*,*,#9753,.F.);
#14415=ORIENTED_EDGE('',*,*,#9756,.F.);
#14416=ORIENTED_EDGE('',*,*,#9759,.F.);
#14417=ORIENTED_EDGE('',*,*,#9818,.F.);
#14418=ORIENTED_EDGE('',*,*,#9807,.T.);
#14419=ORIENTED_EDGE('',*,*,#9819,.F.);
#14420=ORIENTED_EDGE('',*,*,#9820,.F.);
#14421=ORIENTED_EDGE('',*,*,#9816,.T.);
#14422=ORIENTED_EDGE('',*,*,#9810,.T.);
#14423=ORIENTED_EDGE('',*,*,#9813,.T.);
#14424=ORIENTED_EDGE('',*,*,#9821,.F.);
#14425=ORIENTED_EDGE('',*,*,#9760,.F.);
#14426=ORIENTED_EDGE('',*,*,#9757,.F.);
#14427=ORIENTED_EDGE('',*,*,#9754,.F.);
#14428=ORIENTED_EDGE('',*,*,#9751,.F.);
#14429=ORIENTED_EDGE('',*,*,#9748,.F.);
#14430=ORIENTED_EDGE('',*,*,#9745,.F.);
#14431=ORIENTED_EDGE('',*,*,#9742,.F.);
#14432=ORIENTED_EDGE('',*,*,#9739,.F.);
#14433=ORIENTED_EDGE('',*,*,#9736,.F.);
#14434=ORIENTED_EDGE('',*,*,#9733,.F.);
#14435=ORIENTED_EDGE('',*,*,#9730,.F.);
#14436=ORIENTED_EDGE('',*,*,#9727,.F.);
#14437=ORIENTED_EDGE('',*,*,#9724,.F.);
#14438=ORIENTED_EDGE('',*,*,#9721,.F.);
#14439=ORIENTED_EDGE('',*,*,#9718,.F.);
#14440=ORIENTED_EDGE('',*,*,#9715,.F.);
#14441=ORIENTED_EDGE('',*,*,#9822,.F.);
#14442=ORIENTED_EDGE('',*,*,#9819,.T.);
#14443=ORIENTED_EDGE('',*,*,#9809,.T.);
#14444=ORIENTED_EDGE('',*,*,#9806,.T.);
#14445=ORIENTED_EDGE('',*,*,#9803,.T.);
#14446=ORIENTED_EDGE('',*,*,#9800,.T.);
#14447=ORIENTED_EDGE('',*,*,#9797,.T.);
#14448=ORIENTED_EDGE('',*,*,#9794,.T.);
#14449=ORIENTED_EDGE('',*,*,#9791,.T.);
#14450=ORIENTED_EDGE('',*,*,#9788,.T.);
#14451=ORIENTED_EDGE('',*,*,#9785,.T.);
#14452=ORIENTED_EDGE('',*,*,#9782,.T.);
#14453=ORIENTED_EDGE('',*,*,#9779,.T.);
#14454=ORIENTED_EDGE('',*,*,#9776,.T.);
#14455=ORIENTED_EDGE('',*,*,#9773,.T.);
#14456=ORIENTED_EDGE('',*,*,#9770,.T.);
#14457=ORIENTED_EDGE('',*,*,#9767,.T.);
#14458=ORIENTED_EDGE('',*,*,#9764,.T.);
#14459=ORIENTED_EDGE('',*,*,#9758,.T.);
#14460=ORIENTED_EDGE('',*,*,#9821,.T.);
#14461=ORIENTED_EDGE('',*,*,#9812,.T.);
#14462=ORIENTED_EDGE('',*,*,#9818,.T.);
#14463=ORIENTED_EDGE('',*,*,#9823,.F.);
#14464=ORIENTED_EDGE('',*,*,#9824,.T.);
#14465=ORIENTED_EDGE('',*,*,#9825,.T.);
#14466=ORIENTED_EDGE('',*,*,#9826,.F.);
#14467=ORIENTED_EDGE('',*,*,#9827,.F.);
#14468=ORIENTED_EDGE('',*,*,#9828,.T.);
#14469=ORIENTED_EDGE('',*,*,#9829,.T.);
#14470=ORIENTED_EDGE('',*,*,#9824,.F.);
#14471=ORIENTED_EDGE('',*,*,#9830,.F.);
#14472=ORIENTED_EDGE('',*,*,#9831,.T.);
#14473=ORIENTED_EDGE('',*,*,#9832,.T.);
#14474=ORIENTED_EDGE('',*,*,#9828,.F.);
#14475=ORIENTED_EDGE('',*,*,#9833,.F.);
#14476=ORIENTED_EDGE('',*,*,#9834,.T.);
#14477=ORIENTED_EDGE('',*,*,#9835,.T.);
#14478=ORIENTED_EDGE('',*,*,#9831,.F.);
#14479=ORIENTED_EDGE('',*,*,#9836,.F.);
#14480=ORIENTED_EDGE('',*,*,#9837,.T.);
#14481=ORIENTED_EDGE('',*,*,#9838,.T.);
#14482=ORIENTED_EDGE('',*,*,#9834,.F.);
#14483=ORIENTED_EDGE('',*,*,#9839,.F.);
#14484=ORIENTED_EDGE('',*,*,#9826,.T.);
#14485=ORIENTED_EDGE('',*,*,#9840,.T.);
#14486=ORIENTED_EDGE('',*,*,#9837,.F.);
#14487=ORIENTED_EDGE('',*,*,#9840,.F.);
#14488=ORIENTED_EDGE('',*,*,#9825,.F.);
#14489=ORIENTED_EDGE('',*,*,#9829,.F.);
#14490=ORIENTED_EDGE('',*,*,#9832,.F.);
#14491=ORIENTED_EDGE('',*,*,#9835,.F.);
#14492=ORIENTED_EDGE('',*,*,#9838,.F.);
#14493=ORIENTED_EDGE('',*,*,#9841,.T.);
#14494=ORIENTED_EDGE('',*,*,#9817,.T.);
#14495=ORIENTED_EDGE('',*,*,#9820,.T.);
#14496=ORIENTED_EDGE('',*,*,#9822,.T.);
#14497=ORIENTED_EDGE('',*,*,#9714,.F.);
#14498=ORIENTED_EDGE('',*,*,#9841,.F.);
#14499=ORIENTED_EDGE('',*,*,#9842,.T.);
#14500=ORIENTED_EDGE('',*,*,#9843,.T.);
#14501=ORIENTED_EDGE('',*,*,#9842,.F.);
#14502=ORIENTED_EDGE('',*,*,#9843,.F.);
#14503=ORIENTED_EDGE('',*,*,#9823,.T.);
#14504=ORIENTED_EDGE('',*,*,#9839,.T.);
#14505=ORIENTED_EDGE('',*,*,#9836,.T.);
#14506=ORIENTED_EDGE('',*,*,#9833,.T.);
#14507=ORIENTED_EDGE('',*,*,#9830,.T.);
#14508=ORIENTED_EDGE('',*,*,#9827,.T.);
#14509=ORIENTED_EDGE('',*,*,#9815,.T.);
#14630=PLANE('',#16793);
#14631=PLANE('',#16794);
#14632=PLANE('',#16795);
#14633=PLANE('',#16796);
#14634=PLANE('',#16797);
#14635=PLANE('',#16798);
#14636=PLANE('',#16799);
#14637=PLANE('',#16800);
#14638=PLANE('',#16804);
#14639=PLANE('',#16805);
#15430=ADVANCED_FACE('',(#3450),#2345,.T.);
#15431=ADVANCED_FACE('',(#3451),#2346,.T.);
#15432=ADVANCED_FACE('',(#3452),#2347,.T.);
#15433=ADVANCED_FACE('',(#3453),#2348,.T.);
#15434=ADVANCED_FACE('',(#3454),#2349,.T.);
#15435=ADVANCED_FACE('',(#3455),#2350,.T.);
#15436=ADVANCED_FACE('',(#3456),#2351,.T.);
#15437=ADVANCED_FACE('',(#3457),#2352,.T.);
#15438=ADVANCED_FACE('',(#3458),#2353,.T.);
#15439=ADVANCED_FACE('',(#3459),#2354,.T.);
#15440=ADVANCED_FACE('',(#3460),#2355,.T.);
#15441=ADVANCED_FACE('',(#3461),#2356,.T.);
#15442=ADVANCED_FACE('',(#3462),#2357,.T.);
#15443=ADVANCED_FACE('',(#3463),#2358,.T.);
#15444=ADVANCED_FACE('',(#3464),#2359,.T.);
#15445=ADVANCED_FACE('',(#3465),#2360,.T.);
#15446=ADVANCED_FACE('',(#3466),#2361,.T.);
#15447=ADVANCED_FACE('',(#3467),#2362,.T.);
#15448=ADVANCED_FACE('',(#3468),#2363,.T.);
#15449=ADVANCED_FACE('',(#3469),#2364,.T.);
#15450=ADVANCED_FACE('',(#3470),#2365,.T.);
#15451=ADVANCED_FACE('',(#3471),#2366,.T.);
#15452=ADVANCED_FACE('',(#3472),#2367,.T.);
#15453=ADVANCED_FACE('',(#3473),#2368,.T.);
#15454=ADVANCED_FACE('',(#3474),#2369,.T.);
#15455=ADVANCED_FACE('',(#3475),#2370,.T.);
#15456=ADVANCED_FACE('',(#3476),#2371,.T.);
#15457=ADVANCED_FACE('',(#3477),#2372,.T.);
#15458=ADVANCED_FACE('',(#3478),#2373,.T.);
#15459=ADVANCED_FACE('',(#3479),#2374,.T.);
#15460=ADVANCED_FACE('',(#3480),#2375,.T.);
#15461=ADVANCED_FACE('',(#3481),#2376,.T.);
#15462=ADVANCED_FACE('',(#3482),#239,.T.);
#15463=ADVANCED_FACE('',(#3483),#264,.F.);
#15464=ADVANCED_FACE('',(#3484),#2377,.T.);
#15465=ADVANCED_FACE('',(#3485),#265,.F.);
#15466=ADVANCED_FACE('',(#3486),#2378,.T.);
#15467=ADVANCED_FACE('',(#3487),#14630,.F.);
#15468=ADVANCED_FACE('',(#3488),#14631,.F.);
#15469=ADVANCED_FACE('',(#3489),#14632,.F.);
#15470=ADVANCED_FACE('',(#3490),#14633,.F.);
#15471=ADVANCED_FACE('',(#3491),#14634,.F.);
#15472=ADVANCED_FACE('',(#3492),#14635,.F.);
#15473=ADVANCED_FACE('',(#3493),#14636,.F.);
#15474=ADVANCED_FACE('',(#3494,#1713),#14637,.T.);
#15475=ADVANCED_FACE('',(#3495),#2379,.T.);
#15476=ADVANCED_FACE('',(#3496,#1714),#14638,.F.);
#15477=ADVANCED_FACE('',(#3497),#14639,.T.);
#15495=CLOSED_SHELL('',(#15430,#15431,#15432,#15433,#15434,#15435,#15436,
#15437,#15438,#15439,#15440,#15441,#15442,#15443,#15444,#15445,#15446,#15447,
#15448,#15449,#15450,#15451,#15452,#15453,#15454,#15455,#15456,#15457,#15458,
#15459,#15460,#15461,#15462,#15463,#15464,#15465,#15466,#15467,#15468,#15469,
#15470,#15471,#15472,#15473,#15474,#15475,#15476,#15477));
#16752=AXIS2_PLACEMENT_3D('',#61228,#19684,#19685);
#16753=AXIS2_PLACEMENT_3D('',#61229,#19686,#19687);
#16754=AXIS2_PLACEMENT_3D('',#61245,#19689,#19690);
#16755=AXIS2_PLACEMENT_3D('',#61253,#19691,#19692);
#16756=AXIS2_PLACEMENT_3D('',#61301,#19694,#19695);
#16757=AXIS2_PLACEMENT_3D('',#61349,#19697,#19698);
#16758=AXIS2_PLACEMENT_3D('',#61403,#19700,#19701);
#16759=AXIS2_PLACEMENT_3D('',#61451,#19703,#19704);
#16760=AXIS2_PLACEMENT_3D('',#61499,#19706,#19707);
#16761=AXIS2_PLACEMENT_3D('',#61547,#19709,#19710);
#16762=AXIS2_PLACEMENT_3D('',#61601,#19712,#19713);
#16763=AXIS2_PLACEMENT_3D('',#61649,#19715,#19716);
#16764=AXIS2_PLACEMENT_3D('',#61697,#19718,#19719);
#16765=AXIS2_PLACEMENT_3D('',#61751,#19721,#19722);
#16766=AXIS2_PLACEMENT_3D('',#61799,#19724,#19725);
#16767=AXIS2_PLACEMENT_3D('',#61847,#19727,#19728);
#16768=AXIS2_PLACEMENT_3D('',#61898,#19730,#19731);
#16769=AXIS2_PLACEMENT_3D('',#61949,#19733,#19734);
#16770=AXIS2_PLACEMENT_3D('',#61997,#19736,#19737);
#16771=AXIS2_PLACEMENT_3D('',#62011,#19739,#19740);
#16772=AXIS2_PLACEMENT_3D('',#62019,#19741,#19742);
#16773=AXIS2_PLACEMENT_3D('',#62043,#19744,#19745);
#16774=AXIS2_PLACEMENT_3D('',#62067,#19747,#19748);
#16775=AXIS2_PLACEMENT_3D('',#62093,#19750,#19751);
#16776=AXIS2_PLACEMENT_3D('',#62117,#19753,#19754);
#16777=AXIS2_PLACEMENT_3D('',#62141,#19756,#19757);
#16778=AXIS2_PLACEMENT_3D('',#62166,#19759,#19760);
#16779=AXIS2_PLACEMENT_3D('',#62191,#19762,#19763);
#16780=AXIS2_PLACEMENT_3D('',#62215,#19765,#19766);
#16781=AXIS2_PLACEMENT_3D('',#62240,#19768,#19769);
#16782=AXIS2_PLACEMENT_3D('',#62265,#19771,#19772);
#16783=AXIS2_PLACEMENT_3D('',#62289,#19774,#19775);
#16784=AXIS2_PLACEMENT_3D('',#62313,#19777,#19778);
#16785=AXIS2_PLACEMENT_3D('',#62338,#19780,#19781);
#16786=AXIS2_PLACEMENT_3D('',#62363,#19783,#19784);
#16787=AXIS2_PLACEMENT_3D('',#62387,#19786,#19787);
#16788=AXIS2_PLACEMENT_3D('',#62576,#19788,#19789);
#16789=AXIS2_PLACEMENT_3D('',#62682,#19791,#19792);
#16790=AXIS2_PLACEMENT_3D('',#63214,#19793,#19794);
#16791=AXIS2_PLACEMENT_3D('',#63225,#19795,#19796);
#16792=AXIS2_PLACEMENT_3D('',#63759,#19797,#19798);
#16793=AXIS2_PLACEMENT_3D('',#63760,#19799,#19800);
#16794=AXIS2_PLACEMENT_3D('',#63769,#19805,#19806);
#16795=AXIS2_PLACEMENT_3D('',#63775,#19810,#19811);
#16796=AXIS2_PLACEMENT_3D('',#63781,#19815,#19816);
#16797=AXIS2_PLACEMENT_3D('',#63787,#19820,#19821);
#16798=AXIS2_PLACEMENT_3D('',#63793,#19825,#19826);
#16799=AXIS2_PLACEMENT_3D('',#63796,#19829,#19830);
#16800=AXIS2_PLACEMENT_3D('',#63797,#19831,#19832);
#16801=AXIS2_PLACEMENT_3D('',#63799,#19833,#19834);
#16802=AXIS2_PLACEMENT_3D('',#63800,#19835,#19836);
#16803=AXIS2_PLACEMENT_3D('',#63803,#19838,#19839);
#16804=AXIS2_PLACEMENT_3D('',#63804,#19840,#19841);
#16805=AXIS2_PLACEMENT_3D('',#63805,#19842,#19843);
#19684=DIRECTION('axis',(0.,0.,1.));
#19685=DIRECTION('refdir',(1.,0.,0.));
#19686=DIRECTION('center_axis',(0.,0.,1.));
#19687=DIRECTION('ref_axis',(1.,0.,0.));
#19688=DIRECTION('',(0.,0.,-1.));
#19689=DIRECTION('center_axis',(0.,0.,-1.));
#19690=DIRECTION('ref_axis',(1.,0.,0.));
#19691=DIRECTION('center_axis',(0.,0.,1.));
#19692=DIRECTION('ref_axis',(1.,0.,0.));
#19693=DIRECTION('',(0.,0.,-1.));
#19694=DIRECTION('center_axis',(0.,0.,1.));
#19695=DIRECTION('ref_axis',(1.,0.,0.));
#19696=DIRECTION('',(0.,0.,-1.));
#19697=DIRECTION('center_axis',(0.,0.,1.));
#19698=DIRECTION('ref_axis',(1.,0.,0.));
#19699=DIRECTION('',(0.,0.,-1.));
#19700=DIRECTION('center_axis',(0.,0.,1.));
#19701=DIRECTION('ref_axis',(1.,0.,0.));
#19702=DIRECTION('',(0.,0.,-1.));
#19703=DIRECTION('center_axis',(0.,0.,1.));
#19704=DIRECTION('ref_axis',(1.,0.,0.));
#19705=DIRECTION('',(0.,0.,-1.));
#19706=DIRECTION('center_axis',(0.,0.,1.));
#19707=DIRECTION('ref_axis',(1.,0.,0.));
#19708=DIRECTION('',(0.,0.,-1.));
#19709=DIRECTION('center_axis',(0.,0.,1.));
#19710=DIRECTION('ref_axis',(1.,0.,0.));
#19711=DIRECTION('',(0.,0.,-1.));
#19712=DIRECTION('center_axis',(0.,0.,1.));
#19713=DIRECTION('ref_axis',(1.,0.,0.));
#19714=DIRECTION('',(0.,0.,-1.));
#19715=DIRECTION('center_axis',(0.,0.,1.));
#19716=DIRECTION('ref_axis',(1.,0.,0.));
#19717=DIRECTION('',(0.,0.,-1.));
#19718=DIRECTION('center_axis',(0.,0.,1.));
#19719=DIRECTION('ref_axis',(1.,0.,0.));
#19720=DIRECTION('',(0.,0.,-1.));
#19721=DIRECTION('center_axis',(0.,0.,1.));
#19722=DIRECTION('ref_axis',(1.,0.,0.));
#19723=DIRECTION('',(0.,0.,-1.));
#19724=DIRECTION('center_axis',(0.,0.,1.));
#19725=DIRECTION('ref_axis',(1.,0.,0.));
#19726=DIRECTION('',(0.,0.,-1.));
#19727=DIRECTION('center_axis',(0.,0.,1.));
#19728=DIRECTION('ref_axis',(1.,0.,0.));
#19729=DIRECTION('',(0.,0.,-1.));
#19730=DIRECTION('center_axis',(0.,0.,1.));
#19731=DIRECTION('ref_axis',(1.,0.,0.));
#19732=DIRECTION('',(0.,0.,-1.));
#19733=DIRECTION('center_axis',(0.,0.,1.));
#19734=DIRECTION('ref_axis',(1.,0.,0.));
#19735=DIRECTION('',(0.,0.,-1.));
#19736=DIRECTION('center_axis',(0.,0.,1.));
#19737=DIRECTION('ref_axis',(1.,1.29731060939901E-13,0.));
#19738=DIRECTION('',(0.,0.,1.));
#19739=DIRECTION('center_axis',(0.,0.,-1.));
#19740=DIRECTION('ref_axis',(1.,1.29731060939901E-13,0.));
#19741=DIRECTION('center_axis',(0.,0.,1.));
#19742=DIRECTION('ref_axis',(1.,1.29731060939901E-13,0.));
#19743=DIRECTION('',(0.,0.,1.));
#19744=DIRECTION('center_axis',(0.,0.,1.));
#19745=DIRECTION('ref_axis',(1.,1.29731060939901E-13,0.));
#19746=DIRECTION('',(0.,0.,1.));
#19747=DIRECTION('center_axis',(0.,0.,1.));
#19748=DIRECTION('ref_axis',(1.,1.29731060939901E-13,0.));
#19749=DIRECTION('',(0.,0.,1.));
#19750=DIRECTION('center_axis',(0.,0.,1.));
#19751=DIRECTION('ref_axis',(1.,1.29731060939901E-13,0.));
#19752=DIRECTION('',(0.,0.,1.));
#19753=DIRECTION('center_axis',(0.,0.,1.));
#19754=DIRECTION('ref_axis',(1.,1.29731060939901E-13,0.));
#19755=DIRECTION('',(0.,0.,1.));
#19756=DIRECTION('center_axis',(0.,0.,1.));
#19757=DIRECTION('ref_axis',(1.,1.29731060939901E-13,0.));
#19758=DIRECTION('',(0.,0.,1.));
#19759=DIRECTION('center_axis',(0.,0.,1.));
#19760=DIRECTION('ref_axis',(1.,1.29731060939901E-13,0.));
#19761=DIRECTION('',(0.,0.,1.));
#19762=DIRECTION('center_axis',(0.,0.,1.));
#19763=DIRECTION('ref_axis',(1.,1.29731060939901E-13,0.));
#19764=DIRECTION('',(0.,0.,1.));
#19765=DIRECTION('center_axis',(0.,0.,1.));
#19766=DIRECTION('ref_axis',(1.,1.29731060939901E-13,0.));
#19767=DIRECTION('',(0.,0.,1.));
#19768=DIRECTION('center_axis',(0.,0.,1.));
#19769=DIRECTION('ref_axis',(1.,1.29731060939901E-13,0.));
#19770=DIRECTION('',(0.,0.,1.));
#19771=DIRECTION('center_axis',(0.,0.,1.));
#19772=DIRECTION('ref_axis',(1.,1.29731060939901E-13,0.));
#19773=DIRECTION('',(0.,0.,1.));
#19774=DIRECTION('center_axis',(0.,0.,1.));
#19775=DIRECTION('ref_axis',(1.,1.29731060939901E-13,0.));
#19776=DIRECTION('',(0.,0.,1.));
#19777=DIRECTION('center_axis',(0.,0.,1.));
#19778=DIRECTION('ref_axis',(1.,1.29731060939901E-13,0.));
#19779=DIRECTION('',(0.,0.,1.));
#19780=DIRECTION('center_axis',(0.,0.,1.));
#19781=DIRECTION('ref_axis',(1.,1.29731060939901E-13,0.));
#19782=DIRECTION('',(0.,0.,1.));
#19783=DIRECTION('center_axis',(0.,0.,1.));
#19784=DIRECTION('ref_axis',(1.,1.29731060939901E-13,0.));
#19785=DIRECTION('',(0.,0.,1.));
#19786=DIRECTION('center_axis',(0.,0.,-1.));
#19787=DIRECTION('ref_axis',(1.,0.,0.));
#19788=DIRECTION('center_axis',(0.,0.,-1.));
#19789=DIRECTION('ref_axis',(1.,0.,0.));
#19790=DIRECTION('',(0.707106781186548,8.65956056235494E-17,0.707106781186547));
#19791=DIRECTION('center_axis',(0.,0.,1.));
#19792=DIRECTION('ref_axis',(1.,0.,0.));
#19793=DIRECTION('center_axis',(0.,0.,1.));
#19794=DIRECTION('ref_axis',(1.,1.29731060939901E-13,0.));
#19795=DIRECTION('center_axis',(0.,0.,-1.));
#19796=DIRECTION('ref_axis',(1.,1.29731060939901E-13,0.));
#19797=DIRECTION('center_axis',(0.,0.,1.));
#19798=DIRECTION('ref_axis',(1.,0.,0.));
#19799=DIRECTION('center_axis',(-1.60246890531964E-16,-1.,0.));
#19800=DIRECTION('ref_axis',(1.,-1.60246890531964E-16,0.));
#19801=DIRECTION('',(1.,-1.60246890531964E-16,0.));
#19802=DIRECTION('',(0.,0.,1.));
#19803=DIRECTION('',(1.,-1.60246890531964E-16,0.));
#19804=DIRECTION('',(0.,0.,1.));
#19805=DIRECTION('center_axis',(-0.866025403784439,-0.5,0.));
#19806=DIRECTION('ref_axis',(0.5,-0.866025403784439,0.));
#19807=DIRECTION('',(0.5,-0.866025403784439,0.));
#19808=DIRECTION('',(0.,0.,1.));
#19809=DIRECTION('',(0.5,-0.866025403784439,0.));
#19810=DIRECTION('center_axis',(-0.866025403784439,0.5,0.));
#19811=DIRECTION('ref_axis',(-0.5,-0.866025403784439,0.));
#19812=DIRECTION('',(-0.5,-0.866025403784439,0.));
#19813=DIRECTION('',(0.,0.,1.));
#19814=DIRECTION('',(-0.5,-0.866025403784439,0.));
#19815=DIRECTION('center_axis',(1.60246890531964E-16,1.,0.));
#19816=DIRECTION('ref_axis',(-1.,1.60246890531964E-16,0.));
#19817=DIRECTION('',(-1.,1.60246890531964E-16,0.));
#19818=DIRECTION('',(0.,0.,1.));
#19819=DIRECTION('',(-1.,1.60246890531964E-16,0.));
#19820=DIRECTION('center_axis',(0.866025403784439,0.5,0.));
#19821=DIRECTION('ref_axis',(-0.5,0.866025403784439,0.));
#19822=DIRECTION('',(-0.5,0.866025403784439,0.));
#19823=DIRECTION('',(0.,0.,1.));
#19824=DIRECTION('',(-0.5,0.866025403784439,0.));
#19825=DIRECTION('center_axis',(0.866025403784439,-0.5,0.));
#19826=DIRECTION('ref_axis',(0.5,0.866025403784439,0.));
#19827=DIRECTION('',(0.5,0.866025403784439,0.));
#19828=DIRECTION('',(0.5,0.866025403784439,0.));
#19829=DIRECTION('center_axis',(0.,0.,1.));
#19830=DIRECTION('ref_axis',(1.,0.,0.));
#19831=DIRECTION('center_axis',(0.,0.,1.));
#19832=DIRECTION('ref_axis',(1.,0.,0.));
#19833=DIRECTION('center_axis',(0.,0.,1.));
#19834=DIRECTION('ref_axis',(1.,0.,0.));
#19835=DIRECTION('center_axis',(0.,0.,1.));
#19836=DIRECTION('ref_axis',(1.,0.,0.));
#19837=DIRECTION('',(0.,0.,-1.));
#19838=DIRECTION('center_axis',(0.,0.,1.));
#19839=DIRECTION('ref_axis',(1.,0.,0.));
#19840=DIRECTION('center_axis',(0.,0.,1.));
#19841=DIRECTION('ref_axis',(1.,0.,0.));
#19842=DIRECTION('center_axis',(0.,0.,1.));
#19843=DIRECTION('ref_axis',(1.,0.,0.));
#61228=CARTESIAN_POINT('',(0.,0.,0.));
#61229=CARTESIAN_POINT('Origin',(0.,0.,0.));
#61230=CARTESIAN_POINT('',(-1.95633559071744,0.0012731057411345,0.225869692124231));
#61231=CARTESIAN_POINT('',(-1.95587799559821,0.00207186393275607,0.124130307875758));
#61232=CARTESIAN_POINT('',(-1.954,-2.39295984553393E-16,0.));
#61233=CARTESIAN_POINT('',(0.861525859670522,1.75382131162755,0.));
#61234=CARTESIAN_POINT('Ctrl Pts',(-1.95633559071744,0.0012731057411345,
0.225869692124231));
#61235=CARTESIAN_POINT('Ctrl Pts',(-1.95680032440099,0.0682557629313676,
0.222037301306047));
#61236=CARTESIAN_POINT('Ctrl Pts',(-1.95365903766855,0.135191473590706,
0.218204910487863));
#61237=CARTESIAN_POINT('Ctrl Pts',(-1.94676806606145,0.201735328972743,
0.214372519669679));
#61238=CARTESIAN_POINT('Ctrl Pts',(-1.88017193281744,0.844832371344698,
0.1773353028412));
#61239=CARTESIAN_POINT('Ctrl Pts',(-1.46336311091822,1.45133095416213,0.140298086012721));
#61240=CARTESIAN_POINT('Ctrl Pts',(-0.886884671668765,1.7445317403525,0.103260869184242));
#61241=CARTESIAN_POINT('Ctrl Pts',(-0.351138290053491,2.01701592986141,
0.0688405794561611));
#61242=CARTESIAN_POINT('Ctrl Pts',(0.322511385444639,2.01891139473935,0.0344202897280807));
#61243=CARTESIAN_POINT('Ctrl Pts',(0.863567639152679,1.75641488315944,2.92734586571086E-17));
#61244=CARTESIAN_POINT('',(-0.861525859670574,1.75382131162752,1.38777878078145E-16));
#61245=CARTESIAN_POINT('Origin',(0.,0.,0.));
#61246=CARTESIAN_POINT('Ctrl Pts',(-0.861525859670571,1.75382131162752,
2.28983498828939E-15));
#61247=CARTESIAN_POINT('Ctrl Pts',(-1.44496782441851,1.46721837385109,0.0370621399437224));
#61248=CARTESIAN_POINT('Ctrl Pts',(-1.8691020329229,0.869083656944534,0.0741242798874424));
#61249=CARTESIAN_POINT('Ctrl Pts',(-1.94380023116171,0.227435527544788,
0.111186419831163));
#61250=CARTESIAN_POINT('Ctrl Pts',(-1.95249630318745,0.152737362394887,
0.115501049179361));
#61251=CARTESIAN_POINT('Ctrl Pts',(-1.95645657185248,0.0774494727773659,
0.119815678527559));
#61252=CARTESIAN_POINT('Ctrl Pts',(-1.95587799559821,0.00207186393275607,
0.124130307875758));
#61253=CARTESIAN_POINT('Origin',(0.,0.,0.));
#61254=CARTESIAN_POINT('',(-1.95128203910989,0.000979727872364722,0.92586969212423));
#61255=CARTESIAN_POINT('',(-1.95118672945361,0.000916100096969453,0.824130307875757));
#61256=CARTESIAN_POINT('',(-1.954,-2.39295984553393E-16,0.));
#61257=CARTESIAN_POINT('Ctrl Pts',(-1.95128203910989,0.000979727872364722,
0.92586969212423));
#61258=CARTESIAN_POINT('Ctrl Pts',(-1.9524730612105,0.263901717292074,0.910927268943587));
#61259=CARTESIAN_POINT('Ctrl Pts',(-1.90305141123492,0.526394079969068,
0.895984845762944));
#61260=CARTESIAN_POINT('Ctrl Pts',(-1.80089049647467,0.766440059940591,
0.881042422582301));
#61261=CARTESIAN_POINT('Ctrl Pts',(-1.54766811710363,1.36143291361156,0.844005205753822));
#61262=CARTESIAN_POINT('Ctrl Pts',(-0.970428066964404,1.81852045762203,
0.806967988925342));
#61263=CARTESIAN_POINT('Ctrl Pts',(-0.333230591869142,1.92861999489257,
0.769930772096863));
#61264=CARTESIAN_POINT('Ctrl Pts',(0.30396688322612,2.0387195321631,0.732893555268385));
#61265=CARTESIAN_POINT('Ctrl Pts',(1.00112178327742,1.8018310626937,0.695856338439906));
#61266=CARTESIAN_POINT('Ctrl Pts',(1.43930998255098,1.32629143144902,0.658819121611426));
#61267=CARTESIAN_POINT('Ctrl Pts',(1.87749818182454,0.850751800204341,0.621781904782947));
#61268=CARTESIAN_POINT('Ctrl Pts',(2.05671968032037,0.136561007184397,0.584744687954468));
#61269=CARTESIAN_POINT('Ctrl Pts',(1.89499805994521,-0.489512382298273,
0.547707471125989));
#61270=CARTESIAN_POINT('Ctrl Pts',(1.73327643957006,-1.11558577178094,0.51067025429751));
#61271=CARTESIAN_POINT('Ctrl Pts',(1.23061170032392,-1.65354175772633,0.473633037469032));
#61272=CARTESIAN_POINT('Ctrl Pts',(0.616932989107385,-1.8573955796291,0.436595820640553));
#61273=CARTESIAN_POINT('Ctrl Pts',(0.00325427789084558,-2.06124940153187,
0.399558603812074));
#61274=CARTESIAN_POINT('Ctrl Pts',(-0.721438405296094,-1.93100105939202,
0.362521386983595));
#61275=CARTESIAN_POINT('Ctrl Pts',(-1.22559302459517,-1.52602913735885,
0.325484170155115));
#61276=CARTESIAN_POINT('Ctrl Pts',(-1.67758072371516,-1.1629613001496,0.29227934414482));
#61277=CARTESIAN_POINT('Ctrl Pts',(-1.95230901779331,-0.579081973692791,
0.259074518134526));
#61278=CARTESIAN_POINT('Ctrl Pts',(-1.95633559071744,0.0012731057411345,
0.225869692124231));
#61279=CARTESIAN_POINT('Ctrl Pts',(-1.95587799559821,0.00207186393275607,
0.124130307875758));
#61280=CARTESIAN_POINT('Ctrl Pts',(-1.95148667238412,-0.570034995103637,
0.15687781847128));
#61281=CARTESIAN_POINT('Ctrl Pts',(-1.68562951923343,-1.14731024226281,
0.189625329066803));
#61282=CARTESIAN_POINT('Ctrl Pts',(-1.2444215732779,-1.51113938431406,0.222372839662326));
#61283=CARTESIAN_POINT('Ctrl Pts',(-0.745082529182101,-1.92290462488019,
0.259434979606046));
#61284=CARTESIAN_POINT('Ctrl Pts',(-0.0211422530173012,-2.0612735641195,
0.296497119549767));
#61285=CARTESIAN_POINT('Ctrl Pts',(0.595334795120667,-1.86428772433344,
0.333559259493488));
#61286=CARTESIAN_POINT('Ctrl Pts',(1.21181184325864,-1.66730188454737,0.370621399437209));
#61287=CARTESIAN_POINT('Ctrl Pts',(1.72082566336977,-1.13496126573593,0.40768353938093));
#61288=CARTESIAN_POINT('Ctrl Pts',(1.8894870924304,-0.510370283185346,0.444745679324651));
#61289=CARTESIAN_POINT('Ctrl Pts',(2.05814852149104,0.114220699365238,0.481807819268372));
#61290=CARTESIAN_POINT('Ctrl Pts',(1.88645755950116,0.831062045654966,0.518869959212093));
#61291=CARTESIAN_POINT('Ctrl Pts',(1.45292142815886,1.31145007703775,0.555932099155814));
#61292=CARTESIAN_POINT('Ctrl Pts',(1.01938529681656,1.79183810842053,0.592994239099535));
#61293=CARTESIAN_POINT('Ctrl Pts',(0.324003996121834,2.03577282489637,0.630056379043256));
#61294=CARTESIAN_POINT('Ctrl Pts',(-0.314654015224673,1.93172336479658,
0.667118518986976));
#61295=CARTESIAN_POINT('Ctrl Pts',(-0.953312026571179,1.8276739046968,0.704180658930697));
#61296=CARTESIAN_POINT('Ctrl Pts',(-1.53524674856946,1.37564026802139,0.741242798874417));
#61297=CARTESIAN_POINT('Ctrl Pts',(-1.79395555636014,0.782560471576942,
0.778304938818138));
#61298=CARTESIAN_POINT('Ctrl Pts',(-1.90058212652462,0.538123240897563,
0.793580061837345));
#61299=CARTESIAN_POINT('Ctrl Pts',(-1.95230335199157,0.269726953471863,
0.808855184856551));
#61300=CARTESIAN_POINT('Ctrl Pts',(-1.95118672945361,0.000916100096969453,
0.824130307875757));
#61301=CARTESIAN_POINT('Origin',(0.,0.,0.));
#61302=CARTESIAN_POINT('',(-1.95279554503994,-0.00168121501241181,1.62586969212423));
#61303=CARTESIAN_POINT('',(-1.95287184048439,-0.001702989282844,1.52413030787576));
#61304=CARTESIAN_POINT('',(-1.954,-2.39295984553393E-16,0.));
#61305=CARTESIAN_POINT('Ctrl Pts',(-1.95279554503994,-0.00168121501241181,
1.62586969212423));
#61306=CARTESIAN_POINT('Ctrl Pts',(-1.94903656010943,0.455834752155161,
1.59981723658113));
#61307=CARTESIAN_POINT('Ctrl Pts',(-1.78856730317397,0.91572573117829,1.57376478103802));
#61308=CARTESIAN_POINT('Ctrl Pts',(-1.49500760249196,1.26316552728133,1.54771232549492));
#61309=CARTESIAN_POINT('Ctrl Pts',(-1.07767134532899,1.75709989142681,1.51067510866644));
#61310=CARTESIAN_POINT('Ctrl Pts',(-0.39135122029848,2.02376358702057,1.47363789183796));
#61311=CARTESIAN_POINT('Ctrl Pts',(0.249990333148566,1.94116955279127,1.43660067500948));
#61312=CARTESIAN_POINT('Ctrl Pts',(0.891331886595613,1.85857551856197,1.39956345818101));
#61313=CARTESIAN_POINT('Ctrl Pts',(1.4876948684592,1.42672375450961,1.36252624135253));
#61314=CARTESIAN_POINT('Ctrl Pts',(1.76626827046517,0.843167597229759,1.32548902452405));
#61315=CARTESIAN_POINT('Ctrl Pts',(2.04484167247113,0.259611439949913,1.28845180769557));
#61316=CARTESIAN_POINT('Ctrl Pts',(2.00562549461947,-0.475649110557425,
1.25141459086709));
#61317=CARTESIAN_POINT('Ctrl Pts',(1.66655969053473,-1.02626219289756,1.21437737403861));
#61318=CARTESIAN_POINT('Ctrl Pts',(1.32749388644999,-1.57687527523771,1.17734015721013));
#61319=CARTESIAN_POINT('Ctrl Pts',(0.688578456132156,-1.94284088941065,
1.14030294038165));
#61320=CARTESIAN_POINT('Ctrl Pts',(0.0420898544956178,-1.9567474659654,
1.10326572355317));
#61321=CARTESIAN_POINT('Ctrl Pts',(-0.604398747140919,-1.97065404252014,
1.06622850672469));
#61322=CARTESIAN_POINT('Ctrl Pts',(-1.25846052009616,-1.6325015814567,1.02919128989622));
#61323=CARTESIAN_POINT('Ctrl Pts',(-1.62088905227235,-1.09697626925925,
0.992154073067737));
#61324=CARTESIAN_POINT('Ctrl Pts',(-1.83709816073764,-0.777505145902677,
0.970059279419901));
#61325=CARTESIAN_POINT('Ctrl Pts',(-1.94952091996443,-0.387793032173158,
0.947964485772066));
#61326=CARTESIAN_POINT('Ctrl Pts',(-1.95128203910989,0.000979727872364722,
0.92586969212423));
#61327=CARTESIAN_POINT('Ctrl Pts',(-1.95118672945361,0.000916100096969453,
0.824130307875757));
#61328=CARTESIAN_POINT('Ctrl Pts',(-1.94959408276249,-0.382490737583375,
0.845917324800272));
#61329=CARTESIAN_POINT('Ctrl Pts',(-1.84051065227066,-0.766740948347571,
0.867704341724787));
#61330=CARTESIAN_POINT('Ctrl Pts',(-1.62993550876047,-1.0835175828476,0.889491358649302));
#61331=CARTESIAN_POINT('Ctrl Pts',(-1.27172375978704,-1.62238988461419,
0.926553498593023));
#61332=CARTESIAN_POINT('Ctrl Pts',(-0.619817368257128,-1.96600853193387,
0.963615638536743));
#61333=CARTESIAN_POINT('Ctrl Pts',(0.0271864367452719,-1.95701720127518,
1.00067777848046));
#61334=CARTESIAN_POINT('Ctrl Pts',(0.674190241747668,-1.94802587061648,
1.03773991842418));
#61335=CARTESIAN_POINT('Ctrl Pts',(1.31629146022255,-1.5864245619794,1.07480205836791));
#61336=CARTESIAN_POINT('Ctrl Pts',(1.65939903784035,-1.03781956343241,1.11186419831163));
#61337=CARTESIAN_POINT('Ctrl Pts',(2.00250661545815,-0.489214564885407,
1.14892633825535));
#61338=CARTESIAN_POINT('Ctrl Pts',(2.04662055221888,0.246394123571516,1.18598847819907));
#61339=CARTESIAN_POINT('Ctrl Pts',(1.77153295980734,0.832073910176122,1.22305061814279));
#61340=CARTESIAN_POINT('Ctrl Pts',(1.49644536739581,1.41775369678073,1.26011275808651));
#61341=CARTESIAN_POINT('Ctrl Pts',(0.902156245812001,1.85350458153303,1.29717489803023));
#61342=CARTESIAN_POINT('Ctrl Pts',(0.260864347694114,1.93974733338565,1.33423703797395));
#61343=CARTESIAN_POINT('Ctrl Pts',(-0.380427550423769,2.02599008523827,
1.37129917791767));
#61344=CARTESIAN_POINT('Ctrl Pts',(-1.06872222507573,1.76272470419122,1.40836131786139));
#61345=CARTESIAN_POINT('Ctrl Pts',(-1.48876654315921,1.27053027794487,1.44542345780511));
#61346=CARTESIAN_POINT('Ctrl Pts',(-1.78610829781436,0.922114770268632,
1.47165907449533));
#61347=CARTESIAN_POINT('Ctrl Pts',(-1.94903067523895,0.458983666015645,
1.49789469118554));
#61348=CARTESIAN_POINT('Ctrl Pts',(-1.95287184048439,-0.001702989282844,
1.52413030787576));
#61349=CARTESIAN_POINT('Origin',(0.,0.,0.));
#61350=CARTESIAN_POINT('',(-1.9571996697324,4.08272333451705E-5,2.32586969212423));
#61351=CARTESIAN_POINT('',(-1.95720915199432,4.37834080700025E-5,2.22413030787575));
#61352=CARTESIAN_POINT('',(-1.954,-2.39295984553393E-16,0.));
#61353=CARTESIAN_POINT('Ctrl Pts',(-1.9571996697324,4.08272333451412E-5,
2.32586969212423));
#61354=CARTESIAN_POINT('Ctrl Pts',(-1.9572003426898,0.00222795607483405,
2.32574442104715));
#61355=CARTESIAN_POINT('Ctrl Pts',(-1.95719699336635,0.00441508279392128,
2.32561914997006));
#61356=CARTESIAN_POINT('Ctrl Pts',(-1.95718961556757,0.00660219592375261,
2.32549387889298));
#61357=CARTESIAN_POINT('Ctrl Pts',(-1.9550083208942,0.653236559609951,2.2884566620645));
#61358=CARTESIAN_POINT('Ctrl Pts',(-1.60068669068514,1.29868304829585,2.25141944523602));
#61359=CARTESIAN_POINT('Ctrl Pts',(-1.05631192010051,1.64767712566922,2.21438222840754));
#61360=CARTESIAN_POINT('Ctrl Pts',(-0.511937149515876,1.9966712030426,2.17734501157906));
#61361=CARTESIAN_POINT('Ctrl Pts',(0.222490761444335,2.04921286910345,2.14030779475058));
#61362=CARTESIAN_POINT('Ctrl Pts',(0.811002035332165,1.78126653559889,2.10327057792211));
#61363=CARTESIAN_POINT('Ctrl Pts',(1.39951330921999,1.51332020209433,2.06623336109363));
#61364=CARTESIAN_POINT('Ctrl Pts',(1.84210794603544,0.92488586902436,2.02919614426515));
#61365=CARTESIAN_POINT('Ctrl Pts',(1.93631757329266,0.28514740055385,1.99215892743667));
#61366=CARTESIAN_POINT('Ctrl Pts',(2.03052720054988,-0.354591067916664,
1.95512171060819));
#61367=CARTESIAN_POINT('Ctrl Pts',(1.77635181824887,-1.04563367178771,1.91808449377971));
#61368=CARTESIAN_POINT('Ctrl Pts',(1.29006594271768,-1.47185755477259,1.88104727695123));
#61369=CARTESIAN_POINT('Ctrl Pts',(0.803780067186484,-1.89808143775746,
1.84401006012275));
#61370=CARTESIAN_POINT('Ctrl Pts',(0.0853836984250916,-2.05948659985616,
1.80697284329427));
#61371=CARTESIAN_POINT('Ctrl Pts',(-0.536487147273854,-1.88223703762279,
1.76993562646579));
#61372=CARTESIAN_POINT('Ctrl Pts',(-1.1583579929728,-1.70498747538942,1.73289840963732));
#61373=CARTESIAN_POINT('Ctrl Pts',(-1.68370331560931,-1.18908318882399,
1.69586119280884));
#61374=CARTESIAN_POINT('Ctrl Pts',(-1.87219978227984,-0.570528529192665,
1.65882397598036));
#61375=CARTESIAN_POINT('Ctrl Pts',(-1.92810540551016,-0.387073187246384,
1.64783921469498));
#61376=CARTESIAN_POINT('Ctrl Pts',(-1.95438048401311,-0.194588316428208,
1.63685445340961));
#61377=CARTESIAN_POINT('Ctrl Pts',(-1.95279554503994,-0.00168121501241192,
1.62586969212423));
#61378=CARTESIAN_POINT('Ctrl Pts',(-1.95287184048439,-0.00170298928284375,
1.52413030787576));
#61379=CARTESIAN_POINT('Ctrl Pts',(-1.95445695530526,-0.191812291650776,
1.53495683112926));
#61380=CARTESIAN_POINT('Ctrl Pts',(-1.92895173588402,-0.381505322742495,
1.54578335438277));
#61381=CARTESIAN_POINT('Ctrl Pts',(-1.87462310228398,-0.562548805321496,
1.55660987763628));
#61382=CARTESIAN_POINT('Ctrl Pts',(-1.68864138181028,-1.18230999089587,
1.59367201758));
#61383=CARTESIAN_POINT('Ctrl Pts',(-1.16488397934787,-1.70070889059895,
1.63073415752372));
#61384=CARTESIAN_POINT('Ctrl Pts',(-0.543243355780667,-1.88030816136644,
1.66779629746744));
#61385=CARTESIAN_POINT('Ctrl Pts',(0.0783972677865321,-2.05990743213392,
1.70485843741116));
#61386=CARTESIAN_POINT('Ctrl Pts',(0.797921112458524,-1.90070707396579,
1.74192057735488));
#61387=CARTESIAN_POINT('Ctrl Pts',(1.28577075941843,-1.47562399010748,1.7789827172986));
#61388=CARTESIAN_POINT('Ctrl Pts',(1.77362040637834,-1.05054090624917,1.81604485724232));
#61389=CARTESIAN_POINT('Ctrl Pts',(2.02979585562615,-0.359575096700667,
1.85310699718604));
#61390=CARTESIAN_POINT('Ctrl Pts',(1.93696313672928,0.28079594435252,1.89016913712977));
#61391=CARTESIAN_POINT('Ctrl Pts',(1.84413041783241,0.921166985405712,1.92723127707349));
#61392=CARTESIAN_POINT('Ctrl Pts',(1.40228953079084,1.51094325796358,1.96429341701721));
#61393=CARTESIAN_POINT('Ctrl Pts',(0.813813216582781,1.77999452248681,2.00135555696093));
#61394=CARTESIAN_POINT('Ctrl Pts',(0.225336902374724,2.04904578701004,2.03841769690465));
#61395=CARTESIAN_POINT('Ctrl Pts',(-0.509774838999831,1.99737204349863,
2.07547983684837));
#61396=CARTESIAN_POINT('Ctrl Pts',(-1.05482489992153,1.64864094185095,2.11254197679209));
#61397=CARTESIAN_POINT('Ctrl Pts',(-1.59987496084323,1.29990984020327,2.14960411673581));
#61398=CARTESIAN_POINT('Ctrl Pts',(-1.95486334131209,0.654121380419318,
2.18666625667953));
#61399=CARTESIAN_POINT('Ctrl Pts',(-1.95719765431867,0.0070607094029605,
2.22372839662325));
#61400=CARTESIAN_POINT('Ctrl Pts',(-1.95720609227958,0.00472174601940803,
2.22386236704075));
#61401=CARTESIAN_POINT('Ctrl Pts',(-1.95720992231195,0.00238276601260064,
2.22399633745825));
#61402=CARTESIAN_POINT('Ctrl Pts',(-1.95720915199432,4.37834080701142E-5,
2.22413030787575));
#61403=CARTESIAN_POINT('Origin',(0.,0.,0.));
#61404=CARTESIAN_POINT('',(-1.95267691385146,0.00165493661177622,3.02586969212423));
#61405=CARTESIAN_POINT('',(-1.95274315056508,0.00167675988910205,2.92413030787576));
#61406=CARTESIAN_POINT('',(-1.954,-2.39295984553393E-16,0.));
#61407=CARTESIAN_POINT('Ctrl Pts',(-1.95267691385146,0.00165493661177622,
3.02586969212423));
#61408=CARTESIAN_POINT('Ctrl Pts',(-1.95426560914452,0.198992208020636,
3.01463438868469));
#61409=CARTESIAN_POINT('Ctrl Pts',(-1.92675342506316,0.395896803504792,
3.00339908524515));
#61410=CARTESIAN_POINT('Ctrl Pts',(-1.86830808103941,0.583146374609883,
2.9921637818056));
#61411=CARTESIAN_POINT('Ctrl Pts',(-1.67564280138135,1.20041523640586,2.95512656497712));
#61412=CARTESIAN_POINT('Ctrl Pts',(-1.14682887836242,1.71276357431471,2.91808934814864));
#61413=CARTESIAN_POINT('Ctrl Pts',(-0.523776367443795,1.8858136432031,2.88105213132016));
#61414=CARTESIAN_POINT('Ctrl Pts',(0.0992761434748341,2.0588637120915,2.84401491449168));
#61415=CARTESIAN_POINT('Ctrl Pts',(0.816567242293159,1.89261551195942,2.80697769766321));
#61416=CARTESIAN_POINT('Ctrl Pts',(1.29996651882171,1.46312057934516,2.76994048083473));
#61417=CARTESIAN_POINT('Ctrl Pts',(1.78336579535026,1.03362564673089,2.73290326400625));
#61418=CARTESIAN_POINT('Ctrl Pts',(2.03287324958903,0.340883981634439,2.69586604717777));
#61419=CARTESIAN_POINT('Ctrl Pts',(1.93434974962867,-0.298204336020968,
2.65882883034929));
#61420=CARTESIAN_POINT('Ctrl Pts',(1.83582624966831,-0.937292653676373,
2.62179161352081));
#61421=CARTESIAN_POINT('Ctrl Pts',(1.38927179550881,-1.52272762389073,2.58475439669233));
#61422=CARTESIAN_POINT('Ctrl Pts',(0.798966206784796,-1.78669745083631,
2.54771717986385));
#61423=CARTESIAN_POINT('Ctrl Pts',(0.208660618060775,-2.05066727778188,
2.51067996303538));
#61424=CARTESIAN_POINT('Ctrl Pts',(-0.525396105227766,-1.99317196145866,
2.4736427462069));
#61425=CARTESIAN_POINT('Ctrl Pts',(-1.0674039873032,-1.6405131839538,2.43660552937842));
#61426=CARTESIAN_POINT('Ctrl Pts',(-1.60757863467609,-1.28904720517098,
2.39969358362702));
#61427=CARTESIAN_POINT('Ctrl Pts',(-1.95700137841649,-0.644411052866131,
2.36278163787563));
#61428=CARTESIAN_POINT('Ctrl Pts',(-1.9571996697324,4.08272333451705E-5,
2.32586969212423));
#61429=CARTESIAN_POINT('Ctrl Pts',(-1.95720915199432,4.37834080700025E-5,
2.22413030787575));
#61430=CARTESIAN_POINT('Ctrl Pts',(-1.95699681840184,-0.644683222376,2.26105847740198));
#61431=CARTESIAN_POINT('Ctrl Pts',(-1.60725113883781,-1.28960760246236,
2.2979866469282));
#61432=CARTESIAN_POINT('Ctrl Pts',(-1.06669244200308,-1.64098742623895,
2.33491481645442));
#61433=CARTESIAN_POINT('Ctrl Pts',(-0.524172671136578,-1.99364200861572,
2.37197695639814));
#61434=CARTESIAN_POINT('Ctrl Pts',(0.210547116140745,-2.05061829112049,
2.40903909634186));
#61435=CARTESIAN_POINT('Ctrl Pts',(0.800949322066953,-1.78581989384044,
2.44610123628558));
#61436=CARTESIAN_POINT('Ctrl Pts',(1.39135152799316,-1.52102149656038,2.4831633762293));
#61437=CARTESIAN_POINT('Ctrl Pts',(1.83743615256826,-0.934448419495488,
2.52022551617302));
#61438=CARTESIAN_POINT('Ctrl Pts',(1.93488676008295,-0.294763859316313,
2.55728765611674));
#61439=CARTESIAN_POINT('Ctrl Pts',(2.03233736759764,0.344920700862864,2.59434979606046));
#61440=CARTESIAN_POINT('Ctrl Pts',(1.78115395805193,1.03771674415633,2.63141193600418));
#61441=CARTESIAN_POINT('Ctrl Pts',(1.29638398231036,1.46630865646616,2.6684740759479));
#61442=CARTESIAN_POINT('Ctrl Pts',(0.811614006568792,1.894900568776,2.70553621589162));
#61443=CARTESIAN_POINT('Ctrl Pts',(0.0932574646313782,2.05928835010221,
2.74259835583535));
#61444=CARTESIAN_POINT('Ctrl Pts',(-0.529662765081927,1.88417882975093,
2.77966049577907));
#61445=CARTESIAN_POINT('Ctrl Pts',(-1.15258299479523,1.70906930939964,2.81672263572279));
#61446=CARTESIAN_POINT('Ctrl Pts',(-1.68006691228442,1.19446248737086,2.85378477566651));
#61447=CARTESIAN_POINT('Ctrl Pts',(-1.87051544101399,0.576059451476712,
2.89084691561023));
#61448=CARTESIAN_POINT('Ctrl Pts',(-1.92752575844056,0.390941962730205,
2.90194137969874));
#61449=CARTESIAN_POINT('Ctrl Pts',(-1.95433466869055,0.196523398123763,
2.91303584378725));
#61450=CARTESIAN_POINT('Ctrl Pts',(-1.95274315056508,0.00167675988910205,
2.92413030787576));
#61451=CARTESIAN_POINT('Origin',(0.,0.,0.));
#61452=CARTESIAN_POINT('',(-1.95135107115213,-0.00103745302926256,3.72586969212423));
#61453=CARTESIAN_POINT('',(-1.95125983814034,-0.000967513988672578,3.62413030787576));
#61454=CARTESIAN_POINT('',(-1.954,-2.39295984553393E-16,0.));
#61455=CARTESIAN_POINT('Ctrl Pts',(-1.95135107115213,-0.00103745302926256,
3.72586969212423));
#61456=CARTESIAN_POINT('Ctrl Pts',(-1.9494564270682,0.392108141373472,3.70352435632223));
#61457=CARTESIAN_POINT('Ctrl Pts',(-1.83428685915158,0.78627490539017,3.68117902052023));
#61458=CARTESIAN_POINT('Ctrl Pts',(-1.61345116677478,1.10788542383069,3.65883368471823));
#61459=CARTESIAN_POINT('Ctrl Pts',(-1.24741775852795,1.64095230684139,3.62179646788975));
#61460=CARTESIAN_POINT('Ctrl Pts',(-0.591089924893776,1.97468687095231,
3.58475925106126));
#61461=CARTESIAN_POINT('Ctrl Pts',(0.0552900452708404,1.95641963566092,
3.54772203423278));
#61462=CARTESIAN_POINT('Ctrl Pts',(0.701670015435453,1.93815240036952,3.51068481740431));
#61463=CARTESIAN_POINT('Ctrl Pts',(1.3381021221305,1.56788336567581,3.47364760057583));
#61464=CARTESIAN_POINT('Ctrl Pts',(1.6734455320356,1.01499499073225,3.43661038374735));
#61465=CARTESIAN_POINT('Ctrl Pts',(2.0087889419407,0.462106615788698,3.39957316691887));
#61466=CARTESIAN_POINT('Ctrl Pts',(2.04304365505584,-0.273401099404705,
3.36253595009039));
#61467=CARTESIAN_POINT('Ctrl Pts',(1.76053958557416,-0.855064411333041,
3.32549873326191));
#61468=CARTESIAN_POINT('Ctrl Pts',(1.47803551609248,-1.43672772326139,3.28846151643343));
#61469=CARTESIAN_POINT('Ctrl Pts',(0.878772664013962,-1.86454663192466,
3.25142429960495));
#61470=CARTESIAN_POINT('Ctrl Pts',(0.236888497103484,-1.94281203925035,
3.21438708277648));
#61471=CARTESIAN_POINT('Ctrl Pts',(-0.404995669806982,-2.02107744657604,
3.177349865948));
#61472=CARTESIAN_POINT('Ctrl Pts',(-1.08950115154941,-1.74978935256416,
3.14031264911952));
#61473=CARTESIAN_POINT('Ctrl Pts',(-1.50349557427203,-1.25305061271667,
3.10327543229104));
#61474=CARTESIAN_POINT('Ctrl Pts',(-1.79190407667273,-0.906998424134863,
3.0774735189021));
#61475=CARTESIAN_POINT('Ctrl Pts',(-1.94902846959061,-0.451530792879088,
3.05167160551317));
#61476=CARTESIAN_POINT('Ctrl Pts',(-1.95267691385146,0.00165493661177622,
3.02586969212423));
#61477=CARTESIAN_POINT('Ctrl Pts',(-1.95274315056508,0.00167675988910205,
2.92413030787576));
#61478=CARTESIAN_POINT('Ctrl Pts',(-1.94901804708373,-0.45438081105706,
2.95009798373097));
#61479=CARTESIAN_POINT('Ctrl Pts',(-1.78970412039892,-0.912783539307832,
2.97606565958618));
#61480=CARTESIAN_POINT('Ctrl Pts',(-1.49789482266332,-1.25975537577289,
3.00203333544139));
#61481=CARTESIAN_POINT('Ctrl Pts',(-1.08141253561316,-1.75496791736879,
3.03909547538511));
#61482=CARTESIAN_POINT('Ctrl Pts',(-0.3950348215429,-2.02319375080107,3.07615761532883));
#61483=CARTESIAN_POINT('Ctrl Pts',(0.246862437687336,-1.94157962588032,
3.11321975527255));
#61484=CARTESIAN_POINT('Ctrl Pts',(0.888759696917571,-1.85996550095957,
3.15028189521628));
#61485=CARTESIAN_POINT('Ctrl Pts',(1.48617650130778,-1.4285114176858,3.18734403516));
#61486=CARTESIAN_POINT('Ctrl Pts',(1.76548299529208,-0.84483270534745,3.22440617510372));
#61487=CARTESIAN_POINT('Ctrl Pts',(2.04478948927638,-0.261153993009101,
3.26146831504744));
#61488=CARTESIAN_POINT('Ctrl Pts',(2.00598567285476,0.474749348393822,3.29853045499116));
#61489=CARTESIAN_POINT('Ctrl Pts',(1.66684453569178,1.02581762536563,3.33559259493488));
#61490=CARTESIAN_POINT('Ctrl Pts',(1.3277033985288,1.57688590233743,3.3726547348786));
#61491=CARTESIAN_POINT('Ctrl Pts',(0.688224940624468,1.94311911487812,3.40971687482232));
#61492=CARTESIAN_POINT('Ctrl Pts',(0.0413041672205065,1.95677450731496,
3.44677901476604));
#61493=CARTESIAN_POINT('Ctrl Pts',(-0.605616606183457,1.9704298997518,3.48384115470976));
#61494=CARTESIAN_POINT('Ctrl Pts',(-1.25997969508704,1.63150747208479,3.52090329465349));
#61495=CARTESIAN_POINT('Ctrl Pts',(-1.62207261036362,1.09524104808107,3.55796543459721));
#61496=CARTESIAN_POINT('Ctrl Pts',(-1.83754705311226,0.776119342016343,
3.58002039235672));
#61497=CARTESIAN_POINT('Ctrl Pts',(-1.94952253842872,0.387114015523011,
3.60207535011624));
#61498=CARTESIAN_POINT('Ctrl Pts',(-1.95125983814034,-0.000967513988672578,
3.62413030787576));
#61499=CARTESIAN_POINT('Origin',(0.,0.,0.));
#61500=CARTESIAN_POINT('',(-1.95645574651684,-0.00107576288577632,4.42586969212423));
#61501=CARTESIAN_POINT('',(-1.95628130950281,-0.00119277919923279,4.32413030787576));
#61502=CARTESIAN_POINT('',(-1.954,-2.39295984553393E-16,0.));
#61503=CARTESIAN_POINT('Ctrl Pts',(-1.95645574651684,-0.00107576288577632,
4.42586969212423));
#61504=CARTESIAN_POINT('Ctrl Pts',(-1.95258201164419,0.583617837825317,
4.39241432395977));
#61505=CARTESIAN_POINT('Ctrl Pts',(-1.67312331125722,1.17152394520949,4.35895895579531));
#61506=CARTESIAN_POINT('Ctrl Pts',(-1.21525966387556,1.53420296221226,4.32550358763085));
#61507=CARTESIAN_POINT('Ctrl Pts',(-0.70837553387317,1.93571166257503,4.28846637080237));
#61508=CARTESIAN_POINT('Ctrl Pts',(0.0171598407939347,2.06118438706562,
4.25142915397389));
#61509=CARTESIAN_POINT('Ctrl Pts',(0.629444641593513,1.8532226587955,4.21439193714541));
#61510=CARTESIAN_POINT('Ctrl Pts',(1.24172944239309,1.64526093052537,4.17735472031693));
#61511=CARTESIAN_POINT('Ctrl Pts',(1.74076366932515,1.10386474949453,4.14031750348845));
#61512=CARTESIAN_POINT('Ctrl Pts',(1.89826022128925,0.476700023258525,4.10328028665997));
#61513=CARTESIAN_POINT('Ctrl Pts',(2.05575677325334,-0.150464702977478,
4.06624306983149));
#61514=CARTESIAN_POINT('Ctrl Pts',(1.87171565024948,-0.86339797441863,4.02920585300301));
#61515=CARTESIAN_POINT('Ctrl Pts',(1.43032790007833,-1.33596290298842,3.99216863617453));
#61516=CARTESIAN_POINT('Ctrl Pts',(0.988940149907184,-1.80852783155821,
3.95513141934605));
#61517=CARTESIAN_POINT('Ctrl Pts',(0.290205772568748,-2.04072441725662,
3.91809420251758));
#61518=CARTESIAN_POINT('Ctrl Pts',(-0.346233738762281,-1.92633252011348,
3.8810569856891));
#61519=CARTESIAN_POINT('Ctrl Pts',(-0.982673250093302,-1.81194062297035,
3.84401976886062));
#61520=CARTESIAN_POINT('Ctrl Pts',(-1.55681789541692,-1.35096024298568,
3.80698255203214));
#61521=CARTESIAN_POINT('Ctrl Pts',(-1.806020726649,-0.754270452038098,3.76994533520366));
#61522=CARTESIAN_POINT('Ctrl Pts',(-1.90487422217158,-0.517576224744695,
3.75525345417718));
#61523=CARTESIAN_POINT('Ctrl Pts',(-1.9525967846073,-0.259527562563923,
3.74056157315071));
#61524=CARTESIAN_POINT('Ctrl Pts',(-1.95135107115213,-0.00103745302926256,
3.72586969212423));
#61525=CARTESIAN_POINT('Ctrl Pts',(-1.95125983814034,-0.000967513988672578,
3.62413030787576));
#61526=CARTESIAN_POINT('Ctrl Pts',(-1.95244197476311,-0.265035587897937,
3.63913749005996));
#61527=CARTESIAN_POINT('Ctrl Pts',(-1.90258326051973,-0.528675939020291,
3.65414467224416));
#61528=CARTESIAN_POINT('Ctrl Pts',(-1.799560505048,-0.769580726996389,3.66915185442837));
#61529=CARTESIAN_POINT('Ctrl Pts',(-1.54513274280624,-1.36452565772967,
3.70621399437209));
#61530=CARTESIAN_POINT('Ctrl Pts',(-0.966454476673152,-1.8208050988558,
3.74327613431581));
#61531=CARTESIAN_POINT('Ctrl Pts',(-0.328572905191125,-1.92943316874967,
3.78033827425953));
#61532=CARTESIAN_POINT('Ctrl Pts',(0.309308666290907,-2.03806123864353,
3.81740041420325));
#61533=CARTESIAN_POINT('Ctrl Pts',(1.00639354312189,-1.79903793730513,3.85446255414697));
#61534=CARTESIAN_POINT('Ctrl Pts',(1.44340173058911,-1.32184112162819,3.89152469409069));
#61535=CARTESIAN_POINT('Ctrl Pts',(1.88040991805633,-0.844644305951239,
3.92858683403441));
#61536=CARTESIAN_POINT('Ctrl Pts',(2.05734141615979,-0.129273975935752,
3.96564897397814));
#61537=CARTESIAN_POINT('Ctrl Pts',(1.89315776078089,0.496614739501458,4.00271111392186));
#61538=CARTESIAN_POINT('Ctrl Pts',(1.72897410540198,1.12250345493866,4.03977325386558));
#61539=CARTESIAN_POINT('Ctrl Pts',(1.22367529654071,1.65891055579759,4.0768353938093));
#61540=CARTESIAN_POINT('Ctrl Pts',(0.608699149567017,1.86014995417357,4.11389753375302));
#61541=CARTESIAN_POINT('Ctrl Pts',(-0.00627699740667481,2.06138935254956,
4.15095967369674));
#61542=CARTESIAN_POINT('Ctrl Pts',(-0.730930482492791,1.9274610484426,4.18802181364046));
#61543=CARTESIAN_POINT('Ctrl Pts',(-1.23335429038162,1.51970711029871,4.22508395358418));
#61544=CARTESIAN_POINT('Ctrl Pts',(-1.68092015819396,1.15647443240051,4.25809940501471));
#61545=CARTESIAN_POINT('Ctrl Pts',(-1.95213599025838,0.575947822566119,
4.29111485644523));
#61546=CARTESIAN_POINT('Ctrl Pts',(-1.95628130950281,-0.00119277919923279,
4.32413030787576));
#61547=CARTESIAN_POINT('Origin',(0.,0.,0.));
#61548=CARTESIAN_POINT('',(-1.95458266482996,0.00173443779922018,5.12586969212423));
#61549=CARTESIAN_POINT('',(-1.95491180920002,0.00168629508682236,5.02413030787576));
#61550=CARTESIAN_POINT('',(-1.954,-2.39295984553393E-16,0.));
#61551=CARTESIAN_POINT('Ctrl Pts',(-1.95458266482996,0.00173443779922018,
5.12586969212423));
#61552=CARTESIAN_POINT('Ctrl Pts',(-1.95579683437623,0.13363129532035,5.11834150842579));
#61553=CARTESIAN_POINT('Ctrl Pts',(-1.94358523444966,0.265304620125551,
5.11081332472735));
#61554=CARTESIAN_POINT('Ctrl Pts',(-1.91712292268468,0.394048828472761,
5.10328514102891));
#61555=CARTESIAN_POINT('Ctrl Pts',(-1.78693343503641,1.0274455880328,5.06624792420043));
#61556=CARTESIAN_POINT('Ctrl Pts',(-1.31181246839585,1.58994452273665,5.02921070737195));
#61557=CARTESIAN_POINT('Ctrl Pts',(-0.709107816346671,1.8242261056952,4.99217349054347));
#61558=CARTESIAN_POINT('Ctrl Pts',(-0.106403164297495,2.05850768865374,
4.95513627371499));
#61559=CARTESIAN_POINT('Ctrl Pts',(0.623885173160298,1.96457191986698,4.91809905688651));
#61560=CARTESIAN_POINT('Ctrl Pts',(1.14768109757825,1.58539044975217,4.88106184005803));
#61561=CARTESIAN_POINT('Ctrl Pts',(1.67147702199619,1.20620897963737,4.84402462322955));
#61562=CARTESIAN_POINT('Ctrl Pts',(1.9887805333743,0.541781808194522,4.80698740640107));
#61563=CARTESIAN_POINT('Ctrl Pts',(1.95443866449662,-0.103943670439598,
4.76995018957259));
#61564=CARTESIAN_POINT('Ctrl Pts',(1.92009679561895,-0.749669149073727,
4.73291297274411));
#61565=CARTESIAN_POINT('Ctrl Pts',(1.53410954648549,-1.37669293489913,4.69587575591563));
#61566=CARTESIAN_POINT('Ctrl Pts',(0.973049796091196,-1.69817810439032,
4.65883853908716));
#61567=CARTESIAN_POINT('Ctrl Pts',(0.411990045696909,-2.0196632738815,4.62180132225868));
#61568=CARTESIAN_POINT('Ctrl Pts',(-0.324142205958206,-2.03560982703848,
4.5847641054302));
#61569=CARTESIAN_POINT('Ctrl Pts',(-0.898597516275757,-1.7387228886878,
4.54772688860172));
#61570=CARTESIAN_POINT('Ctrl Pts',(-1.47305282659331,-1.44183595033712,
4.51068967177324));
#61571=CARTESIAN_POINT('Ctrl Pts',(-1.8858311955733,-0.832115520478776,
4.47365245494476));
#61572=CARTESIAN_POINT('Ctrl Pts',(-1.94810393739446,-0.188482967432129,
4.43661523811628));
#61573=CARTESIAN_POINT('Ctrl Pts',(-1.9541262996613,-0.126237620787308,
4.43303338945226));
#61574=CARTESIAN_POINT('Ctrl Pts',(-1.95687048211354,-0.0636751036633503,
4.42945154078825));
#61575=CARTESIAN_POINT('Ctrl Pts',(-1.95645574651684,-0.00107576288577632,
4.42586969212423));
#61576=CARTESIAN_POINT('Ctrl Pts',(-1.95628130950281,-0.00119277919923279,
4.32413030787576));
#61577=CARTESIAN_POINT('Ctrl Pts',(-1.95678939935296,-0.0719326340995119,
4.32817699638895));
#61578=CARTESIAN_POINT('Ctrl Pts',(-1.95328521122814,-0.14262162001596,
4.33222368490215));
#61579=CARTESIAN_POINT('Ctrl Pts',(-1.94560169264522,-0.212853377401693,
4.33627037341534));
#61580=CARTESIAN_POINT('Ctrl Pts',(-1.87523115632842,-0.856080354777335,
4.37333251335906));
#61581=CARTESIAN_POINT('Ctrl Pts',(-1.45429595300328,-1.46095473734778,
4.41039465330279));
#61582=CARTESIAN_POINT('Ctrl Pts',(-0.875593536694013,-1.75043093699665,
4.44745679324651));
#61583=CARTESIAN_POINT('Ctrl Pts',(-0.296891120384743,-2.03990713664554,
4.48451893319023));
#61584=CARTESIAN_POINT('Ctrl Pts',(0.439578508908652,-2.01398515337285,
4.52158107313395));
#61585=CARTESIAN_POINT('Ctrl Pts',(0.9964962855145,-1.68453781781564,4.55864321307767));
#61586=CARTESIAN_POINT('Ctrl Pts',(1.55341406212034,-1.35509048225843,4.59570535302139));
#61587=CARTESIAN_POINT('Ctrl Pts',(1.93077998603865,-0.72211779441669,4.63276749296511));
#61588=CARTESIAN_POINT('Ctrl Pts',(1.95575227831571,-0.0755349757277263,
4.66982963290883));
#61589=CARTESIAN_POINT('Ctrl Pts',(1.98072457059277,0.571047842961237,4.70689177285256));
#61590=CARTESIAN_POINT('Ctrl Pts',(1.6533032312286,1.23124079249743,4.74395391279628));
#61591=CARTESIAN_POINT('Ctrl Pts',(1.12345433605614,1.60266118112717,4.78101605273999));
#61592=CARTESIAN_POINT('Ctrl Pts',(0.59360544088369,1.97408156975691,4.81807819268371));
#61593=CARTESIAN_POINT('Ctrl Pts',(-0.138671010097046,2.05672939748021,
4.85514033262744));
#61594=CARTESIAN_POINT('Ctrl Pts',(-0.737976517839776,1.81275016640803,
4.89220247257116));
#61595=CARTESIAN_POINT('Ctrl Pts',(-1.33728202558251,1.56877093533586,4.92926461251488));
#61596=CARTESIAN_POINT('Ctrl Pts',(-1.80361659008724,0.998164645468222,
4.9663267524586));
#61597=CARTESIAN_POINT('Ctrl Pts',(-1.92338886510923,0.362281355122108,
5.00338889240232));
#61598=CARTESIAN_POINT('Ctrl Pts',(-1.94573194011967,0.243659678682544,
5.01030269756014));
#61599=CARTESIAN_POINT('Ctrl Pts',(-1.95601481281436,0.122766393772507,
5.01721650271795));
#61600=CARTESIAN_POINT('Ctrl Pts',(-1.95491180920002,0.00168629508682236,
5.02413030787576));
#61601=CARTESIAN_POINT('Origin',(0.,0.,0.));
#61602=CARTESIAN_POINT('',(-1.9507978584999,-3.45334863967226E-5,5.82586969212423));
#61603=CARTESIAN_POINT('',(-1.95080468396925,0.00018981806121043,5.72413030787576));
#61604=CARTESIAN_POINT('',(-1.954,-2.39295984553393E-16,0.));
#61605=CARTESIAN_POINT('Ctrl Pts',(-1.95079815420139,-3.45302974047446E-5,
5.82586969212423));
#61606=CARTESIAN_POINT('Ctrl Pts',(-1.95074640707532,0.328120037045956,
5.80723147606333));
#61607=CARTESIAN_POINT('Ctrl Pts',(-1.87237758907749,0.656297824114404,
5.78859326000243));
#61608=CARTESIAN_POINT('Ctrl Pts',(-1.715829951129,0.941574404236039,5.76995504394152));
#61609=CARTESIAN_POINT('Ctrl Pts',(-1.4047439120071,1.50846613462089,5.73291782711304));
#61610=CARTESIAN_POINT('Ctrl Pts',(-0.784943311216198,1.90594846094957,
5.69588061028457));
#61611=CARTESIAN_POINT('Ctrl Pts',(-0.139960769924853,1.95218999146749,
5.65884339345609));
#61612=CARTESIAN_POINT('Ctrl Pts',(0.505021771366483,1.99843152198542,5.62180617662761));
#61613=CARTESIAN_POINT('Ctrl Pts',(1.17518625315826,1.69343225669258,5.58476895979913));
#61614=CARTESIAN_POINT('Ctrl Pts',(1.56396070392606,1.17671648942254,5.54773174297065));
#61615=CARTESIAN_POINT('Ctrl Pts',(1.95273515469386,0.660000722152496,5.51069452614217));
#61616=CARTESIAN_POINT('Ctrl Pts',(2.06011957443768,-0.0684315470947738,
5.47365730931369));
#61617=CARTESIAN_POINT('Ctrl Pts',(1.83699012241942,-0.675353292756691,
5.43662009248521));
#61618=CARTESIAN_POINT('Ctrl Pts',(1.61386067040115,-1.28227503841861,5.39958287565673));
#61619=CARTESIAN_POINT('Ctrl Pts',(1.06021734662079,-1.76768626049519,5.36254565882826));
#61620=CARTESIAN_POINT('Ctrl Pts',(0.429328609649713,-1.90953180775813,
5.32550844199978));
#61621=CARTESIAN_POINT('Ctrl Pts',(-0.201560127321352,-2.05137735502108,
5.2884712251713));
#61622=CARTESIAN_POINT('Ctrl Pts',(-0.909694277483132,-1.84965722747041,
5.25143400834282));
#61623=CARTESIAN_POINT('Ctrl Pts',(-1.37113234823603,-1.39664987148696,
5.21439679151434));
#61624=CARTESIAN_POINT('Ctrl Pts',(-1.73877852911313,-1.03572077852157,
5.1848877583843));
#61625=CARTESIAN_POINT('Ctrl Pts',(-1.94982335358017,-0.515275892214865,
5.15537872525427));
#61626=CARTESIAN_POINT('Ctrl Pts',(-1.95458266482996,0.00173443779922018,
5.12586969212423));
#61627=CARTESIAN_POINT('Ctrl Pts',(-1.95491180920002,0.00168629508682236,
5.02413030787576));
#61628=CARTESIAN_POINT('Ctrl Pts',(-1.95010205227512,-0.526295513449078,
5.05427864266167));
#61629=CARTESIAN_POINT('Ctrl Pts',(-1.72879182329996,-1.05782955367232,
5.08442697744757));
#61630=CARTESIAN_POINT('Ctrl Pts',(-1.34689356786549,-1.42005289462677,
5.11457531223348));
#61631=CARTESIAN_POINT('Ctrl Pts',(-0.877416010060499,-1.86534356320495,
5.1516374521772));
#61632=CARTESIAN_POINT('Ctrl Pts',(-0.165250908911267,-2.05476460953673,
5.18869959212092));
#61633=CARTESIAN_POINT('Ctrl Pts',(0.463414671012952,-1.90155708549211,
5.22576173206464));
#61634=CARTESIAN_POINT('Ctrl Pts',(1.09208025093718,-1.74834956144749,5.26282387200837));
#61635=CARTESIAN_POINT('Ctrl Pts',(1.63724630963639,-1.25251346702646,5.29988601195209));
#61636=CARTESIAN_POINT('Ctrl Pts',(1.84921496651671,-0.641152489120857,
5.33694815189581));
#61637=CARTESIAN_POINT('Ctrl Pts',(2.06118362339704,-0.0297915112152539,
5.37401029183953));
#61638=CARTESIAN_POINT('Ctrl Pts',(1.93995487845847,0.697094350174917,5.41107243178325));
#61639=CARTESIAN_POINT('Ctrl Pts',(1.54105412656959,1.20657560296821,5.44813457172697));
#61640=CARTESIAN_POINT('Ctrl Pts',(1.14215337468071,1.71605685576151,5.48519671167069));
#61641=CARTESIAN_POINT('Ctrl Pts',(0.465580615841514,2.00813349995792,5.52225885161441));
#61642=CARTESIAN_POINT('Ctrl Pts',(-0.178779150223708,1.94902809680635,
5.55932099155813));
#61643=CARTESIAN_POINT('Ctrl Pts',(-0.823138916288934,1.88992269365477,
5.59638313150186));
#61644=CARTESIAN_POINT('Ctrl Pts',(-1.43528568958019,1.4796352431552,5.63344527144558));
#61645=CARTESIAN_POINT('Ctrl Pts',(-1.73484296927877,0.906086297567352,
5.6705074113893));
#61646=CARTESIAN_POINT('Ctrl Pts',(-1.87931321146693,0.629475576708828,
5.68838171021812));
#61647=CARTESIAN_POINT('Ctrl Pts',(-1.95107725773013,0.31489133949035,5.70625600904694));
#61648=CARTESIAN_POINT('Ctrl Pts',(-1.95080468396925,0.00018981806121043,
5.72413030787576));
#61649=CARTESIAN_POINT('Origin',(0.,0.,0.));
#61650=CARTESIAN_POINT('',(-1.95470932084261,-0.00171584046685047,6.52586969212424));
#61651=CARTESIAN_POINT('',(-1.95421427783755,-0.00177812761388513,6.42413030787576));
#61652=CARTESIAN_POINT('',(-1.954,-2.39295984553393E-16,0.));
#61653=CARTESIAN_POINT('Ctrl Pts',(-1.95470932084261,-0.00171584046685047,
6.52586969212424));
#61654=CARTESIAN_POINT('Ctrl Pts',(-1.94992946923152,0.519398730151351,
6.49612144370087));
#61655=CARTESIAN_POINT('Ctrl Pts',(-1.73506994162404,1.04399306729571,6.46637319527751));
#61656=CARTESIAN_POINT('Ctrl Pts',(-1.36210733975536,1.40545308526766,6.43662494685414));
#61657=CARTESIAN_POINT('Ctrl Pts',(-0.897760782010601,1.85547867567989,
6.39958773002566));
#61658=CARTESIAN_POINT('Ctrl Pts',(-0.188341937200331,2.05263315093338,
6.36255051319719));
#61659=CARTESIAN_POINT('Ctrl Pts',(0.441620008484366,1.90672665791667,6.32551329636871));
#61660=CARTESIAN_POINT('Ctrl Pts',(1.07158195416906,1.76082016489995,6.28847607954023));
#61661=CARTESIAN_POINT('Ctrl Pts',(1.62208700072817,1.27185270361303,6.25143886271175));
#61662=CARTESIAN_POINT('Ctrl Pts',(1.84130231899333,0.663506254660481,6.21440164588327));
#61663=CARTESIAN_POINT('Ctrl Pts',(2.0605176372585,0.0551598057079281,6.17736442905479));
#61664=CARTESIAN_POINT('Ctrl Pts',(1.94844322722972,-0.672565630910262,
6.14032721222632));
#61665=CARTESIAN_POINT('Ctrl Pts',(1.55634840229719,-1.18676637573315,6.10328999539784));
#61666=CARTESIAN_POINT('Ctrl Pts',(1.16425357736466,-1.70096712055603,6.06625277856936));
#61667=CARTESIAN_POINT('Ctrl Pts',(0.492138337528384,-2.00164317358361,
6.02921556174087));
#61668=CARTESIAN_POINT('Ctrl Pts',(-0.152532956197894,-1.95124792816734,
5.9921783449124));
#61669=CARTESIAN_POINT('Ctrl Pts',(-0.797204249924167,-1.90085268275106,
5.95514112808392));
#61670=CARTESIAN_POINT('Ctrl Pts',(-1.41443159754043,-1.49938613889095,
5.91810391125544));
#61671=CARTESIAN_POINT('Ctrl Pts',(-1.72185953262212,-0.930502299740384,
5.88106669442696));
#61672=CARTESIAN_POINT('Ctrl Pts',(-1.87458069522289,-0.647897528391999,
5.86266769365939));
#61673=CARTESIAN_POINT('Ctrl Pts',(-1.95084923717034,-0.323977343102287,
5.84426869289181));
#61674=CARTESIAN_POINT('Ctrl Pts',(-1.95079815420139,-3.45302974047446E-5,
5.82586969212423));
#61675=CARTESIAN_POINT('Ctrl Pts',(-1.95080468396925,0.00018981806121043,
5.72413030787576));
#61676=CARTESIAN_POINT('Ctrl Pts',(-1.95051207937167,-0.337638415069996,
5.74331814899066));
#61677=CARTESIAN_POINT('Ctrl Pts',(-1.86720620393942,-0.675601803708791,
5.76250599010555));
#61678=CARTESIAN_POINT('Ctrl Pts',(-1.70171536425399,-0.966869859783203,
5.78169383122045));
#61679=CARTESIAN_POINT('Ctrl Pts',(-1.38206269342473,-1.5294666308698,5.81875597116418));
#61680=CARTESIAN_POINT('Ctrl Pts',(-0.755789565660301,-1.91784973236686,
5.85581811110791));
#61681=CARTESIAN_POINT('Ctrl Pts',(-0.109742658556152,-1.95413127900566,
5.89288025105163));
#61682=CARTESIAN_POINT('Ctrl Pts',(0.536304248547996,-1.99041282564447,
5.92994239099535));
#61683=CARTESIAN_POINT('Ctrl Pts',(1.20212493499187,-1.674592817425,5.96700453093906));
#61684=CARTESIAN_POINT('Ctrl Pts',(1.58275908344154,-1.15132366886058,6.00406667088278));
#61685=CARTESIAN_POINT('Ctrl Pts',(1.9633932318912,-0.628054520296152,6.0411288108265));
#61686=CARTESIAN_POINT('Ctrl Pts',(2.05884084234667,0.102663768613233,6.07819095077022));
#61687=CARTESIAN_POINT('Ctrl Pts',(1.82538483877546,0.706146370849535,6.11525309071394));
#61688=CARTESIAN_POINT('Ctrl Pts',(1.59192883520425,1.30962897308584,6.15231523065767));
#61689=CARTESIAN_POINT('Ctrl Pts',(1.02956921760636,1.78587588864905,6.18937737060139));
#61690=CARTESIAN_POINT('Ctrl Pts',(0.395878889512919,1.91675569949154,6.22643951054511));
#61691=CARTESIAN_POINT('Ctrl Pts',(-0.237811438580523,2.04763551033402,
6.26350165048883));
#61692=CARTESIAN_POINT('Ctrl Pts',(-0.942832477169518,1.83314821645578,
6.30056379043255));
#61693=CARTESIAN_POINT('Ctrl Pts',(-1.39626929730598,1.37153365109863,6.33762593037627));
#61694=CARTESIAN_POINT('Ctrl Pts',(-1.7490486198241,1.01239194403086,6.3664607228761));
#61695=CARTESIAN_POINT('Ctrl Pts',(-1.94954331224527,0.503663409317413,
6.39529551537593));
#61696=CARTESIAN_POINT('Ctrl Pts',(-1.95421427783755,-0.00177812761388513,
6.42413030787576));
#61697=CARTESIAN_POINT('Origin',(0.,0.,0.));
#61698=CARTESIAN_POINT('',(-1.95636369417486,0.00113518110994186,7.22586969212423));
#61699=CARTESIAN_POINT('',(-1.95675615924934,0.000851174274233985,7.12413030787576));
#61700=CARTESIAN_POINT('',(-1.954,-2.39295984553393E-16,0.));
#61701=CARTESIAN_POINT('Ctrl Pts',(-1.95636369417486,0.00113518110994186,
7.22586969212423));
#61702=CARTESIAN_POINT('Ctrl Pts',(-1.95682546989371,0.0679235189129894,
7.22204862816689));
#61703=CARTESIAN_POINT('Ctrl Pts',(-1.95370156992351,0.134668159558925,
7.21822756420955));
#61704=CARTESIAN_POINT('Ctrl Pts',(-1.94684940168549,0.201027826582277,
7.2144065002522));
#61705=CARTESIAN_POINT('Ctrl Pts',(-1.88043197355288,0.844245894546327,
7.17736928342373));
#61706=CARTESIAN_POINT('Ctrl Pts',(-1.46373463610807,1.45129475044757,7.14033206659525));
#61707=CARTESIAN_POINT('Ctrl Pts',(-0.887378837876281,1.74447515831938,
7.10329484976677));
#61708=CARTESIAN_POINT('Ctrl Pts',(-0.31102303964449,2.03765556619118,7.06625763293829));
#61709=CARTESIAN_POINT('Ctrl Pts',(0.424991219374283,2.01696752603353,7.02922041610981));
#61710=CARTESIAN_POINT('Ctrl Pts',(0.983968473233738,1.69187494324663,6.99218319928133));
#61711=CARTESIAN_POINT('Ctrl Pts',(1.54294572709319,1.36678236045973,6.95514598245285));
#61712=CARTESIAN_POINT('Ctrl Pts',(1.92488597579333,0.737285235043576,6.91810876562437));
#61713=CARTESIAN_POINT('Ctrl Pts',(1.95506767226643,0.0913519390189264,
6.8810715487959));
#61714=CARTESIAN_POINT('Ctrl Pts',(1.98524936873952,-0.554581357005719,
6.84403433196742));
#61715=CARTESIAN_POINT('Ctrl Pts',(1.66367251298559,-1.21695082363886,6.80699711513894));
#61716=CARTESIAN_POINT('Ctrl Pts',(1.13744494695038,-1.59275037986524,6.76995989831046));
#61717=CARTESIAN_POINT('Ctrl Pts',(0.611217380915185,-1.96854993609162,
6.73292268148198));
#61718=CARTESIAN_POINT('Ctrl Pts',(-0.119660895401274,-2.05777958191125,
6.69588546465349));
#61719=CARTESIAN_POINT('Ctrl Pts',(-0.72084391141631,-1.81962051958034,
6.65884824782502));
#61720=CARTESIAN_POINT('Ctrl Pts',(-1.32202692743135,-1.58146145724943,
6.62181103099654));
#61721=CARTESIAN_POINT('Ctrl Pts',(-1.79351468314497,-1.01591368676797,
6.58477381416807));
#61722=CARTESIAN_POINT('Ctrl Pts',(-1.91962142566216,-0.381691448741754,
6.54773659733959));
#61723=CARTESIAN_POINT('Ctrl Pts',(-1.9444393828574,-0.256875756563692,
6.54044762893447));
#61724=CARTESIAN_POINT('Ctrl Pts',(-1.95588048853217,-0.129400253566584,
6.53315866052935));
#61725=CARTESIAN_POINT('Ctrl Pts',(-1.95470932084261,-0.00171584046685047,
6.52586969212424));
#61726=CARTESIAN_POINT('Ctrl Pts',(-1.95421427783755,-0.00177812761388513,
6.42413030787576));
#61727=CARTESIAN_POINT('Ctrl Pts',(-1.95554703085897,-0.145994290672205,
6.43235765531965));
#61728=CARTESIAN_POINT('Ctrl Pts',(-1.94093747105224,-0.289942854151266,
6.44058500276354));
#61729=CARTESIAN_POINT('Ctrl Pts',(-1.90937423221194,-0.430072724152966,
6.44881235020743));
#61730=CARTESIAN_POINT('Ctrl Pts',(-1.7671897452975,-1.06132269721135,6.48587449015115));
#61731=CARTESIAN_POINT('Ctrl Pts',(-1.28096816978468,-1.61508080649208,
6.52293663009487));
#61732=CARTESIAN_POINT('Ctrl Pts',(-0.67340953434779,-1.83771382585667,
6.55999877003859));
#61733=CARTESIAN_POINT('Ctrl Pts',(-0.0658508989108841,-2.06034684522128,
6.59706090998232));
#61734=CARTESIAN_POINT('Ctrl Pts',(0.663044796450101,-1.95185477466974,
6.63412304992604));
#61735=CARTESIAN_POINT('Ctrl Pts',(1.17942751209788,-1.56192933591821,6.67118518986976));
#61736=CARTESIAN_POINT('Ctrl Pts',(1.69581022774564,-1.17200389716668,6.70824732981348));
#61737=CARTESIAN_POINT('Ctrl Pts',(1.9996799636802,-0.500645090215166,6.7453094697572));
#61738=CARTESIAN_POINT('Ctrl Pts',(1.95185778931935,0.144650188277344,6.78237160970092));
#61739=CARTESIAN_POINT('Ctrl Pts',(1.90403561495849,0.789945466769872,6.81943374964464));
#61740=CARTESIAN_POINT('Ctrl Pts',(1.5045215303022,1.4091772168034,6.85649588958836));
#61741=CARTESIAN_POINT('Ctrl Pts',(0.936301652358751,1.71872386452436,6.89355802953208));
#61742=CARTESIAN_POINT('Ctrl Pts',(0.368081774415317,2.02827051224532,6.9306201694758));
#61743=CARTESIAN_POINT('Ctrl Pts',(-0.368843896815252,2.02813205765373,
6.96768230941953));
#61744=CARTESIAN_POINT('Ctrl Pts',(-0.936947418561655,1.71837191595589,
7.00474444936325));
#61745=CARTESIAN_POINT('Ctrl Pts',(-1.50505094030807,1.40861177425805,7.04180658930697));
#61746=CARTESIAN_POINT('Ctrl Pts',(-1.90433231257031,0.78922994545395,7.07886872925069));
#61747=CARTESIAN_POINT('Ctrl Pts',(-1.95191200566454,0.143916742729559,
7.11593086919441));
#61748=CARTESIAN_POINT('Ctrl Pts',(-1.95542076848464,0.0963281429343837,
7.11866401542153));
#61749=CARTESIAN_POINT('Ctrl Pts',(-1.95701686505733,0.0485985200318871,
7.12139716164864));
#61750=CARTESIAN_POINT('Ctrl Pts',(-1.95675615924934,0.000851174274233985,
7.12413030787576));
#61751=CARTESIAN_POINT('Origin',(0.,0.,0.));
#61752=CARTESIAN_POINT('',(-1.95128545551857,0.000980157954364874,7.92586969212424));
#61753=CARTESIAN_POINT('',(-1.95166123101285,0.00126544742759004,7.82413030787576));
#61754=CARTESIAN_POINT('',(-1.954,-2.39295984553393E-16,0.));
#61755=CARTESIAN_POINT('Ctrl Pts',(-1.95128545551857,0.000980157954364874,
7.92586969212424));
#61756=CARTESIAN_POINT('Ctrl Pts',(-1.95247914943593,0.263701155015296,
7.91093859580443));
#61757=CARTESIAN_POINT('Ctrl Pts',(-1.90313505751618,0.525992349613935,
7.89600749948463));
#61758=CARTESIAN_POINT('Ctrl Pts',(-1.80112460177197,0.765888339627252,
7.88107640316483));
#61759=CARTESIAN_POINT('Ctrl Pts',(-1.54808334564134,1.36096050365993,7.84403918633635));
#61760=CARTESIAN_POINT('Ctrl Pts',(-0.970981193167941,1.81823294990903,
7.80700196950786));
#61761=CARTESIAN_POINT('Ctrl Pts',(-0.333818027149729,1.92852282969788,
7.76996475267938));
#61762=CARTESIAN_POINT('Ctrl Pts',(0.303345138868501,2.03881270948674,7.73292753585091));
#61763=CARTESIAN_POINT('Ctrl Pts',(1.00056931843154,1.80212002281537,7.69589031902244));
#61764=CARTESIAN_POINT('Ctrl Pts',(1.43890387011628,1.32672168613705,7.65885310219396));
#61765=CARTESIAN_POINT('Ctrl Pts',(1.87723842180101,0.851323349458752,7.62181588536548));
#61766=CARTESIAN_POINT('Ctrl Pts',(2.05668334560742,0.13721936277351,7.58477866853699));
#61767=CARTESIAN_POINT('Ctrl Pts',(1.8951501609247,-0.488917833023672,7.54774145170851));
#61768=CARTESIAN_POINT('Ctrl Pts',(1.73361697624198,-1.11505502882086,7.51070423488003));
#61769=CARTESIAN_POINT('Ctrl Pts',(1.23110568307013,-1.65322543373001,7.47366701805156));
#61770=CARTESIAN_POINT('Ctrl Pts',(0.61749399359133,-1.85723879665063,7.43662980122308));
#61771=CARTESIAN_POINT('Ctrl Pts',(0.00388230411252383,-2.06125215957126,
7.3995925843946));
#61772=CARTESIAN_POINT('Ctrl Pts',(-0.72082978167322,-1.93110848050335,
7.36255536756612));
#61773=CARTESIAN_POINT('Ctrl Pts',(-1.22511706515588,-1.52634300095596,
7.32551815073764));
#61774=CARTESIAN_POINT('Ctrl Pts',(-1.6773779241913,-1.16333645789233,7.2923019978665));
#61775=CARTESIAN_POINT('Ctrl Pts',(-1.95234952088687,-0.579449614967985,
7.25908584499537));
#61776=CARTESIAN_POINT('Ctrl Pts',(-1.95636369417486,0.00113518110994186,
7.22586969212423));
#61777=CARTESIAN_POINT('Ctrl Pts',(-1.95675615924934,0.000851174274233985,
7.12413030787576));
#61778=CARTESIAN_POINT('Ctrl Pts',(-1.95348162971424,-0.598867317271105,
7.15845930159236));
#61779=CARTESIAN_POINT('Ctrl Pts',(-1.65727828481393,-1.20138176331325,
7.19278829530897));
#61780=CARTESIAN_POINT('Ctrl Pts',(-1.17884051406102,-1.56237241050387,
7.22711728902557));
#61781=CARTESIAN_POINT('Ctrl Pts',(-0.662311315437018,-1.95210378436822,
7.2641794289693));
#61782=CARTESIAN_POINT('Ctrl Pts',(0.0666250957372189,-2.06032195545224,
7.30124156891302));
#61783=CARTESIAN_POINT('Ctrl Pts',(0.674100031098693,-1.83746065393738,
7.33830370885674));
#61784=CARTESIAN_POINT('Ctrl Pts',(1.28157496646017,-1.61459935242253,7.37536584880046));
#61785=CARTESIAN_POINT('Ctrl Pts',(1.76758842600887,-1.0606585783088,7.41242798874417));
#61786=CARTESIAN_POINT('Ctrl Pts',(1.9095357026966,-0.429355222190436,7.44949012868789));
#61787=CARTESIAN_POINT('Ctrl Pts',(2.05148297938434,0.201948133927931,7.48655226863161));
#61788=CARTESIAN_POINT('Ctrl Pts',(1.84936407321109,0.910614072050953,7.52361440857534));
#61789=CARTESIAN_POINT('Ctrl Pts',(1.39575382755531,1.37205822017881,7.56067654851907));
#61790=CARTESIAN_POINT('Ctrl Pts',(0.942143581899539,1.83350236830666,7.59773868846279));
#61791=CARTESIAN_POINT('Ctrl Pts',(0.237041996761252,2.04772472643938,7.6348008284065));
#61792=CARTESIAN_POINT('Ctrl Pts',(-0.396599106844383,1.91660680765389,
7.67186296835022));
#61793=CARTESIAN_POINT('Ctrl Pts',(-1.03024021045003,1.78548888886839,7.70892510829394));
#61794=CARTESIAN_POINT('Ctrl Pts',(-1.59242083252301,1.30903069316467,7.74598724823766));
#61795=CARTESIAN_POINT('Ctrl Pts',(-1.82565005336597,0.705460409477194,
7.78304938818139));
#61796=CARTESIAN_POINT('Ctrl Pts',(-1.9118230851659,0.482454556858425,7.79674302807951));
#61797=CARTESIAN_POINT('Ctrl Pts',(-1.95308968355645,0.242096139413284,
7.81043666797764));
#61798=CARTESIAN_POINT('Ctrl Pts',(-1.95166123101285,0.00126544742759004,
7.82413030787576));
#61799=CARTESIAN_POINT('Origin',(0.,0.,0.));
#61800=CARTESIAN_POINT('',(-1.95279013340439,-0.00168009551267251,8.62586969212423));
#61801=CARTESIAN_POINT('',(-1.95215444869335,-0.00150235120299324,8.52413030787576));
#61802=CARTESIAN_POINT('',(-1.954,-2.39295984553393E-16,0.));
#61803=CARTESIAN_POINT('Ctrl Pts',(-1.95279013340439,-0.00168009551267251,
8.62586969212423));
#61804=CARTESIAN_POINT('Ctrl Pts',(-1.94903607268958,0.455640131522026,
8.59982856344197));
#61805=CARTESIAN_POINT('Ctrl Pts',(-1.78871895344458,0.915331173731693,
8.57378743475971));
#61806=CARTESIAN_POINT('Ctrl Pts',(-1.49539281844263,1.26270942713959,8.54774630607745));
#61807=CARTESIAN_POINT('Ctrl Pts',(-1.07820722729247,1.75677110357261,8.51070908924897));
#61808=CARTESIAN_POINT('Ctrl Pts',(-0.391968436807465,2.02364430724413,
8.47367187242049));
#61809=CARTESIAN_POINT('Ctrl Pts',(0.24939826400162,1.94124580780539,8.43663465559201));
#61810=CARTESIAN_POINT('Ctrl Pts',(0.890764964810705,1.85884730836666,8.39959743876353));
#61811=CARTESIAN_POINT('Ctrl Pts',(1.48725957594388,1.42717710581768,8.36256022193505));
#61812=CARTESIAN_POINT('Ctrl Pts',(1.76601098282085,0.843706103134459,8.32552300510657));
#61813=CARTESIAN_POINT('Ctrl Pts',(2.04476238969783,0.260235100451228,8.28848578827809));
#61814=CARTESIAN_POINT('Ctrl Pts',(2.00577059231861,-0.475036702366233,
8.25144857144961));
#61815=CARTESIAN_POINT('Ctrl Pts',(1.66687269277466,-1.02575348200379,8.21441135462113));
#61816=CARTESIAN_POINT('Ctrl Pts',(1.32797479323072,-1.57647026164133,8.17737413779266));
#61817=CARTESIAN_POINT('Ctrl Pts',(0.689170791522051,-1.94263201809897,
8.14033692096418));
#61818=CARTESIAN_POINT('Ctrl Pts',(0.0426865627857745,-1.95673519857469,
8.1032997041357));
#61819=CARTESIAN_POINT('Ctrl Pts',(-0.60379766595052,-1.97083837905041,
8.06626248730722));
#61820=CARTESIAN_POINT('Ctrl Pts',(-1.25796212171444,-1.6328829835442,8.02922527047874));
#61821=CARTESIAN_POINT('Ctrl Pts',(-1.62055416970245,-1.09746934488294,
7.99218805365026));
#61822=CARTESIAN_POINT('Ctrl Pts',(-1.83697171385623,-0.777901098892797,
7.97008193314158));
#61823=CARTESIAN_POINT('Ctrl Pts',(-1.94951814111497,-0.387989405753114,
7.94797581263291));
#61824=CARTESIAN_POINT('Ctrl Pts',(-1.95128545551857,0.000980157954364874,
7.92586969212424));
#61825=CARTESIAN_POINT('Ctrl Pts',(-1.95166123101285,0.00126544742759004,
7.82413030787576));
#61826=CARTESIAN_POINT('Ctrl Pts',(-1.94922354508138,-0.409717467160323,
7.84749880792136));
#61827=CARTESIAN_POINT('Ctrl Pts',(-1.82244856716882,-0.822075748123473,
7.87086730796695));
#61828=CARTESIAN_POINT('Ctrl Pts',(-1.58232634722073,-1.15191832939155,
7.89423580801255));
#61829=CARTESIAN_POINT('Ctrl Pts',(-1.20149560061961,-1.67504441290151,
7.93129794795627));
#61830=CARTESIAN_POINT('Ctrl Pts',(-0.535556287804454,-1.99061420825021,
7.96836008789999));
#61831=CARTESIAN_POINT('Ctrl Pts',(0.110476940437387,-1.95408990384897,
8.00542222784371));
#61832=CARTESIAN_POINT('Ctrl Pts',(0.756510168679237,-1.91756559944773,
8.04248436778743));
#61833=CARTESIAN_POINT('Ctrl Pts',(1.38263731234777,-1.52894719529654,8.07954650773116));
#61834=CARTESIAN_POINT('Ctrl Pts',(1.70207855773424,-0.966230350379699,
8.11660864767487));
#61835=CARTESIAN_POINT('Ctrl Pts',(2.02151980312072,-0.403513505462853,
8.1536707876186));
#61836=CARTESIAN_POINT('Ctrl Pts',(2.03427515022513,0.333301780219651,8.19073292756232));
#61837=CARTESIAN_POINT('Ctrl Pts',(1.73450237337761,0.906738122863988,8.22779506750604));
#61838=CARTESIAN_POINT('Ctrl Pts',(1.43472959653009,1.48017446550833,8.26485720744976));
#61839=CARTESIAN_POINT('Ctrl Pts',(0.822428695730641,1.89023186511451,8.30191934739348));
#61840=CARTESIAN_POINT('Ctrl Pts',(0.178046765554912,1.94909513773745,8.3389814873372));
#61841=CARTESIAN_POINT('Ctrl Pts',(-0.466335164620799,2.00795841036038,
8.37604362728092));
#61842=CARTESIAN_POINT('Ctrl Pts',(-1.14279812417278,1.71562755600011,8.41310576722464));
#61843=CARTESIAN_POINT('Ctrl Pts',(-1.54150740386038,1.20599644714809,8.45016790716836));
#61844=CARTESIAN_POINT('Ctrl Pts',(-1.80673309918174,0.866984359672774,
8.47482204073749));
#61845=CARTESIAN_POINT('Ctrl Pts',(-1.94905131081074,0.431815751432988,
8.49947617430663));
#61846=CARTESIAN_POINT('Ctrl Pts',(-1.95215444869335,-0.00150235120299324,
8.52413030787576));
#61847=CARTESIAN_POINT('Origin',(0.,0.,0.));
#61848=CARTESIAN_POINT('',(-1.95719986784682,3.71606954582295E-5,9.32586969212424));
#61849=CARTESIAN_POINT('',(-1.95707453392556,-0.000466568259871601,9.22413030787576));
#61850=CARTESIAN_POINT('',(-1.954,-2.39295984553393E-16,0.));
#61851=CARTESIAN_POINT('Ctrl Pts',(-1.95719986784682,3.71606954581456E-5,
9.32586969212423));
#61852=CARTESIAN_POINT('Ctrl Pts',(-1.95720042510874,0.00202653151786848,
9.32575574790799));
#61853=CARTESIAN_POINT('Ctrl Pts',(-1.95719765412071,0.00401590074103218,
9.32564180369175));
#61854=CARTESIAN_POINT('Ctrl Pts',(-1.95719155021855,0.00600525973720184,
9.32552785947551));
#61855=CARTESIAN_POINT('Ctrl Pts',(-1.95520749560565,0.65264027922361,9.28849064264703));
#61856=CARTESIAN_POINT('Ctrl Pts',(-1.60108272580438,1.29819476052309,9.25145342581855));
#61857=CARTESIAN_POINT('Ctrl Pts',(-1.0568144211536,1.64735485073218,9.21441620899007));
#61858=CARTESIAN_POINT('Ctrl Pts',(-0.512546116502833,1.99651494094127,
9.17737899216159));
#61859=CARTESIAN_POINT('Ctrl Pts',(0.221865722997436,2.04928064005996,9.14034177533311));
#61860=CARTESIAN_POINT('Ctrl Pts',(0.810458692323854,1.78151382429043,9.10330455850463));
#61861=CARTESIAN_POINT('Ctrl Pts',(1.39905166165026,1.51374700852089,9.06626734167615));
#61862=CARTESIAN_POINT('Ctrl Pts',(1.84182576080283,0.925447677863139,9.02923012484767));
#61863=CARTESIAN_POINT('Ctrl Pts',(1.93623051178265,0.285737974246437,8.99219290801919));
#61864=CARTESIAN_POINT('Ctrl Pts',(2.03063526276248,-0.353971729370283,
8.95515569119071));
#61865=CARTESIAN_POINT('Ctrl Pts',(1.77667066556955,-1.04509180594595,8.91811847436223));
#61866=CARTESIAN_POINT('Ctrl Pts',(1.29051481285208,-1.47146399547075,8.88108125753376));
#61867=CARTESIAN_POINT('Ctrl Pts',(0.804358960134614,-1.89783618499555,
8.84404404070528));
#61868=CARTESIAN_POINT('Ctrl Pts',(0.0860118518926114,-2.05946048746948,
8.8070068238768));
#61869=CARTESIAN_POINT('Ctrl Pts',(-0.535913025040727,-1.88240059832962,
8.76996960704832));
#61870=CARTESIAN_POINT('Ctrl Pts',(-1.15783790197406,-1.70534070918976,
8.73293239021984));
#61871=CARTESIAN_POINT('Ctrl Pts',(-1.68334054759872,-1.18959662843613,
8.69589517339136));
#61872=CARTESIAN_POINT('Ctrl Pts',(-1.87202567450341,-0.571099513462055,
8.65885795656288));
#61873=CARTESIAN_POINT('Ctrl Pts',(-1.92804495632289,-0.387472087407564,
8.64786186841667));
#61874=CARTESIAN_POINT('Ctrl Pts',(-1.95437531748109,-0.194787452297348,
8.63686578027045));
#61875=CARTESIAN_POINT('Ctrl Pts',(-1.95279013340439,-0.00168009551267234,
8.62586969212424));
#61876=CARTESIAN_POINT('Ctrl Pts',(-1.95215444869335,-0.00150235120299324,
8.52413030787576));
#61877=CARTESIAN_POINT('Ctrl Pts',(-1.95371620524508,-0.21958398707372,
8.53653831425035));
#61878=CARTESIAN_POINT('Ctrl Pts',(-1.92001564940553,-0.437196901383431,
8.54894632062494));
#61879=CARTESIAN_POINT('Ctrl Pts',(-1.84897391479539,-0.641847309864828,
8.56135432699953));
#61880=CARTESIAN_POINT('Ctrl Pts',(-1.63677554621959,-1.25312859468192,
8.59841646694325));
#61881=CARTESIAN_POINT('Ctrl Pts',(-1.0914232092448,-1.74875980097234,8.63547860688697));
#61882=CARTESIAN_POINT('Ctrl Pts',(-0.462700104058479,-1.90173108515756,
8.67254074683069));
#61883=CARTESIAN_POINT('Ctrl Pts',(0.166023001127845,-2.05470236934278,
8.70960288677441));
#61884=CARTESIAN_POINT('Ctrl Pts',(0.878116874525705,-1.86501373142281,
8.74666502671813));
#61885=CARTESIAN_POINT('Ctrl Pts',(1.34742707561642,-1.41954668207959,8.78372716666185));
#61886=CARTESIAN_POINT('Ctrl Pts',(1.81673727670714,-0.974079632736377,
8.82078930660557));
#61887=CARTESIAN_POINT('Ctrl Pts',(2.04326380549072,-0.272834171969915,
8.85785144654929));
#61888=CARTESIAN_POINT('Ctrl Pts',(1.92325259761237,0.363004067433246,8.89491358649301));
#61889=CARTESIAN_POINT('Ctrl Pts',(1.80324138973402,0.998842306836407,8.93197572643673));
#61890=CARTESIAN_POINT('Ctrl Pts',(1.33669244519374,1.56927332487627,8.96903786638045));
#61891=CARTESIAN_POINT('Ctrl Pts',(0.737295301650971,1.81302734225987,9.00610000632417));
#61892=CARTESIAN_POINT('Ctrl Pts',(0.137898158108199,2.05678135964346,9.0431621462679));
#61893=CARTESIAN_POINT('Ctrl Pts',(-0.59434718443707,1.9738583763708,9.08022428621162));
#61894=CARTESIAN_POINT('Ctrl Pts',(-1.12405647662483,1.60223891616111,9.11728642615534));
#61895=CARTESIAN_POINT('Ctrl Pts',(-1.63307724594775,1.24513356361944,9.15290105339548));
#61896=CARTESIAN_POINT('Ctrl Pts',(-1.95507366281261,0.621442230158499,
9.18851568063562));
#61897=CARTESIAN_POINT('Ctrl Pts',(-1.95707453392556,-0.000466568259871601,
9.22413030787576));
#61898=CARTESIAN_POINT('Origin',(0.,0.,0.));
#61899=CARTESIAN_POINT('',(-1.95268202714777,0.00165579016441021,10.0258696921242));
#61900=CARTESIAN_POINT('',(-1.9535343393295,0.00178280253715055,9.92413030787576));
#61901=CARTESIAN_POINT('',(-1.954,-2.39295984553393E-16,0.));
#61902=CARTESIAN_POINT('Ctrl Pts',(-1.95268202714777,0.00165579016441021,
10.0258696921242));
#61903=CARTESIAN_POINT('Ctrl Pts',(-1.9542709496717,0.198793394721131,10.0146457155455));
#61904=CARTESIAN_POINT('Ctrl Pts',(-1.92681564478375,0.395498739780043,
10.0034217389668));
#61905=CARTESIAN_POINT('Ctrl Pts',(-1.86848643290836,0.582577638715851,
9.99219776238813));
#61906=CARTESIAN_POINT('Ctrl Pts',(-1.67600993827966,1.1999062383733,9.95516054555966));
#61907=CARTESIAN_POINT('Ctrl Pts',(-1.14735119634562,1.71241362792136,9.91812332873117));
#61908=CARTESIAN_POINT('Ctrl Pts',(-0.524351231736321,1.8856531990772,9.88108611190269));
#61909=CARTESIAN_POINT('Ctrl Pts',(0.0986487328729629,2.05889277023303,
9.84404889507421));
#61910=CARTESIAN_POINT('Ctrl Pts',(0.815989920157508,1.89286452299667,9.80701167824573));
#61911=CARTESIAN_POINT('Ctrl Pts',(1.29952003507049,1.46351732792493,9.76997446141725));
#61912=CARTESIAN_POINT('Ctrl Pts',(1.78305014998348,1.03417013285319,9.73293724458878));
#61913=CARTESIAN_POINT('Ctrl Pts',(2.0327691925249,0.341503989946047,9.69590002776029));
#61914=CARTESIAN_POINT('Ctrl Pts',(1.9344406978275,-0.297614493697593,9.65886281093182));
#61915=CARTESIAN_POINT('Ctrl Pts',(1.8361122031301,-0.936732977341234,9.62182559410334));
#61916=CARTESIAN_POINT('Ctrl Pts',(1.38973617119388,-1.52230380172138,9.58478837727486));
#61917=CARTESIAN_POINT('Ctrl Pts',(0.799511084736072,-1.78645358874384,
9.54775116044638));
#61918=CARTESIAN_POINT('Ctrl Pts',(0.209285998278261,-2.0506033757663,9.5107139436179));
#61919=CARTESIAN_POINT('Ctrl Pts',(-0.524788142701144,-1.99333212543108,
9.47367672678942));
#61920=CARTESIAN_POINT('Ctrl Pts',(-1.06690354347858,-1.6408387214268,9.43663950996094));
#61921=CARTESIAN_POINT('Ctrl Pts',(-1.60735113766186,-1.28942975594381,
9.3997162373487));
#61922=CARTESIAN_POINT('Ctrl Pts',(-1.95701928883641,-0.644612332051665,
9.36279296473647));
#61923=CARTESIAN_POINT('Ctrl Pts',(-1.95719986784682,3.71606954582295E-5,
9.32586969212424));
#61924=CARTESIAN_POINT('Ctrl Pts',(-1.95707453392556,-0.000466568259871601,
9.22413030787576));
#61925=CARTESIAN_POINT('Ctrl Pts',(-1.95715585687005,-0.0257432861687418,
9.22557782057934));
#61926=CARTESIAN_POINT('Ctrl Pts',(-1.95670857405052,-0.0510170594794435,
9.22702533328292));
#61927=CARTESIAN_POINT('Ctrl Pts',(-1.95572375776859,-0.0762698699047084,
9.2284728459865));
#61928=CARTESIAN_POINT('Ctrl Pts',(-1.93050850489432,-0.722843258614067,
9.26553498593022));
#61929=CARTESIAN_POINT('Ctrl Pts',(-1.55290475731554,-1.35567409888606,
9.30259712587394));
#61930=CARTESIAN_POINT('Ctrl Pts',(-0.995863227266852,-1.68491214354887,
9.33965926581766));
#61931=CARTESIAN_POINT('Ctrl Pts',(-0.438821697218168,-2.01415018821168,
9.37672140576139));
#61932=CARTESIAN_POINT('Ctrl Pts',(0.297657615300397,-2.03979543726533,
9.4137835457051));
#61933=CARTESIAN_POINT('Ctrl Pts',(0.876251218790847,-1.75010180082627,
9.45084568564882));
#61934=CARTESIAN_POINT('Ctrl Pts',(1.45484482228131,-1.46040816438721,9.48790782559255));
#61935=CARTESIAN_POINT('Ctrl Pts',(1.87555271674363,-0.855375642455424,
9.52496996553627));
#61936=CARTESIAN_POINT('Ctrl Pts',(1.94568154283725,-0.21212227253196,9.56203210547999));
#61937=CARTESIAN_POINT('Ctrl Pts',(2.01581036893087,0.431131097391505,9.59909424542371));
#61938=CARTESIAN_POINT('Ctrl Pts',(1.73536012665579,1.11260531530666,9.63615638536743));
#61939=CARTESIAN_POINT('Ctrl Pts',(1.23278314419194,1.52017044141902,9.67321852531115));
#61940=CARTESIAN_POINT('Ctrl Pts',(0.730206161728088,1.92773556753138,9.71028066525487));
#61941=CARTESIAN_POINT('Ctrl Pts',(0.00550243907548716,2.06139160184095,
9.74734280519859));
#61942=CARTESIAN_POINT('Ctrl Pts',(-0.609398062732146,1.85992111567971,
9.78440494514231));
#61943=CARTESIAN_POINT('Ctrl Pts',(-1.22429856453979,1.65845062951848,9.82146708508603));
#61944=CARTESIAN_POINT('Ctrl Pts',(-1.72939584550245,1.12185362288641,9.85852922502976));
#61945=CARTESIAN_POINT('Ctrl Pts',(-1.89334427223443,0.495903289718102,
9.89559136497348));
#61946=CARTESIAN_POINT('Ctrl Pts',(-1.93542598326109,0.335236538822793,
9.90510434594091));
#61947=CARTESIAN_POINT('Ctrl Pts',(-1.95503184094814,0.168682937546108,
9.91461732690834));
#61948=CARTESIAN_POINT('Ctrl Pts',(-1.9535343393295,0.00178280253715055,
9.92413030787576));
#61949=CARTESIAN_POINT('Origin',(0.,0.,0.));
#61950=CARTESIAN_POINT('',(-1.95129684289216,-0.00113636086278679,10.7258696921242));
#61951=CARTESIAN_POINT('',(-1.95093054978418,-0.000550606481354719,10.6241303078758));
#61952=CARTESIAN_POINT('',(-1.954,-2.39295984553393E-16,0.));
#61953=CARTESIAN_POINT('Ctrl Pts',(-1.95129684289216,-0.00113636086278679,
10.7258696921242));
#61954=CARTESIAN_POINT('Ctrl Pts',(-1.94942963316978,0.391854106201406,
10.7035356831831));
#61955=CARTESIAN_POINT('Ctrl Pts',(-1.83442754086643,0.785903964976412,
10.6812016742419));
#61956=CARTESIAN_POINT('Ctrl Pts',(-1.61381630858742,1.10744756631717,10.6588676653008));
#61957=CARTESIAN_POINT('Ctrl Pts',(-1.24796949325566,1.64067382739912,10.6218304484723));
#61958=CARTESIAN_POINT('Ctrl Pts',(-0.591690439027595,1.97450300329055,
10.5847932316438));
#61959=CARTESIAN_POINT('Ctrl Pts',(0.0547076636758263,1.95640786233593,
10.5477560148153));
#61960=CARTESIAN_POINT('Ctrl Pts',(0.701105766379276,1.9383127213813,10.5107187979868));
#61961=CARTESIAN_POINT('Ctrl Pts',(1.33762291755807,1.56829326358058,10.4736815811584));
#61962=CARTESIAN_POINT('Ctrl Pts',(1.67312833478204,1.01552035674769,10.4366443643299));
#61963=CARTESIAN_POINT('Ctrl Pts',(2.00863375200599,0.462747449914819,10.3996071475014));
#61964=CARTESIAN_POINT('Ctrl Pts',(2.04312743527515,-0.272778905950186,
10.3625699306729));
#61965=CARTESIAN_POINT('Ctrl Pts',(1.7608042651717,-0.854535269464722,10.3255327138444));
#61966=CARTESIAN_POINT('Ctrl Pts',(1.47848109506825,-1.43629163297926,10.288495497016));
#61967=CARTESIAN_POINT('Ctrl Pts',(0.879341071592168,-1.86427800414334,
10.2514582801875));
#61968=CARTESIAN_POINT('Ctrl Pts',(0.237478981470821,-1.94273555725334,
10.214421063359));
#61969=CARTESIAN_POINT('Ctrl Pts',(-0.404383108650536,-2.02119311036335,
10.1773838465305));
#61970=CARTESIAN_POINT('Ctrl Pts',(-1.08896726541717,-1.75012184541928,
10.140346629702));
#61971=CARTESIAN_POINT('Ctrl Pts',(-1.5031122201388,-1.25351130806383,10.1033094128736));
#61972=CARTESIAN_POINT('Ctrl Pts',(-1.7917522457641,-0.907396556226723,
10.0774961726238));
#61973=CARTESIAN_POINT('Ctrl Pts',(-1.94902777514884,-0.451727225472274,
10.051682932374));
#61974=CARTESIAN_POINT('Ctrl Pts',(-1.95268202714777,0.00165579016441021,
10.0258696921242));
#61975=CARTESIAN_POINT('Ctrl Pts',(-1.9535343393295,0.00178280253715055,
9.92413030787576));
#61976=CARTESIAN_POINT('Ctrl Pts',(-1.94919764294582,-0.481552375812319,
9.95167946685205));
#61977=CARTESIAN_POINT('Ctrl Pts',(-1.76787653021499,-0.967793777264111,
9.97922862582834));
#61978=CARTESIAN_POINT('Ctrl Pts',(-1.44290486192301,-1.32238333502052,
10.0067777848046));
#61979=CARTESIAN_POINT('Ctrl Pts',(-1.00571745237828,-1.79941596688631,
10.0438399247484));
#61980=CARTESIAN_POINT('Ctrl Pts',(-0.308543060787511,-2.03817757091334,
10.0809020646921));
#61981=CARTESIAN_POINT('Ctrl Pts',(0.329297761185238,-1.92930969998698,
10.1179642046358));
#61982=CARTESIAN_POINT('Ctrl Pts',(0.967138583157977,-1.82044182906063,
10.1550263445795));
#61983=CARTESIAN_POINT('Ctrl Pts',(1.5456458355127,-1.36394448318089,10.1920884845232));
#61984=CARTESIAN_POINT('Ctrl Pts',(1.79984980484802,-0.76890421197536,10.229150624467));
#61985=CARTESIAN_POINT('Ctrl Pts',(2.05405377418334,-0.173863940769825,
10.2662127644107));
#61986=CARTESIAN_POINT('Ctrl Pts',(1.98395446049928,0.5597192557615,10.3032749043544));
#61987=CARTESIAN_POINT('Ctrl Pts',(1.62166047466929,1.09585000349956,10.3403370442981));
#61988=CARTESIAN_POINT('Ctrl Pts',(1.2593664888393,1.63198075123761,10.3773991842419));
#61989=CARTESIAN_POINT('Ctrl Pts',(0.604877830863377,1.9706590501824,10.4144613241856));
#61990=CARTESIAN_POINT('Ctrl Pts',(-0.042038551539475,1.95675976549601,
10.4515234641293));
#61991=CARTESIAN_POINT('Ctrl Pts',(-0.688954933942345,1.94286048080962,
10.488585604073));
#61992=CARTESIAN_POINT('Ctrl Pts',(-1.32829904077215,1.57638361249205,10.5256477440167));
#61993=CARTESIAN_POINT('Ctrl Pts',(-1.66723158702796,1.02518946943711,10.5627098839605));
#61994=CARTESIAN_POINT('Ctrl Pts',(-1.85446111291195,0.720704641366568,
10.5831833585989));
#61995=CARTESIAN_POINT('Ctrl Pts',(-1.95001820365716,0.359852200961074,
10.6036568332373));
#61996=CARTESIAN_POINT('Ctrl Pts',(-1.95093054978418,-0.000550606481354719,
10.6241303078758));
#61997=CARTESIAN_POINT('Origin',(0.,0.,-1.29405622560369));
#61998=CARTESIAN_POINT('',(-1.55334812646815,-0.000904610707407963,10.9559437743963));
#61999=CARTESIAN_POINT('',(-1.55659711405804,-0.00105088068675666,11.0940562256037));
#62000=CARTESIAN_POINT('',(-1.5555,-2.01987159101623E-13,-1.29405622560369));
#62001=CARTESIAN_POINT('',(0.499806597877791,1.47301514408978,11.4445));
#62002=CARTESIAN_POINT('Ctrl Pts',(-1.55334812646815,-0.000904610707408108,
10.9559437743963));
#62003=CARTESIAN_POINT('Ctrl Pts',(-1.55432667860164,-0.206859868644216,
10.9706469822836));
#62004=CARTESIAN_POINT('Ctrl Pts',(-1.42041322258558,-0.930327919713715,
11.0223874069994));
#62005=CARTESIAN_POINT('Ctrl Pts',(-0.324962964057439,-1.80887727526569,
11.1111650485437));
#62006=CARTESIAN_POINT('Ctrl Pts',(1.34445241673909,-1.25560970886474,11.2222766990291));
#62007=CARTESIAN_POINT('Ctrl Pts',(1.78171768593789,0.450698535437549,11.3333883495146));
#62008=CARTESIAN_POINT('Ctrl Pts',(0.989503531151977,1.30685679928735,11.4074627831715));
#62009=CARTESIAN_POINT('Ctrl Pts',(0.499806597877626,1.47301514408983,11.4445));
#62010=CARTESIAN_POINT('',(1.55548765964692,0.00619602180124784,11.4445));
#62011=CARTESIAN_POINT('Origin',(0.,0.,11.4445));
#62012=CARTESIAN_POINT('Ctrl Pts',(-1.55659711405804,-0.0010508806867568,
11.0940562256037));
#62013=CARTESIAN_POINT('Ctrl Pts',(-1.55726922058417,-0.079449137192624,
11.099684397238));
#62014=CARTESIAN_POINT('Ctrl Pts',(-1.51630179095532,-0.673453815214831,
11.142374708816));
#62015=CARTESIAN_POINT('Ctrl Pts',(-0.75277483453787,-1.67898453189698,
11.2221271603377));
#62016=CARTESIAN_POINT('Ctrl Pts',(1.00462758039806,-1.53944373403644,11.3333135801688));
#62017=CARTESIAN_POINT('Ctrl Pts',(1.55754888396286,-0.511266487217653,
11.4074378600563));
#62018=CARTESIAN_POINT('Ctrl Pts',(1.55548765964692,0.00619602180124784,
11.4445));
#62019=CARTESIAN_POINT('Origin',(0.,0.,-1.29405622560369));
#62020=CARTESIAN_POINT('',(-1.55445081536763,0.00131810726739325,10.2559437743963));
#62021=CARTESIAN_POINT('',(-1.55305653540906,-0.000438315446397164,10.3940562256037));
#62022=CARTESIAN_POINT('',(-1.5555,-2.01987159101623E-13,-1.29405622560369));
#62023=CARTESIAN_POINT('Ctrl Pts',(-1.55445081536763,0.00131810726739319,
10.2559437743963));
#62024=CARTESIAN_POINT('Ctrl Pts',(-1.55154181384031,-0.359601688445403,
10.2817570146461));
#62025=CARTESIAN_POINT('Ctrl Pts',(-1.24670140973274,-1.24280598265434,
10.3446074717243));
#62026=CARTESIAN_POINT('Ctrl Pts',(0.223056668548975,-1.82477852394609,
10.4444951456311));
#62027=CARTESIAN_POINT('Ctrl Pts',(1.65390974917898,-0.802670846854376,
10.5556067961165));
#62028=CARTESIAN_POINT('Ctrl Pts',(1.57153269033781,0.953897085409752,10.6667184466019));
#62029=CARTESIAN_POINT('Ctrl Pts',(0.0514163720288116,1.83756944970195,
10.7778300970874));
#62030=CARTESIAN_POINT('Ctrl Pts',(-1.30849536725084,1.14582374749785,10.8742385396855));
#62031=CARTESIAN_POINT('Ctrl Pts',(-1.55186171668149,0.311939131113674,
10.9336097654551));
#62032=CARTESIAN_POINT('Ctrl Pts',(-1.55334812646815,-0.000904610707408108,
10.9559437743963));
#62033=CARTESIAN_POINT('Ctrl Pts',(-1.55305653540906,-0.000438315446397077,
10.3940562256037));
#62034=CARTESIAN_POINT('Ctrl Pts',(-1.55364500629154,-0.232901140548306,
10.410644890909));
#62035=CARTESIAN_POINT('Ctrl Pts',(-1.39557528484751,-0.983968830408974,
10.464295696158));
#62036=CARTESIAN_POINT('Ctrl Pts',(-0.231259578302998,-1.82421227428175,
10.5550086413507));
#62037=CARTESIAN_POINT('Ctrl Pts',(1.40774638007895,-1.1829694620695,10.6661950611819));
#62038=CARTESIAN_POINT('Ctrl Pts',(1.75706993010233,0.541796064983141,10.7773814810131));
#62039=CARTESIAN_POINT('Ctrl Pts',(0.497080432048737,1.77049779856472,10.8885679008442));
#62040=CARTESIAN_POINT('Ctrl Pts',(-1.13185991314487,1.39680492671116,10.9941261490411));
#62041=CARTESIAN_POINT('Ctrl Pts',(-1.55284332390808,0.436812153822664,
11.0626222572943));
#62042=CARTESIAN_POINT('Ctrl Pts',(-1.55659711405804,-0.0010508806867568,
11.0940562256037));
#62043=CARTESIAN_POINT('Origin',(0.,0.,-1.29405622560369));
#62044=CARTESIAN_POINT('',(-1.55804728476752,2.95821195149996E-5,9.5559437743963));
#62045=CARTESIAN_POINT('',(-1.55512930646214,0.00141921665610299,9.69405622560371));
#62046=CARTESIAN_POINT('',(-1.5555,-2.01987159101623E-13,-1.29405622560369));
#62047=CARTESIAN_POINT('Ctrl Pts',(-1.55804728476752,2.95821195150548E-5,
9.5559437743963));
#62048=CARTESIAN_POINT('Ctrl Pts',(-1.55790353315504,-0.513149683984934,
9.59286704700854));
#62049=CARTESIAN_POINT('Ctrl Pts',(-1.00033131917675,-1.54135965233235,
9.66682753644926));
#62050=CARTESIAN_POINT('Ctrl Pts',(0.750970673805211,-1.67799333720618,
9.77782524271844));
#62051=CARTESIAN_POINT('Ctrl Pts',(1.81699613594968,-0.279545920640164,
9.88893689320389));
#62052=CARTESIAN_POINT('Ctrl Pts',(1.22062258834496,1.37466418983892,10.0000485436893));
#62053=CARTESIAN_POINT('Ctrl Pts',(-0.492515922639386,1.77116921324136,
10.1111601941748));
#62054=CARTESIAN_POINT('Ctrl Pts',(-1.46173837715872,0.831558022400444,
10.1964586044104));
#62055=CARTESIAN_POINT('Ctrl Pts',(-1.55571569202373,0.15825134364817,10.2447197978176));
#62056=CARTESIAN_POINT('Ctrl Pts',(-1.55445081536763,0.00131810726739319,
10.2559437743963));
#62057=CARTESIAN_POINT('Ctrl Pts',(-1.55512930646214,0.00141921665610296,
9.69405622560371));
#62058=CARTESIAN_POINT('Ctrl Pts',(-1.55167703869094,-0.383344278698275,
9.72160538457999));
#62059=CARTESIAN_POINT('Ctrl Pts',(-1.21314953523015,-1.29115961930375,
9.7862166835));
#62060=CARTESIAN_POINT('Ctrl Pts',(0.309373610575528,-1.81257875466721,
9.88789012236375));
#62061=CARTESIAN_POINT('Ctrl Pts',(1.69095195914933,-0.722381792257861,
9.99907654219489));
#62062=CARTESIAN_POINT('Ctrl Pts',(1.52354231364944,1.0295455294481,10.1102629620261));
#62063=CARTESIAN_POINT('Ctrl Pts',(-0.0394931635484403,1.83836962465064,
10.2214493818572));
#62064=CARTESIAN_POINT('Ctrl Pts',(-1.33855689695156,1.09373648628768,10.3160471363831));
#62065=CARTESIAN_POINT('Ctrl Pts',(-1.5523302537302,0.286463714736223,10.3735827509653));
#62066=CARTESIAN_POINT('Ctrl Pts',(-1.55305653540906,-0.000438315446397077,
10.3940562256037));
#62067=CARTESIAN_POINT('Origin',(0.,0.,-1.29405622560369));
#62068=CARTESIAN_POINT('',(-1.55453687436568,-0.00133745576774406,8.85594377439631));
#62069=CARTESIAN_POINT('',(-1.55794751152569,-0.000371416033132788,8.99405622560372));
#62070=CARTESIAN_POINT('',(-1.5555,-2.01987159101623E-13,-1.29405622560369));
#62071=CARTESIAN_POINT('Ctrl Pts',(-1.55453687436568,-0.00133745576774402,
8.85594377439631));
#62072=CARTESIAN_POINT('Ctrl Pts',(-1.55579877499581,-0.155062375664632,
8.86693986254252));
#62073=CARTESIAN_POINT('Ctrl Pts',(-1.46423861786649,-0.825096309536398,
8.91497316751722));
#62074=CARTESIAN_POINT('Ctrl Pts',(-0.503376402892206,-1.7681153483915,
9.00004368932038));
#62075=CARTESIAN_POINT('Ctrl Pts',(1.2121644264892,-1.38212772940753,9.11115533980582));
#62076=CARTESIAN_POINT('Ctrl Pts',(1.81867711471885,0.26839009932345,9.22226699029127));
#62077=CARTESIAN_POINT('Ctrl Pts',(0.761253709552246,1.67335367481701,9.33337864077668));
#62078=CARTESIAN_POINT('Ctrl Pts',(-0.99265255914171,1.54733978795034,9.44449029126215));
#62079=CARTESIAN_POINT('Ctrl Pts',(-1.55732851093913,0.517959404958592,
9.51867866913534));
#62080=CARTESIAN_POINT('Ctrl Pts',(-1.55804772838109,0.00161323939398619,
9.55582983018006));
#62081=CARTESIAN_POINT('Ctrl Pts',(-1.55804728476752,2.95821195150548E-5,
9.5559437743963));
#62082=CARTESIAN_POINT('Ctrl Pts',(-1.55794751152569,-0.000371416033132616,
8.99405622560372));
#62083=CARTESIAN_POINT('Ctrl Pts',(-1.55801224941728,-0.020493184051098,
8.99550373830729));
#62084=CARTESIAN_POINT('Ctrl Pts',(-1.54853952527048,-0.55575068168544,
9.03401339095459));
#62085=CARTESIAN_POINT('Ctrl Pts',(-0.935609375970031,-1.5829679799695,
9.1095851835456));
#62086=CARTESIAN_POINT('Ctrl Pts',(0.823234386500799,-1.64421340203127,
9.22077160337675));
#62087=CARTESIAN_POINT('Ctrl Pts',(1.82795976495949,-0.199287985657338,
9.33195802320793));
#62088=CARTESIAN_POINT('Ctrl Pts',(1.15819463928053,1.42819381470141,9.44314444303908));
#62089=CARTESIAN_POINT('Ctrl Pts',(-0.572526917402423,1.74738822826618,
9.55433086287024));
#62090=CARTESIAN_POINT('Ctrl Pts',(-1.47990815776177,0.783419353749631,
9.63796812372513));
#62091=CARTESIAN_POINT('Ctrl Pts',(-1.5563214066504,0.1342816322173,9.68454324463628));
#62092=CARTESIAN_POINT('Ctrl Pts',(-1.55512930646214,0.00141921665610296,
9.69405622560371));
#62093=CARTESIAN_POINT('Origin',(0.,0.,-1.29405622560369));
#62094=CARTESIAN_POINT('',(-1.55333906144275,0.000780263919018194,8.15594377439631));
#62095=CARTESIAN_POINT('',(-1.55403083159801,-0.00119596074553197,8.29405622560371));
#62096=CARTESIAN_POINT('',(-1.5555,-2.01987159101623E-13,-1.29405622560369));
#62097=CARTESIAN_POINT('Ctrl Pts',(-1.55333906144275,0.000780263919018167,
8.15594377439631));
#62098=CARTESIAN_POINT('Ctrl Pts',(-1.55193217426013,-0.308862600127516,
8.17804989490498));
#62099=CARTESIAN_POINT('Ctrl Pts',(-1.3122308335565,-1.13929638534857,8.23719323224213));
#62100=CARTESIAN_POINT('Ctrl Pts',(0.0400949547363229,-1.83793690702293,
8.33337378640777));
#62101=CARTESIAN_POINT('Ctrl Pts',(1.56567267939011,-0.963477420579929,
8.44448543689319));
#62102=CARTESIAN_POINT('Ctrl Pts',(1.65879203582308,0.792482593671729,8.55559708737864));
#62103=CARTESIAN_POINT('Ctrl Pts',(0.234256671005791,1.82338791618694,8.66670873786407));
#62104=CARTESIAN_POINT('Ctrl Pts',(-1.24241507899534,1.24912116508194,8.7668243002033));
#62105=CARTESIAN_POINT('Ctrl Pts',(-1.55154841917538,0.362716593952071,
8.82990264571404));
#62106=CARTESIAN_POINT('Ctrl Pts',(-1.55453687436568,-0.00133745576774402,
8.85594377439631));
#62107=CARTESIAN_POINT('Ctrl Pts',(-1.55403083159801,-0.00119596074553188,
8.29405622560371));
#62108=CARTESIAN_POINT('Ctrl Pts',(-1.55527408252746,-0.17480188940304,
8.30646423197829));
#62109=CARTESIAN_POINT('Ctrl Pts',(-1.4483135129372,-0.865473027753662,
8.3559343782966));
#62110=CARTESIAN_POINT('Ctrl Pts',(-0.434704832044991,-1.78666848096071,
8.44246666455862));
#62111=CARTESIAN_POINT('Ctrl Pts',(1.26590215885116,-1.33365823077974,8.55365308438979));
#62112=CARTESIAN_POINT('Ctrl Pts',(1.8068878531032,0.341040818691465,8.66483950422094));
#62113=CARTESIAN_POINT('Ctrl Pts',(0.69268588294083,1.70333168137465,8.77602592405212));
#62114=CARTESIAN_POINT('Ctrl Pts',(-1.03328002592178,1.50787500329959,8.88576483117969));
#62115=CARTESIAN_POINT('Ctrl Pts',(-1.55635469933735,0.494704907375218,
8.95844159836357));
#62116=CARTESIAN_POINT('Ctrl Pts',(-1.55794751152569,-0.000371416033132616,
8.99405622560372));
#62117=CARTESIAN_POINT('Origin',(0.,0.,-1.29405622560369));
#62118=CARTESIAN_POINT('',(-1.55738164088485,0.00090367155389158,7.45594377439631));
#62119=CARTESIAN_POINT('',(-1.55363820104426,0.00100737127591941,7.59405622560371));
#62120=CARTESIAN_POINT('',(-1.5555,-2.01987159101623E-13,-1.29405622560369));
#62121=CARTESIAN_POINT('Ctrl Pts',(-1.55738164088485,0.000903671553891608,
7.45594377439631));
#62122=CARTESIAN_POINT('Ctrl Pts',(-1.55418612064456,-0.461276292775272,
7.48915992726744));
#62123=CARTESIAN_POINT('Ctrl Pts',(-1.09121796390773,-1.44436334125619,
7.55941329696705));
#62124=CARTESIAN_POINT('Ctrl Pts',(0.580004387659595,-1.74448118065669,
7.66670388349515));
#62125=CARTESIAN_POINT('Ctrl Pts',(1.7800908511122,-0.459234407622611,7.77781553398057));
#62126=CARTESIAN_POINT('Ctrl Pts',(1.35154441460109,1.24617309179735,7.88892718446602));
#62127=CARTESIAN_POINT('Ctrl Pts',(-0.313551099181417,1.81143738163968,
8.00003883495145));
#62128=CARTESIAN_POINT('Ctrl Pts',(-1.41757073229054,0.936656796997624,
8.08904436492822));
#62129=CARTESIAN_POINT('Ctrl Pts',(-1.55428931266511,0.209921774117757,
8.1410126780765));
#62130=CARTESIAN_POINT('Ctrl Pts',(-1.55333906144275,0.000780263919018167,
8.15594377439631));
#62131=CARTESIAN_POINT('Ctrl Pts',(-1.55363820104426,0.00100737127591942,
7.59405622560371));
#62132=CARTESIAN_POINT('Ctrl Pts',(-1.55169765832855,-0.326159426902871,
7.6174247256493));
#62133=CARTESIAN_POINT('Ctrl Pts',(-1.29071878250434,-1.17503987929593,
7.67785536563862));
#62134=CARTESIAN_POINT('Ctrl Pts',(0.103792628149562,-1.8358593744105,7.77534814557165));
#62135=CARTESIAN_POINT('Ctrl Pts',(1.59909575810308,-0.907769413831382,
7.8865345654028));
#62136=CARTESIAN_POINT('Ctrl Pts',(1.62955779866738,0.851876712390422,7.99772098523398));
#62137=CARTESIAN_POINT('Ctrl Pts',(0.167274199086701,1.83116681231986,8.10890740506512));
#62138=CARTESIAN_POINT('Ctrl Pts',(-1.26795424285233,1.21093838634352,8.20768581852172));
#62139=CARTESIAN_POINT('Ctrl Pts',(-1.55156054962447,0.343750973057136,
8.26940209203457));
#62140=CARTESIAN_POINT('Ctrl Pts',(-1.55403083159801,-0.00119596074553188,
8.29405622560371));
#62141=CARTESIAN_POINT('Origin',(0.,0.,-1.29405622560369));
#62142=CARTESIAN_POINT('',(-1.55606466149984,-0.00136591087330588,6.7559437743963));
#62143=CARTESIAN_POINT('',(-1.55769406638298,0.000677585252333857,6.89405622560371));
#62144=CARTESIAN_POINT('',(-1.5555,-2.01987159101623E-13,-1.29405622560369));
#62145=CARTESIAN_POINT('Ctrl Pts',(-1.55606466149984,-0.00136591087330577,
6.7559437743963));
#62146=CARTESIAN_POINT('Ctrl Pts',(-1.55699698050756,-0.10301028373747,
6.76323274280142));
#62147=CARTESIAN_POINT('Ctrl Pts',(-1.50160999329305,-0.720125819190329,
6.80755892803501));
#62148=CARTESIAN_POINT('Ctrl Pts',(-0.677079673289082,-1.70914680334463,
6.8889223300971));
#62149=CARTESIAN_POINT('Ctrl Pts',(1.06838781720774,-1.49605051766532,7.00003398058251));
#62150=CARTESIAN_POINT('Ctrl Pts',(1.83637062036826,0.0858057341481814,
7.11114563106797));
#62151=CARTESIAN_POINT('Ctrl Pts',(0.924229284360448,1.589156980696,7.22225728155339));
#62152=CARTESIAN_POINT('Ctrl Pts',(-0.833503847528551,1.63856370505402,
7.33336893203883));
#62153=CARTESIAN_POINT('Ctrl Pts',(-1.53115801604342,0.622214122864029,
7.41126442965314));
#62154=CARTESIAN_POINT('Ctrl Pts',(-1.55774924177056,0.0540711533618156,
7.45212271043896));
#62155=CARTESIAN_POINT('Ctrl Pts',(-1.55738164088485,0.000903671553891608,
7.45594377439631));
#62156=CARTESIAN_POINT('Ctrl Pts',(-1.55769406638298,0.000677585252333878,
6.89405622560371));
#62157=CARTESIAN_POINT('Ctrl Pts',(-1.55508734647919,-0.476733936548398,
6.92838521932031));
#62158=CARTESIAN_POINT('Ctrl Pts',(-1.06472330039144,-1.47419539900055,
6.99977635298063));
#62159=CARTESIAN_POINT('Ctrl Pts',(0.633314188332071,-1.72628667698419,
7.10822962658467));
#62160=CARTESIAN_POINT('Ctrl Pts',(1.7940008868909,-0.403377453646542,7.21941604641583));
#62161=CARTESIAN_POINT('Ctrl Pts',(1.31130494233742,1.28904301731096,7.33060246624699));
#62162=CARTESIAN_POINT('Ctrl Pts',(-0.372603218894873,1.80064416072257,
7.44178888607816));
#62163=CARTESIAN_POINT('Ctrl Pts',(-1.43301362666466,0.901927254173143,
7.52960680586373));
#62164=CARTESIAN_POINT('Ctrl Pts',(-1.55477533406966,0.192722899107996,
7.58036258570558));
#62165=CARTESIAN_POINT('Ctrl Pts',(-1.55363820104426,0.00100737127591942,
7.59405622560371));
#62166=CARTESIAN_POINT('Origin',(0.,0.,-1.29405622560369));
#62167=CARTESIAN_POINT('',(-1.55295085115974,-2.74912889200857E-5,6.0559437743963));
#62168=CARTESIAN_POINT('',(-1.55567057787938,-0.00141549514015751,6.19405622560371));
#62169=CARTESIAN_POINT('',(-1.5555,-2.01987159101623E-13,-1.29405622560369));
#62170=CARTESIAN_POINT('Ctrl Pts',(-1.55295114066544,-2.74881667468134E-5,
6.0559437743963));
#62171=CARTESIAN_POINT('Ctrl Pts',(-1.55299180574127,-0.257905198155464,
6.07434277516388));
#62172=CARTESIAN_POINT('Ctrl Pts',(-1.37005956536857,-1.03483686203599,
6.12977899275993));
#62173=CARTESIAN_POINT('Ctrl Pts',(-0.143272298638598,-1.83278278249422,
6.22225242718446));
#62174=CARTESIAN_POINT('Ctrl Pts',(1.46185859526926,-1.11471481859797,6.33336407766989));
#62175=CARTESIAN_POINT('Ctrl Pts',(1.72951224644592,0.623223129190563,6.44447572815534));
#62176=CARTESIAN_POINT('Ctrl Pts',(0.414808152398764,1.79096450999678,6.55558737864077));
#62177=CARTESIAN_POINT('Ctrl Pts',(-1.1682689842466,1.35101180160119,6.6594100607211));
#62178=CARTESIAN_POINT('Ctrl Pts',(-1.55225961585962,0.413472223515983,
6.72619552597294));
#62179=CARTESIAN_POINT('Ctrl Pts',(-1.55606466149984,-0.00136591087330577,
6.7559437743963));
#62180=CARTESIAN_POINT('Ctrl Pts',(-1.55567057787938,-0.00141549514015748,
6.19405622560371));
#62181=CARTESIAN_POINT('Ctrl Pts',(-1.55673152840384,-0.11622012238534,
6.2022835730476));
#62182=CARTESIAN_POINT('Ctrl Pts',(-1.49271086742403,-0.747018195902368,
6.2475730604352));
#62183=CARTESIAN_POINT('Ctrl Pts',(-0.632665469493242,-1.72652453095426,
6.32992468776653));
#62184=CARTESIAN_POINT('Ctrl Pts',(1.10806726459172,-1.46742614445027,6.44111110759769));
#62185=CARTESIAN_POINT('Ctrl Pts',(1.83376231205259,0.135898253011021,6.55229752742886));
#62186=CARTESIAN_POINT('Ctrl Pts',(0.879651525947856,1.61473395492061,6.66348394726001));
#62187=CARTESIAN_POINT('Ctrl Pts',(-0.880258220622017,1.61440330069759,
6.77467036709119));
#62188=CARTESIAN_POINT('Ctrl Pts',(-1.53940153309356,0.591912849892102,
6.85152779320574));
#62189=CARTESIAN_POINT('Ctrl Pts',(-1.55790160368306,0.0386873070159844,
6.89132307937659));
#62190=CARTESIAN_POINT('Ctrl Pts',(-1.55769406638298,0.000677585252333878,
6.89405622560371));
#62191=CARTESIAN_POINT('Origin',(0.,0.,-1.29405622560369));
#62192=CARTESIAN_POINT('',(-1.55596383579478,0.00138071545366175,5.3559437743963));
#62193=CARTESIAN_POINT('',(-1.5529563387483,0.000151106445085702,5.49405622560371));
#62194=CARTESIAN_POINT('',(-1.5555,-2.01987159101623E-13,-1.29405622560369));
#62195=CARTESIAN_POINT('Ctrl Pts',(-1.55596383579478,0.00138071545366179,
5.3559437743963));
#62196=CARTESIAN_POINT('Ctrl Pts',(-1.55217514150148,-0.410190199764792,
5.38545280752634));
#62197=CARTESIAN_POINT('Ctrl Pts',(-1.17330640529453,-1.34449549172498,
5.45199905748485));
#62198=CARTESIAN_POINT('Ctrl Pts',(0.403262995152723,-1.79359935217008,
5.55558252427184));
#62199=CARTESIAN_POINT('Ctrl Pts',(1.72546185411942,-0.634350903950841,
5.66669417475728));
#62200=CARTESIAN_POINT('Ctrl Pts',(1.46900873501267,1.1052750860401,5.77780582524271));
#62201=CARTESIAN_POINT('Ctrl Pts',(-0.13146340126236,1.83366765077345,5.88891747572816));
#62202=CARTESIAN_POINT('Ctrl Pts',(-1.36655195880861,1.04159698732297,5.98163012544601));
#62203=CARTESIAN_POINT('Ctrl Pts',(-1.55290994688111,0.261203028467153,
6.0373055583354));
#62204=CARTESIAN_POINT('Ctrl Pts',(-1.55295114066544,-2.74881667468134E-5,
6.0559437743963));
#62205=CARTESIAN_POINT('Ctrl Pts',(-1.5529563387483,0.000151106445085633,
5.49405622560371));
#62206=CARTESIAN_POINT('Ctrl Pts',(-1.55272340811799,-0.268780222436924,
5.5132440667186));
#62207=CARTESIAN_POINT('Ctrl Pts',(-1.35831396530156,-1.05747938365068,
5.56949404777722));
#62208=CARTESIAN_POINT('Ctrl Pts',(-0.103102773360761,-1.83589824620028,
5.66280616877956));
#62209=CARTESIAN_POINT('Ctrl Pts',(1.4869956060099,-1.08166382022474,5.77399258861071));
#62210=CARTESIAN_POINT('Ctrl Pts',(1.71494149863546,0.663421591850831,5.88517900844189));
#62211=CARTESIAN_POINT('Ctrl Pts',(0.371926577693494,1.80078404398782,5.99636542827304));
#62212=CARTESIAN_POINT('Ctrl Pts',(-1.18720103315053,1.32645343006727,6.09932450066032));
#62213=CARTESIAN_POINT('Ctrl Pts',(-1.55195221197423,0.40094597399841,6.16522143310387));
#62214=CARTESIAN_POINT('Ctrl Pts',(-1.55567057787938,-0.00141549514015748,
6.19405622560371));
#62215=CARTESIAN_POINT('Origin',(0.,0.,-1.29405622560369));
#62216=CARTESIAN_POINT('',(-1.55745492001379,-0.000856371120316566,4.6559437743963));
#62217=CARTESIAN_POINT('',(-1.55622585425313,0.00134239099646036,4.79405622560371));
#62218=CARTESIAN_POINT('',(-1.5555,-2.01987159101623E-13,-1.29405622560369));
#62219=CARTESIAN_POINT('Ctrl Pts',(-1.55745492001379,-0.000856371120316864,
4.65594377439631));
#62220=CARTESIAN_POINT('Ctrl Pts',(-1.5577850741697,-0.0506891626144068,
4.65952562306032));
#62221=CARTESIAN_POINT('Ctrl Pts',(-1.53301192978291,-0.615473136307116,
4.70014468855281));
#62222=CARTESIAN_POINT('Ctrl Pts',(-0.844041411881997,-1.63316067010957,
4.77780097087378));
#62223=CARTESIAN_POINT('Ctrl Pts',(0.913973507436636,-1.59507746114991,
4.88891262135923));
#62224=CARTESIAN_POINT('Ctrl Pts',(1.83577980123458,-0.0976329900371924,
5.00002427184466));
#62225=CARTESIAN_POINT('Ctrl Pts',(1.0780025055099,1.48913742733129,5.1111359223301));
#62226=CARTESIAN_POINT('Ctrl Pts',(-0.666056105926533,1.7134727727987,5.22224757281553));
#62227=CARTESIAN_POINT('Ctrl Pts',(-1.49938299705611,0.726891414718789,
5.30385019017093));
#62228=CARTESIAN_POINT('Ctrl Pts',(-1.55693038683329,0.106378444150779,
5.34841559069786));
#62229=CARTESIAN_POINT('Ctrl Pts',(-1.55596383579478,0.00138071545366179,
5.3559437743963));
#62230=CARTESIAN_POINT('Ctrl Pts',(-1.55622585425313,0.00134239099646029,
4.79405622560371));
#62231=CARTESIAN_POINT('Ctrl Pts',(-1.55239700220769,-0.418962472451577,
4.82420456038961));
#62232=CARTESIAN_POINT('Ctrl Pts',(-1.15964303797854,-1.36226320639006,
4.89141503511923));
#62233=CARTESIAN_POINT('Ctrl Pts',(0.435376164803608,-1.7865050090601,4.99568764979258));
#62234=CARTESIAN_POINT('Ctrl Pts',(1.73732980498774,-0.602360109052031,
5.10687406962374));
#62235=CARTESIAN_POINT('Ctrl Pts',(1.44781397169404,1.13357278356683,5.21806048945491));
#62236=CARTESIAN_POINT('Ctrl Pts',(-0.167962271460079,1.83110382765203,
5.32924690928607));
#62237=CARTESIAN_POINT('Ctrl Pts',(-1.37758975876034,1.02035875886683,5.42124548800234));
#62238=CARTESIAN_POINT('Ctrl Pts',(-1.55317332364345,0.250672199885809,
5.47618192677488));
#62239=CARTESIAN_POINT('Ctrl Pts',(-1.5529563387483,0.000151106445085633,
5.49405622560371));
#62240=CARTESIAN_POINT('Origin',(0.,0.,-1.29405622560369));
#62241=CARTESIAN_POINT('',(-1.55339129538237,-0.00082587420025254,3.9559437743963));
#62242=CARTESIAN_POINT('',(-1.5573160577951,-0.00094952305265919,4.09405622560371));
#62243=CARTESIAN_POINT('',(-1.5555,-2.01987159101623E-13,-1.29405622560369));
#62244=CARTESIAN_POINT('Ctrl Pts',(-1.55339129538237,-0.000825874200252562,
3.9559437743963));
#62245=CARTESIAN_POINT('Ctrl Pts',(-1.55438295724494,-0.206599346759669,
3.97063565542278));
#62246=CARTESIAN_POINT('Ctrl Pts',(-1.42062281789543,-0.929876204718288,
4.02236475327773));
#62247=CARTESIAN_POINT('Ctrl Pts',(-0.325213021862407,-1.80938005122649,
4.11113106796117));
#62248=CARTESIAN_POINT('Ctrl Pts',(1.34348911316817,-1.25485325124609,4.2222427184466));
#62249=CARTESIAN_POINT('Ctrl Pts',(1.78301209192838,0.447758371671112,4.33335436893204));
#62250=CARTESIAN_POINT('Ctrl Pts',(0.591229481908682,1.74070887258225,4.44446601941748));
#62251=CARTESIAN_POINT('Ctrl Pts',(-1.0856218085317,1.45071736103991,4.55199582123889));
#62252=CARTESIAN_POINT('Ctrl Pts',(-1.55437119708937,0.464594445617744,
4.62248840623184));
#62253=CARTESIAN_POINT('Ctrl Pts',(-1.55745492001379,-0.000856371120316864,
4.65594377439631));
#62254=CARTESIAN_POINT('Ctrl Pts',(-1.5573160577951,-0.000949523052659442,
4.0940562256037));
#62255=CARTESIAN_POINT('Ctrl Pts',(-1.55772052747877,-0.0572626470532979,
4.0981029141169));
#62256=CARTESIAN_POINT('Ctrl Pts',(-1.52938259291224,-0.628915705084586,
4.13921174257381));
#62257=CARTESIAN_POINT('Ctrl Pts',(-0.822616502622442,-1.64452261823584,
4.21738271097444));
#62258=CARTESIAN_POINT('Ctrl Pts',(0.936204134582059,-1.58261630557358,
4.3285691308056));
#62259=CARTESIAN_POINT('Ctrl Pts',(1.83742116834086,-0.0709647969689106,
4.43975555063676));
#62260=CARTESIAN_POINT('Ctrl Pts',(1.0554806974386,1.50569354438759,4.55094197046793));
#62261=CARTESIAN_POINT('Ctrl Pts',(-0.693325883166112,1.70307127625589,
4.66212839029909));
#62262=CARTESIAN_POINT('Ctrl Pts',(-1.50503746143118,0.709862178387775,
4.74316647534435));
#62263=CARTESIAN_POINT('Ctrl Pts',(-1.55710391061042,0.0977293375193425,
4.78714242044589));
#62264=CARTESIAN_POINT('Ctrl Pts',(-1.55622585425313,0.00134239099646029,
4.79405622560371));
#62265=CARTESIAN_POINT('Origin',(0.,0.,-1.29405622560369));
#62266=CARTESIAN_POINT('',(-1.55444674488022,0.00131742778884735,3.2559437743963));
#62267=CARTESIAN_POINT('',(-1.5533186684889,-0.000770198572060954,3.39405622560371));
#62268=CARTESIAN_POINT('',(-1.5555,-2.01987159101623E-13,-1.29405622560369));
#62269=CARTESIAN_POINT('Ctrl Pts',(-1.55444674488022,0.00131742778884739,
3.2559437743963));
#62270=CARTESIAN_POINT('Ctrl Pts',(-1.55154236665719,-0.359445316439912,
3.28174568778523));
#62271=CARTESIAN_POINT('Ctrl Pts',(-1.24691611905359,-1.24248704432008,
3.34458481800264));
#62272=CARTESIAN_POINT('Ctrl Pts',(0.222506403513669,-1.8248590575151,3.44446116504855));
#62273=CARTESIAN_POINT('Ctrl Pts',(1.65365282072159,-0.803151310699741,
3.55557281553397));
#62274=CARTESIAN_POINT('Ctrl Pts',(1.57184646516792,0.953372104320743,3.66668446601942));
#62275=CARTESIAN_POINT('Ctrl Pts',(0.0519332482321354,1.83764050268212,
3.77779611650485));
#62276=CARTESIAN_POINT('Ctrl Pts',(-1.30823935507303,1.14600960175539,3.87421588596382));
#62277=CARTESIAN_POINT('Ctrl Pts',(-1.55188304621527,0.312141358191517,
3.9335984385943));
#62278=CARTESIAN_POINT('Ctrl Pts',(-1.55339129538237,-0.000825874200252562,
3.9559437743963));
#62279=CARTESIAN_POINT('Ctrl Pts',(-1.5533186684889,-0.000770198572060919,
3.39405622560371));
#62280=CARTESIAN_POINT('Ctrl Pts',(-1.5542597194186,-0.210984061911746,
3.4090634077879));
#62281=CARTESIAN_POINT('Ctrl Pts',(-1.41654850766895,-0.939166341982764,
3.46113272991582));
#62282=CARTESIAN_POINT('Ctrl Pts',(-0.308692884081366,-1.81269447386996,
3.55026419198746));
#62283=CARTESIAN_POINT('Ctrl Pts',(1.35606994996762,-1.24186426112907,3.66145061181863));
#62284=CARTESIAN_POINT('Ctrl Pts',(1.77861387826841,0.466567491694538,3.77263703164979));
#62285=CARTESIAN_POINT('Ctrl Pts',(0.571870330903418,1.74760318061885,3.88382345148095));
#62286=CARTESIAN_POINT('Ctrl Pts',(-1.09574509035902,1.43939945308724,3.99096318279893));
#62287=CARTESIAN_POINT('Ctrl Pts',(-1.55401613758806,0.458488658137791,
4.06104077417318));
#62288=CARTESIAN_POINT('Ctrl Pts',(-1.5573160577951,-0.000949523052659442,
4.0940562256037));
#62289=CARTESIAN_POINT('Origin',(0.,0.,-1.29405622560369));
#62290=CARTESIAN_POINT('',(-1.55804712705668,3.25009013604671E-5,2.5559437743963));
#62291=CARTESIAN_POINT('',(-1.55449947323643,0.00133480041304715,2.69405622560371));
#62292=CARTESIAN_POINT('',(-1.5555,-2.01987159101623E-13,-1.29405622560369));
#62293=CARTESIAN_POINT('Ctrl Pts',(-1.55804712705668,3.25009013604029E-5,
2.5559437743963));
#62294=CARTESIAN_POINT('Ctrl Pts',(-1.55788927539753,-0.512989453804214,
2.59285572014769));
#62295=CARTESIAN_POINT('Ctrl Pts',(-1.0006227616332,-1.54106832868198,2.66680488272757));
#62296=CARTESIAN_POINT('Ctrl Pts',(0.750458968510211,-1.67822257683237,
2.77779126213592));
#62297=CARTESIAN_POINT('Ctrl Pts',(1.81691053470019,-0.280099604209337,
2.88890291262136));
#62298=CARTESIAN_POINT('Ctrl Pts',(1.22104229764526,1.37429086670804,3.0000145631068));
#62299=CARTESIAN_POINT('Ctrl Pts',(-0.491976593161155,1.77132117679823,
3.11112621359223));
#62300=CARTESIAN_POINT('Ctrl Pts',(-1.46161229246342,0.831876851886141,
3.19643595068874));
#62301=CARTESIAN_POINT('Ctrl Pts',(-1.55571144064704,0.158409610837222,
3.24470847095676));
#62302=CARTESIAN_POINT('Ctrl Pts',(-1.55444674488022,0.00131742778884739,
3.2559437743963));
#62303=CARTESIAN_POINT('Ctrl Pts',(-1.55449947323643,0.00133480041304701,
2.69405622560371));
#62304=CARTESIAN_POINT('Ctrl Pts',(-1.55153406972295,-0.361714100102126,
2.72002390145891));
#62305=CARTESIAN_POINT('Ctrl Pts',(-1.2437032104418,-1.24745277135715,2.78305371725784));
#62306=CARTESIAN_POINT('Ctrl Pts',(0.231926238140432,-1.82410602009977,
2.88314567300049));
#62307=CARTESIAN_POINT('Ctrl Pts',(1.65866396469461,-0.793716828903688,
2.99433209283165));
#62308=CARTESIAN_POINT('Ctrl Pts',(1.56599354026699,0.96375141196464,3.10551851266282));
#62309=CARTESIAN_POINT('Ctrl Pts',(0.0388050940998321,1.83838154825996,
3.21670493249398));
#62310=CARTESIAN_POINT('Ctrl Pts',(-1.31300314367493,1.13822266482633,3.31288417014094));
#62311=CARTESIAN_POINT('Ctrl Pts',(-1.55193567478298,0.308165737536199,
3.37200126784418));
#62312=CARTESIAN_POINT('Ctrl Pts',(-1.5533186684889,-0.000770198572060919,
3.39405622560371));
#62313=CARTESIAN_POINT('Origin',(0.,0.,-1.29405622560369));
#62314=CARTESIAN_POINT('',(-1.55454118234884,-0.00133834695600709,1.8559437743963));
#62315=CARTESIAN_POINT('',(-1.55805467550008,3.4854191793785E-5,1.9940562256037));
#62316=CARTESIAN_POINT('',(-1.5555,-2.01987159101623E-13,-1.29405622560369));
#62317=CARTESIAN_POINT('Ctrl Pts',(-1.55454118234884,-0.00133834695600729,
1.8559437743963));
#62318=CARTESIAN_POINT('Ctrl Pts',(-1.55580288786201,-0.154903851691022,
1.86692853568168));
#62319=CARTESIAN_POINT('Ctrl Pts',(-1.46436232298065,-0.824775316270878,
1.91495051379553));
#62320=CARTESIAN_POINT('Ctrl Pts',(-0.503915664640746,-1.76796168665343,
2.00000970873786));
#62321=CARTESIAN_POINT('Ctrl Pts',(1.21174280763407,-1.38249741391359,2.1111213592233));
#62322=CARTESIAN_POINT('Ctrl Pts',(1.81875888824183,0.267835396201195,2.22223300970874));
#62323=CARTESIAN_POINT('Ctrl Pts',(0.761764071097843,1.67312138149853,2.33334466019417));
#62324=CARTESIAN_POINT('Ctrl Pts',(-0.992180579104728,1.54764252547341,
2.44445631067961));
#62325=CARTESIAN_POINT('Ctrl Pts',(-1.55725669913861,0.518277207581445,
2.51865601541365));
#62326=CARTESIAN_POINT('Ctrl Pts',(-1.55804766277071,0.0017735852989955,
2.55581850331921));
#62327=CARTESIAN_POINT('Ctrl Pts',(-1.55804712705668,3.25009013604029E-5,
2.5559437743963));
#62328=CARTESIAN_POINT('Ctrl Pts',(-1.55805467550008,3.48541917938314E-5,
1.9940562256037));
#62329=CARTESIAN_POINT('Ctrl Pts',(-1.55788564535512,-0.513206116891616,
2.03098439512992));
#62330=CARTESIAN_POINT('Ctrl Pts',(-1.00003893378143,-1.54186484140614,
2.10497470459985));
#62331=CARTESIAN_POINT('Ctrl Pts',(0.752488571272716,-1.67777039880966,
2.21602715401351));
#62332=CARTESIAN_POINT('Ctrl Pts',(1.81781810074028,-0.276929424335053,
2.32721357384467));
#62333=CARTESIAN_POINT('Ctrl Pts',(1.21794738393109,1.37759091140133,2.43839999367584));
#62334=CARTESIAN_POINT('Ctrl Pts',(-0.497615974795104,1.77017821004958,
2.549586413507));
#62335=CARTESIAN_POINT('Ctrl Pts',(-1.46313162187878,0.828233020270418,
2.63480515748296));
#62336=CARTESIAN_POINT('Ctrl Pts',(-1.55576641614544,0.156444291597347,
2.68296176151519));
#62337=CARTESIAN_POINT('Ctrl Pts',(-1.55449947323643,0.00133480041304701,
2.69405622560371));
#62338=CARTESIAN_POINT('Origin',(0.,0.,-1.29405622560369));
#62339=CARTESIAN_POINT('',(-1.55333634177863,0.000779921548230329,1.1559437743963));
#62340=CARTESIAN_POINT('',(-1.55460191805193,-0.00135568056800359,1.2940562256037));
#62341=CARTESIAN_POINT('',(-1.5555,-2.01987159101623E-13,-1.29405622560369));
#62342=CARTESIAN_POINT('Ctrl Pts',(-1.55333634177863,0.000779921548230561,
1.1559437743963));
#62343=CARTESIAN_POINT('Ctrl Pts',(-1.55193438638927,-0.308706275100063,
1.17803856804414));
#62344=CARTESIAN_POINT('Ctrl Pts',(-1.31241956589738,-1.1389814578602,1.23717057852045));
#62345=CARTESIAN_POINT('Ctrl Pts',(0.0395347168138628,-1.83794704008407,
1.33333980582524));
#62346=CARTESIAN_POINT('Ctrl Pts',(1.56537855283131,-0.963955976349113,
1.44445145631068));
#62347=CARTESIAN_POINT('Ctrl Pts',(1.65903376979378,0.791977165381959,1.55556310679611));
#62348=CARTESIAN_POINT('Ctrl Pts',(0.234812759114929,1.82331608910266,1.66667475728155));
#62349=CARTESIAN_POINT('Ctrl Pts',(-1.24220109658982,1.24943524423025,1.76680164648161));
#62350=CARTESIAN_POINT('Ctrl Pts',(-1.55154880719052,0.362871523529771,
1.8298913188532));
#62351=CARTESIAN_POINT('Ctrl Pts',(-1.55454118234884,-0.00133834695600729,
1.8559437743963));
#62352=CARTESIAN_POINT('Ctrl Pts',(-1.55460191805193,-0.00135568056800364,
1.2940562256037));
#62353=CARTESIAN_POINT('Ctrl Pts',(-1.5558637635503,-0.152693971168416,
1.30488274885721));
#62354=CARTESIAN_POINT('Ctrl Pts',(-1.46605510259419,-0.820638709603335,
1.35277141205443));
#62355=CARTESIAN_POINT('Ctrl Pts',(-0.510374815939226,-1.76654153931159,
1.43772221519537));
#62356=CARTESIAN_POINT('Ctrl Pts',(1.20797626960931,-1.38634273102519,1.54890863502654));
#62357=CARTESIAN_POINT('Ctrl Pts',(1.81976886629041,0.263806680570579,1.6600950548577));
#62358=CARTESIAN_POINT('Ctrl Pts',(0.764574137846417,1.67229745635935,1.77128147468886));
#62359=CARTESIAN_POINT('Ctrl Pts',(-0.991003621173195,1.54889135395602,
1.88246789452002));
#62360=CARTESIAN_POINT('Ctrl Pts',(-1.5572087700955,0.518861158146894,1.95672614482497));
#62361=CARTESIAN_POINT('Ctrl Pts',(-1.55805528871865,0.00189682319971778,
1.9939222551862));
#62362=CARTESIAN_POINT('Ctrl Pts',(-1.55805467550008,3.48541917938314E-5,
1.9940562256037));
#62363=CARTESIAN_POINT('Origin',(0.,0.,-1.29405622560369));
#62364=CARTESIAN_POINT('',(-1.55735926886437,0.00101346774827271,0.455943774396301));
#62365=CARTESIAN_POINT('',(-1.55326046963413,0.000729270061605516,0.594056225603705));
#62366=CARTESIAN_POINT('',(-1.5555,-2.01987159101623E-13,-1.29405622560369));
#62367=CARTESIAN_POINT('Ctrl Pts',(-1.55735926886437,0.00101346774827265,
0.455943774396301));
#62368=CARTESIAN_POINT('Ctrl Pts',(-1.5541538777776,-0.460983628495037,
0.489148600406595));
#62369=CARTESIAN_POINT('Ctrl Pts',(-1.09151218308356,-1.44423481489054,
0.559390643245367));
#62370=CARTESIAN_POINT('Ctrl Pts',(0.579488995883613,-1.74456230311225,
0.666669902912619));
#62371=CARTESIAN_POINT('Ctrl Pts',(1.77994191588978,-0.459827600750814,
0.777781553398056));
#62372=CARTESIAN_POINT('Ctrl Pts',(1.35192905881154,1.24578720765632,0.888893203883492));
#62373=CARTESIAN_POINT('Ctrl Pts',(-0.313001003158473,1.81151906168851,
1.00000485436893));
#62374=CARTESIAN_POINT('Ctrl Pts',(-1.41742497137191,0.93698092273704,1.08902171120653));
#62375=CARTESIAN_POINT('Ctrl Pts',(-1.55428446607623,0.210081433596544,
1.14100135121566));
#62376=CARTESIAN_POINT('Ctrl Pts',(-1.55333634177863,0.000779921548230561,
1.1559437743963));
#62377=CARTESIAN_POINT('Ctrl Pts',(-1.55326046963413,0.000729270061605551,
0.594056225603705));
#62378=CARTESIAN_POINT('Ctrl Pts',(-1.55199262831984,-0.304485333833814,
0.615843242528215));
#62379=CARTESIAN_POINT('Ctrl Pts',(-1.31743653601245,-1.13071739766558,
0.674692399396446));
#62380=CARTESIAN_POINT('Ctrl Pts',(0.0255447675030308,-1.83860034663711,
0.770603696208398));
#62381=CARTESIAN_POINT('Ctrl Pts',(1.55899683301632,-0.975032021788082,
0.881790116039561));
#62382=CARTESIAN_POINT('Ctrl Pts',(1.66434877052597,0.781732535368643,0.992976535870723));
#62383=CARTESIAN_POINT('Ctrl Pts',(0.245080507541896,1.82238325373942,1.10416295570189));
#62384=CARTESIAN_POINT('Ctrl Pts',(-1.23863138927055,1.25487925833816,1.20452285227955));
#62385=CARTESIAN_POINT('Ctrl Pts',(-1.55154412248428,0.365378245899198,
1.26782060891349));
#62386=CARTESIAN_POINT('Ctrl Pts',(-1.55460191805193,-0.00135568056800364,
1.2940562256037));
#62387=CARTESIAN_POINT('Origin',(0.,0.,11.5));
#62388=CARTESIAN_POINT('',(-1.77892626630995,-0.0012009523392913,11.2223275485995));
#62389=CARTESIAN_POINT('Ctrl Pts',(1.55548765964692,0.00619602180104861,
11.4445));
#62390=CARTESIAN_POINT('Ctrl Pts',(1.55843889773201,-0.053546881811892,
11.4417867591843));
#62391=CARTESIAN_POINT('Ctrl Pts',(1.55766805736304,-0.113278156040886,
11.439086160746));
#62392=CARTESIAN_POINT('Ctrl Pts',(1.55338999746751,-0.172741258360748,
11.4363936568093));
#62393=CARTESIAN_POINT('Ctrl Pts',(1.54917978268939,-0.231261344159722,
11.4337438528932));
#62394=CARTESIAN_POINT('Ctrl Pts',(1.54157226362346,-0.289522447371128,
11.4311018887755));
#62395=CARTESIAN_POINT('Ctrl Pts',(1.5307259163647,-0.347284232316321,11.4284634295395));
#62396=CARTESIAN_POINT('Ctrl Pts',(1.52490021612,-0.37830876404678,11.427046282158));
#62397=CARTESIAN_POINT('Ctrl Pts',(1.51813939227042,-0.409189253639797,
11.4256301458963));
#62398=CARTESIAN_POINT('Ctrl Pts',(1.51046300038634,-0.439887833717896,
11.4242143490555));
#62399=CARTESIAN_POINT('Ctrl Pts',(1.50749771858011,-0.451746261786366,
11.4236674467248));
#62400=CARTESIAN_POINT('Ctrl Pts',(1.50439653465153,-0.463574222421597,
11.4231207471528));
#62401=CARTESIAN_POINT('Ctrl Pts',(1.50116353235453,-0.47535996619676,11.4225746575513));
#62402=CARTESIAN_POINT('Ctrl Pts',(1.48455611813741,-0.535901441503565,
11.4197694828629));
#62403=CARTESIAN_POINT('Ctrl Pts',(1.46445634965142,-0.595403551134085,
11.4169769764437));
#62404=CARTESIAN_POINT('Ctrl Pts',(1.4410621824655,-0.653580209875647,11.414192092755));
#62405=CARTESIAN_POINT('Ctrl Pts',(1.41747802435967,-0.712229338392404,
11.4113845922059));
#62406=CARTESIAN_POINT('Ctrl Pts',(1.39054537943373,-0.769532412755046,
11.4085848387028));
#62407=CARTESIAN_POINT('Ctrl Pts',(1.36041578548535,-0.825184282227088,
11.4057876627772));
#62408=CARTESIAN_POINT('Ctrl Pts',(1.35261592294621,-0.839591277975912,
11.4050635379265));
#62409=CARTESIAN_POINT('Ctrl Pts',(1.34460155997405,-0.853887506909652,
11.4043395858183));
#62410=CARTESIAN_POINT('Ctrl Pts',(1.33637481784576,-0.868067413704247,
11.4036157167661));
#62411=CARTESIAN_POINT('Ctrl Pts',(1.33123141939554,-0.87693275912219,11.4031631503791));
#62412=CARTESIAN_POINT('Ctrl Pts',(1.32600576325494,-0.885751206456736,
11.4027106878625));
#62413=CARTESIAN_POINT('Ctrl Pts',(1.32070341258855,-0.894513477947337,
11.4022587210796));
#62414=CARTESIAN_POINT('Ctrl Pts',(1.28755838481391,-0.949286492822766,
11.3994334738427));
#62415=CARTESIAN_POINT('Ctrl Pts',(1.25136992677528,-1.00195372283142,11.3966231054397));
#62416=CARTESIAN_POINT('Ctrl Pts',(1.21232687524415,-1.05222079285711,11.3938225048748));
#62417=CARTESIAN_POINT('Ctrl Pts',(1.17352218779371,-1.10218097437215,11.3910390024248));
#62418=CARTESIAN_POINT('Ctrl Pts',(1.13189715922074,-1.14977118940024,11.3882651489085));
#62419=CARTESIAN_POINT('Ctrl Pts',(1.08759128036108,-1.19468014867466,11.3854959263702));
#62420=CARTESIAN_POINT('Ctrl Pts',(1.05692354853581,-1.22576532190738,11.3835791203762));
#62421=CARTESIAN_POINT('Ctrl Pts',(1.0249704261144,-1.25556541150052,11.3816645331574));
#62422=CARTESIAN_POINT('Ctrl Pts',(0.991767007145199,-1.28396712328559,
11.379750500582));
#62423=CARTESIAN_POINT('Ctrl Pts',(0.971829282858114,-1.30102155672743,
11.378601177562));
#62424=CARTESIAN_POINT('Ctrl Pts',(0.951440575196337,-1.31757160665078,
11.3774520545279));
#62425=CARTESIAN_POINT('Ctrl Pts',(0.930607078503626,-1.33359088746794,
11.3763027711782));
#62426=CARTESIAN_POINT('Ctrl Pts',(0.921822018225176,-1.34034589118487,
11.3758181418501));
#62427=CARTESIAN_POINT('Ctrl Pts',(0.912957575551233,-1.34700657088378,
11.3753334724466));
#62428=CARTESIAN_POINT('Ctrl Pts',(0.904026617991894,-1.35356212132308,
11.3748494000991));
#62429=CARTESIAN_POINT('Ctrl Pts',(0.898865665597572,-1.35735039189889,
11.3745696681303));
#62430=CARTESIAN_POINT('Ctrl Pts',(0.893681522170691,-1.36110432047063,
11.3742900812105));
#62431=CARTESIAN_POINT('Ctrl Pts',(0.888474357058895,-1.36482361432558,
11.3740106343829));
#62432=CARTESIAN_POINT('Ctrl Pts',(0.838811308516624,-1.4002961732508,11.3713454257582));
#62433=CARTESIAN_POINT('Ctrl Pts',(0.787057395286918,-1.43262124116857,
11.368692960317));
#62434=CARTESIAN_POINT('Ctrl Pts',(0.733560484100527,-1.46184200007972,
11.3660489378073));
#62435=CARTESIAN_POINT('Ctrl Pts',(0.677705393253366,-1.49235082960671,
11.3632883650152));
#62436=CARTESIAN_POINT('Ctrl Pts',(0.619949541746925,-1.51947609806138,
11.3605369959002));
#62437=CARTESIAN_POINT('Ctrl Pts',(0.560651932851881,-1.54322365588157,
11.3577899361005));
#62438=CARTESIAN_POINT('Ctrl Pts',(0.511114145446654,-1.56306259192994,
11.3554950161722));
#62439=CARTESIAN_POINT('Ctrl Pts',(0.460499386969577,-1.58054347420583,
11.3532031037542));
#62440=CARTESIAN_POINT('Ctrl Pts',(0.409004561176526,-1.5956447160272,11.3509113452381));
#62441=CARTESIAN_POINT('Ctrl Pts',(0.394571471762801,-1.59987732717035,
11.3502690058367));
#62442=CARTESIAN_POINT('Ctrl Pts',(0.38006920116156,-1.60392285642947,11.3496266785255));
#62443=CARTESIAN_POINT('Ctrl Pts',(0.365502000908426,-1.60778049339754,
11.3489843004725));
#62444=CARTESIAN_POINT('Ctrl Pts',(0.352945849497182,-1.61110557117631,
11.3484306047756));
#62445=CARTESIAN_POINT('Ctrl Pts',(0.340339686983491,-1.61429135213649,
11.3478767954507));
#62446=CARTESIAN_POINT('Ctrl Pts',(0.327707338901135,-1.61733252206154,
11.3473237518226));
#62447=CARTESIAN_POINT('Ctrl Pts',(0.26442068399392,-1.63256844418037,11.3445530649309));
#62448=CARTESIAN_POINT('Ctrl Pts',(0.200363163100888,-1.64421053384351,
11.3417964693365));
#62449=CARTESIAN_POINT('Ctrl Pts',(0.135902532141567,-1.65227549235515,
11.3390491503551));
#62450=CARTESIAN_POINT('Ctrl Pts',(0.0706504004584388,-1.66043947907059,
11.3362680975283));
#62451=CARTESIAN_POINT('Ctrl Pts',(0.00498413291330568,-1.6649382180869,
11.333496550525));
#62452=CARTESIAN_POINT('Ctrl Pts',(-0.0607337043444866,-1.66573959706564,
11.3307295151184));
#62453=CARTESIAN_POINT('Ctrl Pts',(-0.114943810254912,-1.66640064802417,
11.3284470102656));
#62454=CARTESIAN_POINT('Ctrl Pts',(-0.169189647051337,-1.66454499730668,
11.326167575313));
#62455=CARTESIAN_POINT('Ctrl Pts',(-0.223269283792523,-1.66012780789457,
11.3238884070273));
#62456=CARTESIAN_POINT('Ctrl Pts',(-0.242921115785065,-1.65852265909112,
11.3230601871106));
#62457=CARTESIAN_POINT('Ctrl Pts',(-0.262550978640708,-1.65657902103982,
11.3222320024074));
#62458=CARTESIAN_POINT('Ctrl Pts',(-0.282149042864747,-1.65429391513469,
11.3214037184036));
#62459=CARTESIAN_POINT('Ctrl Pts',(-0.293822649715497,-1.65293278948249,
11.3209103501959));
#62460=CARTESIAN_POINT('Ctrl Pts',(-0.305486007024825,-1.65145026241138,
11.3204169024293));
#62461=CARTESIAN_POINT('Ctrl Pts',(-0.317120120921591,-1.64984824722041,
11.3199240638241));
#62462=CARTESIAN_POINT('Ctrl Pts',(-0.382649500838262,-1.64082486451904,
11.3171481404934));
#62463=CARTESIAN_POINT('Ctrl Pts',(-0.447374851901241,-1.62800143931766,
11.3143862955204));
#62464=CARTESIAN_POINT('Ctrl Pts',(-0.510936115769287,-1.6113566500933,
11.3116336908415));
#62465=CARTESIAN_POINT('Ctrl Pts',(-0.573549739883189,-1.59496001930709,
11.3089221249567));
#62466=CARTESIAN_POINT('Ctrl Pts',(-0.635034780101342,-1.57485515271455,
11.3062195258916));
#62467=CARTESIAN_POINT('Ctrl Pts',(-0.695044280650932,-1.55097228857054,
11.3035212687658));
#62468=CARTESIAN_POINT('Ctrl Pts',(-0.755213263935446,-1.52702595273528,
11.3008158406849));
#62469=CARTESIAN_POINT('Ctrl Pts',(-0.813899721511821,-1.49928127162975,
11.2981147776525));
#62470=CARTESIAN_POINT('Ctrl Pts',(-0.870916818143125,-1.46801413582731,
11.2954134178164));
#62471=CARTESIAN_POINT('Ctrl Pts',(-0.88517189274549,-1.46019691292752,
11.2947380399339));
#62472=CARTESIAN_POINT('Ctrl Pts',(-0.8993225020166,-1.4521592870016,11.294062643499));
#62473=CARTESIAN_POINT('Ctrl Pts',(-0.913365468395192,-1.44390514150358,
11.2933871556582));
#62474=CARTESIAN_POINT('Ctrl Pts',(-0.922789553247202,-1.43836587255875,
11.2929338429778));
#62475=CARTESIAN_POINT('Ctrl Pts',(-0.932156968408698,-1.43273389293101,
11.2924808828034));
#62476=CARTESIAN_POINT('Ctrl Pts',(-0.941465939330546,-1.42701150822941,
11.2920283046203));
#62477=CARTESIAN_POINT('Ctrl Pts',(-0.997258564244995,-1.39271482109252,
11.2893158109378));
#62478=CARTESIAN_POINT('Ctrl Pts',(-1.05096555773083,-1.35516769400791,
11.2866164406656));
#62479=CARTESIAN_POINT('Ctrl Pts',(-1.10242222381511,-1.31470157532149,
11.2839256753843));
#62480=CARTESIAN_POINT('Ctrl Pts',(-1.15490559840975,-1.27342804116106,
11.2811812215953));
#62481=CARTESIAN_POINT('Ctrl Pts',(-1.20504870548191,-1.22911724367845,
11.2784457196118));
#62482=CARTESIAN_POINT('Ctrl Pts',(-1.25265335579406,-1.18207076364008,
11.2757143751156));
#62483=CARTESIAN_POINT('Ctrl Pts',(-1.28397500867159,-1.15111636092502,
11.2739172770666));
#62484=CARTESIAN_POINT('Ctrl Pts',(-1.31419725536704,-1.11897666094205,
11.2721219788063));
#62485=CARTESIAN_POINT('Ctrl Pts',(-1.34325581778868,-1.08572815742637,
11.2703271147686));
#62486=CARTESIAN_POINT('Ctrl Pts',(-1.36209363901681,-1.06417411919684,
11.2691635565932));
#62487=CARTESIAN_POINT('Ctrl Pts',(-1.38044228251278,-1.04215395727969,
11.2680001809021));
#62488=CARTESIAN_POINT('Ctrl Pts',(-1.39828252264694,-1.01968718394611,
11.2668366156616));
#62489=CARTESIAN_POINT('Ctrl Pts',(-1.40805056143521,-1.00738598666853,
11.2661995306046));
#62490=CARTESIAN_POINT('Ctrl Pts',(-1.41766921695113,-0.994946604236495,
11.2655621759649));
#62491=CARTESIAN_POINT('Ctrl Pts',(-1.42711662985222,-0.982397385607975,
11.264925758661));
#62492=CARTESIAN_POINT('Ctrl Pts',(-1.46820629310292,-0.927817028752221,
11.262157786839));
#62493=CARTESIAN_POINT('Ctrl Pts',(-1.50612185513061,-0.871087521735772,
11.2594035844773));
#62494=CARTESIAN_POINT('Ctrl Pts',(-1.54066769776793,-0.812525394359864,
11.2566583590267));
#62495=CARTESIAN_POINT('Ctrl Pts',(-1.57505516312501,-0.754231748217875,
11.2539257192103));
#62496=CARTESIAN_POINT('Ctrl Pts',(-1.60610442219133,-0.694121381542228,
11.2512019741836));
#62497=CARTESIAN_POINT('Ctrl Pts',(-1.63358497140864,-0.632471603998023,
11.2484823970106));
#62498=CARTESIAN_POINT('Ctrl Pts',(-1.65966108961598,-0.573972522557314,
11.2459018075444));
#62499=CARTESIAN_POINT('Ctrl Pts',(-1.68252420078453,-0.514086499095208,
11.2433249708101));
#62500=CARTESIAN_POINT('Ctrl Pts',(-1.70193725006908,-0.453031690747441,
11.2407478481942));
#62501=CARTESIAN_POINT('Ctrl Pts',(-1.70639988231082,-0.438996535720931,
11.2401554244947));
#62502=CARTESIAN_POINT('Ctrl Pts',(-1.71068001578898,-0.424899564800969,
11.239562985688));
#62503=CARTESIAN_POINT('Ctrl Pts',(-1.71477442803653,-0.410743347710776,
11.2389704827146));
#62504=CARTESIAN_POINT('Ctrl Pts',(-1.7181060933816,-0.399224288308597,
11.238488356953));
#62505=CARTESIAN_POINT('Ctrl Pts',(-1.72131496051192,-0.387664952239154,
11.2380061462914));
#62506=CARTESIAN_POINT('Ctrl Pts',(-1.72439513423882,-0.376083269559728,
11.2375245092466));
#62507=CARTESIAN_POINT('Ctrl Pts',(-1.73399637264737,-0.339981897872015,
11.2360231938976));
#62508=CARTESIAN_POINT('Ctrl Pts',(-1.74235845090443,-0.303626928305512,
11.234525913273));
#62509=CARTESIAN_POINT('Ctrl Pts',(-1.74944665354966,-0.267065873422436,
11.2330319031487));
#62510=CARTESIAN_POINT('Ctrl Pts',(-1.76197449586933,-0.202447076028902,
11.2303913574139));
#62511=CARTESIAN_POINT('Ctrl Pts',(-1.77052625497235,-0.137185361680741,
11.227761027999));
#62512=CARTESIAN_POINT('Ctrl Pts',(-1.77528061829343,-0.0715870718432795,
11.2251366955952));
#62513=CARTESIAN_POINT('Ctrl Pts',(-1.77697828156189,-0.0481635764959884,
11.2241996126621));
#62514=CARTESIAN_POINT('Ctrl Pts',(-1.7781912975682,-0.0246970169190114,
11.2232632943623));
#62515=CARTESIAN_POINT('Ctrl Pts',(-1.77892626630995,-0.00120095233929127,
11.2223275485995));
#62516=CARTESIAN_POINT('',(1.88128289424299,-0.51655738433239,11.046));
#62517=CARTESIAN_POINT('Ctrl Pts',(1.88079991776263,-0.516378774142054,
11.046));
#62518=CARTESIAN_POINT('Ctrl Pts',(1.89035995045861,-0.445151004206684,
11.0555631104642));
#62519=CARTESIAN_POINT('Ctrl Pts',(1.8961423315859,-0.373654493774377,11.0651669654983));
#62520=CARTESIAN_POINT('Ctrl Pts',(1.89809144951916,-0.302224012343752,
11.0748303404806));
#62521=CARTESIAN_POINT('Ctrl Pts',(1.89999077178002,-0.23261842246626,11.0842468375051));
#62522=CARTESIAN_POINT('Ctrl Pts',(1.89824990827702,-0.163074621232238,
11.0937198521185));
#62523=CARTESIAN_POINT('Ctrl Pts',(1.89277099599951,-0.0939167257851171,
11.1032667571406));
#62524=CARTESIAN_POINT('Ctrl Pts',(1.88910201129244,-0.0476047485319078,
11.1096598962807));
#62525=CARTESIAN_POINT('Ctrl Pts',(1.8837557967888,-0.00146614169388357,
11.1160861707414));
#62526=CARTESIAN_POINT('Ctrl Pts',(1.87669176161129,0.0443950771863014,
11.1225507975725));
#62527=CARTESIAN_POINT('Ctrl Pts',(1.87063241478827,0.0837336455737761,
11.1280959874063));
#62528=CARTESIAN_POINT('Ctrl Pts',(1.8633089856103,0.122868068816038,11.1336693960131));
#62529=CARTESIAN_POINT('Ctrl Pts',(1.85469071090361,0.161728394728602,11.1392743160301));
#62530=CARTESIAN_POINT('Ctrl Pts',(1.85223436103037,0.172804226014781,11.1408718103131));
#62531=CARTESIAN_POINT('Ctrl Pts',(1.84967323324123,0.183855475695868,11.142471538338));
#62532=CARTESIAN_POINT('Ctrl Pts',(1.84700939076218,0.19487013146115,11.1440720571876));
#62533=CARTESIAN_POINT('Ctrl Pts',(1.83137216521354,0.259528105007685,11.1534673853433));
#62534=CARTESIAN_POINT('Ctrl Pts',(1.81217652429567,0.323030635926077,11.1629048835303));
#62535=CARTESIAN_POINT('Ctrl Pts',(1.78934255453511,0.385087390709459,11.1724028038701));
#62536=CARTESIAN_POINT('Ctrl Pts',(1.78198218565347,0.405090947322401,11.1754643914102));
#62537=CARTESIAN_POINT('Ctrl Pts',(1.77424343060636,0.424944079046285,11.1785322571122));
#62538=CARTESIAN_POINT('Ctrl Pts',(1.76612263817241,0.444636415640588,11.181607012295));
#62539=CARTESIAN_POINT('Ctrl Pts',(1.73919119835162,0.509943216945239,11.1918039955137));
#62540=CARTESIAN_POINT('Ctrl Pts',(1.70806080167302,0.573485248201441,11.2020767507448));
#62541=CARTESIAN_POINT('Ctrl Pts',(1.67301702698032,0.634984575310704,11.2124475752393));
#62542=CARTESIAN_POINT('Ctrl Pts',(1.64235372412421,0.688796486531309,11.2215220466721));
#62543=CARTESIAN_POINT('Ctrl Pts',(1.60869302252863,0.741044106677185,11.2306716023846));
#62544=CARTESIAN_POINT('Ctrl Pts',(1.57220891785208,0.791506873950779,11.239911179793));
#62545=CARTESIAN_POINT('Ctrl Pts',(1.56528521292053,0.801083354276364,11.2416646038728));
#62546=CARTESIAN_POINT('Ctrl Pts',(1.55825911602623,0.81059620160376,11.2434214216921));
#62547=CARTESIAN_POINT('Ctrl Pts',(1.55114206425445,0.820030590825838,11.2451792455347));
#62548=CARTESIAN_POINT('Ctrl Pts',(1.51163333781795,0.872403499555923,11.254937412757));
#62549=CARTESIAN_POINT('Ctrl Pts',(1.46925448012712,0.922460374176763,11.2647444648472));
#62550=CARTESIAN_POINT('Ctrl Pts',(1.42425895086728,0.969999034377404,11.2746213834588));
#62551=CARTESIAN_POINT('Ctrl Pts',(1.37955552976012,1.01722907657888,11.2844341817346));
#62552=CARTESIAN_POINT('Ctrl Pts',(1.33226826113497,1.06197396880102,11.2943159423384));
#62553=CARTESIAN_POINT('Ctrl Pts',(1.28262305484525,1.10398985376236,11.3042872409362));
#62554=CARTESIAN_POINT('Ctrl Pts',(1.23402945162958,1.14511574274852,11.3140473238087));
#62555=CARTESIAN_POINT('Ctrl Pts',(1.18317581682196,1.18362727550242,11.3238931915966));
#62556=CARTESIAN_POINT('Ctrl Pts',(1.13026675802768,1.2192467284131,11.3338441399431));
#62557=CARTESIAN_POINT('Ctrl Pts',(1.11612186853279,1.22876935528969,11.3365044606506));
#62558=CARTESIAN_POINT('Ctrl Pts',(1.1018300740637,1.23808499004259,11.3391722917297));
#62559=CARTESIAN_POINT('Ctrl Pts',(1.0873953214649,1.24718768011963,11.3418480018757));
#62560=CARTESIAN_POINT('Ctrl Pts',(1.07843141524914,1.25284040326838,11.3435096039465));
#62561=CARTESIAN_POINT('Ctrl Pts',(1.06941317684967,1.25841040829158,11.3451740914355));
#62562=CARTESIAN_POINT('Ctrl Pts',(1.06035226952456,1.2638900735973,11.346839603865));
#62563=CARTESIAN_POINT('Ctrl Pts',(1.00742079701965,1.29590085828569,11.3565690958694));
#62564=CARTESIAN_POINT('Ctrl Pts',(0.952938092487177,1.32489391547385,11.3663514013733));
#62565=CARTESIAN_POINT('Ctrl Pts',(0.897108858642945,1.35066478023243,11.3762079140514));
#62566=CARTESIAN_POINT('Ctrl Pts',(0.842238965806958,1.37599281162795,11.3858950574554));
#62567=CARTESIAN_POINT('Ctrl Pts',(0.78606756226141,1.39820862213323,11.3956538796688));
#62568=CARTESIAN_POINT('Ctrl Pts',(0.72878604220227,1.41706842320411,11.4055046903548));
#62569=CARTESIAN_POINT('Ctrl Pts',(0.67317444208947,1.43537840719681,11.4150683217683));
#62570=CARTESIAN_POINT('Ctrl Pts',(0.616515828164059,1.45052520284418,11.4247186563809));
#62571=CARTESIAN_POINT('Ctrl Pts',(0.558993687390787,1.46223733220615,11.4344742788813));
#62572=CARTESIAN_POINT('Ctrl Pts',(0.539362537898783,1.46623444634835,11.4378036765901));
#62573=CARTESIAN_POINT('Ctrl Pts',(0.519630929867265,1.46983109384517,11.4411453373854));
#62574=CARTESIAN_POINT('Ctrl Pts',(0.499806597877626,1.47301514408983,11.4445));
#62575=CARTESIAN_POINT('',(1.56060797133591,1.17265290216009,11.046));
#62576=CARTESIAN_POINT('Origin',(0.,0.,11.046));
#62577=CARTESIAN_POINT('Ctrl Pts',(-1.77892626630995,-0.00120095233929127,
11.2223275485995));
#62578=CARTESIAN_POINT('Ctrl Pts',(-1.78091222637221,0.0622877965358305,
11.2197990686688));
#62579=CARTESIAN_POINT('Ctrl Pts',(-1.77941067542291,0.125992016111799,
11.2172747683064));
#62580=CARTESIAN_POINT('Ctrl Pts',(-1.77452381634337,0.189646102027163,
11.2147508586347));
#62581=CARTESIAN_POINT('Ctrl Pts',(-1.77287868795546,0.211074823838332,
11.2139012013432));
#62582=CARTESIAN_POINT('Ctrl Pts',(-1.7708495726434,0.232497857027148,11.2130515883281));
#62583=CARTESIAN_POINT('Ctrl Pts',(-1.76843936997923,0.253904972833394,
11.2122018750387));
#62584=CARTESIAN_POINT('Ctrl Pts',(-1.76712267121633,0.265599725029338,
11.2117376748892));
#62585=CARTESIAN_POINT('Ctrl Pts',(-1.76569197102713,0.277291668505868,
11.2112733675823));
#62586=CARTESIAN_POINT('Ctrl Pts',(-1.7641484990815,0.288972974548762,11.2108091738099));
#62587=CARTESIAN_POINT('Ctrl Pts',(-1.75515036560026,0.357072658062498,
11.2081030167356));
#62588=CARTESIAN_POINT('Ctrl Pts',(-1.74235696629666,0.42456963250346,11.2054102736121));
#62589=CARTESIAN_POINT('Ctrl Pts',(-1.72594903242932,0.491138664005795,
11.2027264834948));
#62590=CARTESIAN_POINT('Ctrl Pts',(-1.70928395222888,0.558750970212142,
11.2000006328234));
#62591=CARTESIAN_POINT('Ctrl Pts',(-1.68888999030711,0.625407040269523,
11.1972840179815));
#62592=CARTESIAN_POINT('Ctrl Pts',(-1.66490278446929,0.690766734877331,
11.1945719649831));
#62593=CARTESIAN_POINT('Ctrl Pts',(-1.64112198461878,0.755564019991226,
11.1918832487577));
#62594=CARTESIAN_POINT('Ctrl Pts',(-1.61380916520598,0.81908815011939,11.1891990162058));
#62595=CARTESIAN_POINT('Ctrl Pts',(-1.5830482712126,0.880993120829078,11.186514712963));
#62596=CARTESIAN_POINT('Ctrl Pts',(-1.57216641681974,0.902892382846704,
11.1855651242728));
#62597=CARTESIAN_POINT('Ctrl Pts',(-1.56085264019442,0.92458881232314,11.1846155267362));
#62598=CARTESIAN_POINT('Ctrl Pts',(-1.54910931637308,0.946066284278751,
11.1836657187303));
#62599=CARTESIAN_POINT('Ctrl Pts',(-1.54396572241992,0.955473450134084,
11.1832497013582));
#62600=CARTESIAN_POINT('Ctrl Pts',(-1.53874121405367,0.964835754579395,
11.1828337685169));
#62601=CARTESIAN_POINT('Ctrl Pts',(-1.5334404792476,0.974144495398925,11.18241823656));
#62602=CARTESIAN_POINT('Ctrl Pts',(-1.49854818334159,1.03541964895223,11.179682981066));
#62603=CARTESIAN_POINT('Ctrl Pts',(-1.46030493742689,1.09447092650475,11.1769608571821));
#62604=CARTESIAN_POINT('Ctrl Pts',(-1.41884997832206,1.15095727599886,11.1742472453603));
#62605=CARTESIAN_POINT('Ctrl Pts',(-1.37811238995456,1.20646613920276,11.1715805921112));
#62606=CARTESIAN_POINT('Ctrl Pts',(-1.33427285188376,1.25949901944966,11.1689221588738));
#62607=CARTESIAN_POINT('Ctrl Pts',(-1.28741864153,1.30971119589593,11.166267561795));
#62608=CARTESIAN_POINT('Ctrl Pts',(-1.26549062822221,1.33321075474058,11.1650251966024));
#62609=CARTESIAN_POINT('Ctrl Pts',(-1.24290170835111,1.35609210845284,11.1637836716393));
#62610=CARTESIAN_POINT('Ctrl Pts',(-1.21965775424868,1.37831740927343,11.1625425375316));
#62611=CARTESIAN_POINT('Ctrl Pts',(-1.19165584264812,1.40509215276722,11.1610473475387));
#62612=CARTESIAN_POINT('Ctrl Pts',(-1.16270333140537,1.43091488294274,11.1595527247918));
#62613=CARTESIAN_POINT('Ctrl Pts',(-1.13285929301872,1.45577404177113,11.1580578836196));
#62614=CARTESIAN_POINT('Ctrl Pts',(-1.12175109882477,1.46502682318719,11.1575014915585));
#62615=CARTESIAN_POINT('Ctrl Pts',(-1.11051936159011,1.47414607111053,11.156945069237));
#62616=CARTESIAN_POINT('Ctrl Pts',(-1.09916702235175,1.48313103947397,11.1563885761416));
#62617=CARTESIAN_POINT('Ctrl Pts',(-1.0900493418525,1.49034735578674,11.1559416262983));
#62618=CARTESIAN_POINT('Ctrl Pts',(-1.08085382696811,1.49747696130526,11.1554946319594));
#62619=CARTESIAN_POINT('Ctrl Pts',(-1.07159363370462,1.50451093778695,11.1550481251347));
#62620=CARTESIAN_POINT('Ctrl Pts',(-1.01611106549685,1.54665509923293,11.152372873695));
#62621=CARTESIAN_POINT('Ctrl Pts',(-0.958209601759993,1.58545013781557,
11.1497101571816));
#62622=CARTESIAN_POINT('Ctrl Pts',(-0.898278760372612,1.62088563165273,
11.1470556568828));
#62623=CARTESIAN_POINT('Ctrl Pts',(-0.837571419107242,1.65678024897295,
11.1443667632881));
#62624=CARTESIAN_POINT('Ctrl Pts',(-0.774780874239298,1.6892280755481,11.1416863001956));
#62625=CARTESIAN_POINT('Ctrl Pts',(-0.71027313016202,1.71817742298682,11.1390097788418));
#62626=CARTESIAN_POINT('Ctrl Pts',(-0.66261429365752,1.73956543207362,11.13703234349));
#62627=CARTESIAN_POINT('Ctrl Pts',(-0.614017264977652,1.75904301818697,
11.135057059686));
#62628=CARTESIAN_POINT('Ctrl Pts',(-0.56462073685077,1.77657345707156,11.1330821172509));
#62629=CARTESIAN_POINT('Ctrl Pts',(-0.539231747042784,1.78558380964183,
11.1320670298498));
#62630=CARTESIAN_POINT('Ctrl Pts',(-0.513631449727103,1.79407954038564,
11.1310520326313));
#62631=CARTESIAN_POINT('Ctrl Pts',(-0.487838223654543,1.802054170041,11.1300368798027));
#62632=CARTESIAN_POINT('Ctrl Pts',(-0.475799003301229,1.80577640018727,
11.1295630480858));
#62633=CARTESIAN_POINT('Ctrl Pts',(-0.463717747565173,1.80938508638487,
11.129089182467));
#62634=CARTESIAN_POINT('Ctrl Pts',(-0.451596312388482,1.81287949077367,
11.1286152579519));
#62635=CARTESIAN_POINT('Ctrl Pts',(-0.439480899976025,1.81637215890158,
11.1281415689151));
#62636=CARTESIAN_POINT('Ctrl Pts',(-0.427332434103985,1.81974856717366,
11.1276680985874));
#62637=CARTESIAN_POINT('Ctrl Pts',(-0.415160020480683,1.8230065701324,11.1271950974533));
#62638=CARTESIAN_POINT('Ctrl Pts',(-0.345659931193023,1.8416085913534,11.1244944316633));
#62639=CARTESIAN_POINT('Ctrl Pts',(-0.275309825422015,1.85637496302517,
11.1218062647546));
#62640=CARTESIAN_POINT('Ctrl Pts',(-0.204481476884407,1.86725830113956,
11.1191261497819));
#62641=CARTESIAN_POINT('Ctrl Pts',(-0.133579826115251,1.87815290272383,
11.1164432610836));
#62642=CARTESIAN_POINT('Ctrl Pts',(-0.0621979169225611,1.88515673586772,
11.1137684409964));
#62643=CARTESIAN_POINT('Ctrl Pts',(0.00930939936232982,1.88817434312463,
11.111097228754));
#62644=CARTESIAN_POINT('Ctrl Pts',(0.0795378313902503,1.89113798149254,
11.1084737902425));
#62645=CARTESIAN_POINT('Ctrl Pts',(0.149888204683991,1.89025686041538,11.1058538316796));
#62646=CARTESIAN_POINT('Ctrl Pts',(0.220026910137412,1.88539116319202,11.1032331273822));
#62647=CARTESIAN_POINT('Ctrl Pts',(0.236366392955163,1.88425765244837,11.1026226092302));
#62648=CARTESIAN_POINT('Ctrl Pts',(0.252694364144288,1.88290767750495,11.102012050607));
#62649=CARTESIAN_POINT('Ctrl Pts',(0.269006539233807,1.88133906123029,11.1014013980884));
#62650=CARTESIAN_POINT('Ctrl Pts',(0.280730896030037,1.88021162011471,11.1009624923038));
#62651=CARTESIAN_POINT('Ctrl Pts',(0.292446914187848,1.8789711508204,11.1005235443156));
#62652=CARTESIAN_POINT('Ctrl Pts',(0.304138944100939,1.87761870427971,11.1000850620809));
#62653=CARTESIAN_POINT('Ctrl Pts',(0.375822773838615,1.86932685519343,11.0973967277121));
#62654=CARTESIAN_POINT('Ctrl Pts',(0.446738242932316,1.85681796775178,11.0947208906731));
#62655=CARTESIAN_POINT('Ctrl Pts',(0.516529562716851,1.84000805096474,11.0920531719144));
#62656=CARTESIAN_POINT('Ctrl Pts',(0.584847521294231,1.82355300752536,11.0894417712386));
#62657=CARTESIAN_POINT('Ctrl Pts',(0.652089317501138,1.80297695165361,11.0868381496919));
#62658=CARTESIAN_POINT('Ctrl Pts',(0.718036401553849,1.77856692481578,11.084238199749));
#62659=CARTESIAN_POINT('Ctrl Pts',(0.785323202313169,1.75366100765569,11.0815854317561));
#62660=CARTESIAN_POINT('Ctrl Pts',(0.851262956271168,1.7247633139281,11.0789364860598));
#62661=CARTESIAN_POINT('Ctrl Pts',(0.915607648721953,1.6921267735849,11.0762869996812));
#62662=CARTESIAN_POINT('Ctrl Pts',(0.930631108062465,1.68450666199239,11.0756683868732));
#62663=CARTESIAN_POINT('Ctrl Pts',(0.945567515715628,1.67668252571399,11.0750497445899));
#62664=CARTESIAN_POINT('Ctrl Pts',(0.960413518624615,1.6686572293506,11.074431017298));
#62665=CARTESIAN_POINT('Ctrl Pts',(0.975205360081844,1.66066121101609,11.073814547258));
#62666=CARTESIAN_POINT('Ctrl Pts',(0.989912270604597,1.65246257743845,11.0731977870787));
#62667=CARTESIAN_POINT('Ctrl Pts',(1.00450295029956,1.6440805277344,11.0725818668126));
#62668=CARTESIAN_POINT('Ctrl Pts',(1.06739734574523,1.60794897253934,11.0699268888682));
#62669=CARTESIAN_POINT('Ctrl Pts',(1.12821828188749,1.56837054324493,11.0672840147147));
#62670=CARTESIAN_POINT('Ctrl Pts',(1.18673956352194,1.52565231730803,11.0646490274931));
#62671=CARTESIAN_POINT('Ctrl Pts',(1.24608357911593,1.48233352805146,11.0619769957398));
#62672=CARTESIAN_POINT('Ctrl Pts',(1.30306365724006,1.43578546725283,11.0593130742375));
#62673=CARTESIAN_POINT('Ctrl Pts',(1.35742307425591,1.38627866511896,11.056652865764));
#62674=CARTESIAN_POINT('Ctrl Pts',(1.41159294455999,1.3369444890372,11.0540019332135));
#62675=CARTESIAN_POINT('Ctrl Pts',(1.4631611896777,1.28467147000892,11.0513546878431));
#62676=CARTESIAN_POINT('Ctrl Pts',(1.51184108762766,1.22968809505141,11.0487067782687));
#62677=CARTESIAN_POINT('Ctrl Pts',(1.52842600119773,1.21095562929319,11.0478046532996));
#62678=CARTESIAN_POINT('Ctrl Pts',(1.54467532477781,1.19190827830405,11.0469024512351));
#62679=CARTESIAN_POINT('Ctrl Pts',(1.56057659382849,1.17255425406029,11.046));
#62680=CARTESIAN_POINT('',(-0.999999999999999,-1.22464679914735E-16,12.));
#62681=CARTESIAN_POINT('',(-1.5,-1.83697019872103E-16,11.5));
#62682=CARTESIAN_POINT('Origin',(0.,0.,12.));
#62683=CARTESIAN_POINT('Ctrl Pts',(1.13509973994371,-1.59049193030953,-0.230074082272069));
#62684=CARTESIAN_POINT('Ctrl Pts',(1.66385127640631,-1.21313337847033,-0.19303686544359));
#62685=CARTESIAN_POINT('Ctrl Pts',(2.30633516687349,0.103782615975306,-0.118962431786632));
#62686=CARTESIAN_POINT('Ctrl Pts',(1.16188988078006,1.99753850566951,-0.00785078130119459));
#62687=CARTESIAN_POINT('Ctrl Pts',(-1.04655428901899,2.05782953697956,0.103260869184242));
#62688=CARTESIAN_POINT('Ctrl Pts',(-2.29698075471667,0.238333788527267,
0.214372519669679));
#62689=CARTESIAN_POINT('Ctrl Pts',(-1.44613108848303,-1.80075271725216,
0.325484170155115));
#62690=CARTESIAN_POINT('Ctrl Pts',(0.727946961077783,-2.19149774367173,
0.436595820640553));
#62691=CARTESIAN_POINT('Ctrl Pts',(2.2359411788162,-0.57762978583554,0.547707471125989));
#62692=CARTESIAN_POINT('Ctrl Pts',(1.69827668332871,1.56494259322429,0.658819121611427));
#62693=CARTESIAN_POINT('Ctrl Pts',(-0.393188016825179,2.27560800163251,
0.769930772096863));
#62694=CARTESIAN_POINT('Ctrl Pts',(-2.12490816724285,0.90434536960108,0.881042422582301));
#62695=CARTESIAN_POINT('Ctrl Pts',(-1.9125222930514,-1.29434912039326,0.992154073067737));
#62696=CARTESIAN_POINT('Ctrl Pts',(0.0496630258143332,-2.30880650358359,
1.10326572355317));
#62697=CARTESIAN_POINT('Ctrl Pts',(1.96640931676781,-1.21090966106477,1.21437737403861));
#62698=CARTESIAN_POINT('Ctrl Pts',(2.08405785032279,0.994871990457256,1.32548902452405));
#62699=CARTESIAN_POINT('Ctrl Pts',(0.294968904732024,2.29042728261432,1.43660067500948));
#62700=CARTESIAN_POINT('Ctrl Pts',(-1.76399147035948,1.49043619583305,1.54771232549492));
#62701=CARTESIAN_POINT('Ctrl Pts',(-2.20904863824581,-0.673178902258552,
1.65882397598036));
#62702=CARTESIAN_POINT('Ctrl Pts',(-0.633012670336293,-2.22089176195486,
1.7699356264658));
#62703=CARTESIAN_POINT('Ctrl Pts',(1.52217643594786,-1.73667627565877,1.88104727695123));
#62704=CARTESIAN_POINT('Ctrl Pts',(2.28470258285089,0.336451535954383,1.99215892743667));
#62705=CARTESIAN_POINT('Ctrl Pts',(0.956918672404541,2.10175453516431,2.10327057792211));
#62706=CARTESIAN_POINT('Ctrl Pts',(-1.24636506047609,1.94412953698174,2.21438222840754));
#62707=CARTESIAN_POINT('Ctrl Pts',(-2.30932995110325,0.00779007092406014,
2.32549387889298));
#62708=CARTESIAN_POINT('Ctrl Pts',(-1.2594528285163,-1.93567664513544,2.43660552937842));
#62709=CARTESIAN_POINT('Ctrl Pts',(0.942717341349318,-2.1081625941051,2.54771717986386));
#62710=CARTESIAN_POINT('Ctrl Pts',(2.28238070382781,-0.351857683462,2.65882883034929));
#62711=CARTESIAN_POINT('Ctrl Pts',(1.53385834111148,1.72636731182735,2.76994048083473));
#62712=CARTESIAN_POINT('Ctrl Pts',(-0.618014955343493,2.22511191222357,
2.88105213132016));
#62713=CARTESIAN_POINT('Ctrl Pts',(-2.20445672440028,0.68806689849701,2.99216378180561));
#62714=CARTESIAN_POINT('Ctrl Pts',(-1.77400663329184,-1.47850125855229,
3.10327543229104));
#62715=CARTESIAN_POINT('Ctrl Pts',(0.279509811935462,-2.29236554058792,
3.21438708277648));
#62716=CARTESIAN_POINT('Ctrl Pts',(2.07729836817097,-1.00890881459812,3.32549873326191));
#62717=CARTESIAN_POINT('Ctrl Pts',(1.97453422882556,1.1976143309821,3.43661038374735));
#62718=CARTESIAN_POINT('Ctrl Pts',(0.0652379087403971,2.30842143506323,
3.54772203423278));
#62719=CARTESIAN_POINT('Ctrl Pts',(-1.90374559216213,1.30721774273047,3.65883368471823));
#62720=CARTESIAN_POINT('Ctrl Pts',(-2.13096254074055,-0.889979863001003,
3.76994533520366));
#62721=CARTESIAN_POINT('Ctrl Pts',(-0.408528604769679,-2.27292100295502,
3.8810569856891));
#62722=CARTESIAN_POINT('Ctrl Pts',(1.6876745272456,-1.57633124585981,3.99216863617453));
#62723=CARTESIAN_POINT('Ctrl Pts',(2.23979789625721,0.562468568463683,4.10328028665997));
#62724=CARTESIAN_POINT('Ctrl Pts',(0.742695215461042,2.18665711155622,4.21439193714541));
#62725=CARTESIAN_POINT('Ctrl Pts',(-1.43391090854028,1.81023893808443,4.32550358763085));
#62726=CARTESIAN_POINT('Ctrl Pts',(-2.29860956455329,-0.222395090620434,
4.43661523811628));
#62727=CARTESIAN_POINT('Ctrl Pts',(-1.06027445761331,-2.05155638019547,
4.54772688860172));
#62728=CARTESIAN_POINT('Ctrl Pts',(1.14812229735204,-2.00371672072451,4.65883853908716));
#62729=CARTESIAN_POINT('Ctrl Pts',(2.30608404475241,-0.122645363248325,
4.76995018957259));
#62730=CARTESIAN_POINT('Ctrl Pts',(1.35417351061808,1.87063615108022,4.88106184005803));
#62731=CARTESIAN_POINT('Ctrl Pts',(-0.83669150175529,2.1524434574405,4.99217349054346));
#62732=CARTESIAN_POINT('Ctrl Pts',(-2.26205440167697,0.464946653328952,
5.10328514102891));
#62733=CARTESIAN_POINT('Ctrl Pts',(-1.61782842764492,-1.64793709991974,
5.21439679151433));
#62734=CARTESIAN_POINT('Ctrl Pts',(0.506574022840452,-2.25309748257175,
5.32550844199978));
#62735=CARTESIAN_POINT('Ctrl Pts',(2.1675039941815,-0.796863816342033,5.43662009248521));
#62736=CARTESIAN_POINT('Ctrl Pts',(1.84535073495005,1.38843299139974,5.54773174297065));
#62737=CARTESIAN_POINT('Ctrl Pts',(-0.1651427104253,2.30343078727826,5.65884339345609));
#62738=CARTESIAN_POINT('Ctrl Pts',(-2.024544512798,1.1109838082922,5.76995504394152));
#62739=CARTESIAN_POINT('Ctrl Pts',(-2.03165894515671,-1.09791959503082,
5.88106669442697));
#62740=CARTESIAN_POINT('Ctrl Pts',(-0.179976902307884,-2.30231922661119,
5.99217834491239));
#62741=CARTESIAN_POINT('Ctrl Pts',(1.83636881720094,-1.40029106752845,6.10328999539785));
#62742=CARTESIAN_POINT('Ctrl Pts',(2.17259204728728,0.782885242326115,6.21440164588326));
#62743=CARTESIAN_POINT('Ctrl Pts',(0.521076907609949,2.24978762618687,6.32551329636872));
#62744=CARTESIAN_POINT('Ctrl Pts',(-1.60717962682088,1.6583242004264,6.43662494685413));
#62745=CARTESIAN_POINT('Ctrl Pts',(-2.26500243885858,-0.450365916286509,
6.5477365973396));
#62746=CARTESIAN_POINT('Ctrl Pts',(-0.850539171717745,-2.14700922773088,
6.65884824782501));
#62747=CARTESIAN_POINT('Ctrl Pts',(1.34209565723166,-1.87932029027199,6.76995989831046));
#62748=CARTESIAN_POINT('Ctrl Pts',(2.30682622449346,0.107788109627418,6.8810715487959));
#62749=CARTESIAN_POINT('Ctrl Pts',(1.16100547839306,1.99627948587589,6.99218319928133));
#62750=CARTESIAN_POINT('Ctrl Pts',(-1.04703729866327,2.05834360634882,7.10329484976677));
#62751=CARTESIAN_POINT('Ctrl Pts',(-2.29712931099768,0.237197038645086,
7.21440650025221));
#62752=CARTESIAN_POINT('Ctrl Pts',(-1.44554186745893,-1.80096480143545,
7.32551815073763));
#62753=CARTESIAN_POINT('Ctrl Pts',(0.72859438989827,-2.19139583863915,7.43662980122308));
#62754=CARTESIAN_POINT('Ctrl Pts',(2.23612826941383,-0.576884623911715,
7.5477414517085));
#62755=CARTESIAN_POINT('Ctrl Pts',(1.6977934979946,1.56542733614398,7.65885310219396));
#62756=CARTESIAN_POINT('Ctrl Pts',(-0.393879040694563,2.27550539615811,
7.76996475267938));
#62757=CARTESIAN_POINT('Ctrl Pts',(-2.12518549811472,0.903688057410859,
7.88107640316484));
#62758=CARTESIAN_POINT('Ctrl Pts',(-1.91212657747833,-1.29492758803799,
7.99218805365025));
#62759=CARTESIAN_POINT('Ctrl Pts',(0.0503667898133586,-2.30879377455661,
8.1032997041357));
#62760=CARTESIAN_POINT('Ctrl Pts',(1.96677879493939,-1.21030850518371,8.21441135462113));
#62761=CARTESIAN_POINT('Ctrl Pts',(2.08375418707704,0.995506903268707,8.32552300510658));
#62762=CARTESIAN_POINT('Ctrl Pts',(0.294270353677539,2.29051751091564,8.436634655592));
#62763=CARTESIAN_POINT('Ctrl Pts',(-1.76444601777748,1.4898978999011,8.54774630607746));
#62764=CARTESIAN_POINT('Ctrl Pts',(-2.2088431932234,-0.673852547682493,
8.65885795656288));
#62765=CARTESIAN_POINT('Ctrl Pts',(-0.632335256349382,-2.2210847899434,
8.76996960704833));
#62766=CARTESIAN_POINT('Ctrl Pts',(1.52270606837662,-1.73621188252162,8.88108125753376));
#62767=CARTESIAN_POINT('Ctrl Pts',(2.28459985995541,0.337148347205355,8.99219290801919));
#62768=CARTESIAN_POINT('Ctrl Pts',(0.956277562497704,2.10204633917866,9.10330455850463));
#62769=CARTESIAN_POINT('Ctrl Pts',(-1.2469579560031,1.94374924182257,9.21441620899007));
#62770=CARTESIAN_POINT('Ctrl Pts',(-2.30933226540692,0.00708579792413808,
9.32552785947551));
#62771=CARTESIAN_POINT('Ctrl Pts',(-1.25886228368054,-1.93606087509586,
9.43663950996094));
#62772=CARTESIAN_POINT('Ctrl Pts',(0.943360139257667,-2.10787462610152,
9.54775116044639));
#62773=CARTESIAN_POINT('Ctrl Pts',(2.28248823506631,-0.351162152961091,
9.65886281093181));
#62774=CARTESIAN_POINT('Ctrl Pts',(1.53333110744206,1.72683627576032,9.76997446141726));
#62775=CARTESIAN_POINT('Ctrl Pts',(-0.618692454411617,2.22492101746939,
9.88108611190268));
#62776=CARTESIAN_POINT('Ctrl Pts',(-2.20466868021367,0.687398848825245,
9.99219776238814));
#62777=CARTESIAN_POINT('Ctrl Pts',(-1.7735514221838,-1.47905058047522,10.1033094128735));
#62778=CARTESIAN_POINT('Ctrl Pts',(0.280201048116106,-2.29226437530741,
10.214421063359));
#62779=CARTESIAN_POINT('Ctrl Pts',(2.07762111854432,-1.0083052618152,10.3255327138444));
#62780=CARTESIAN_POINT('Ctrl Pts',(1.97414006873683,1.19827380577986,10.4366443643299));
#62781=CARTESIAN_POINT('Ctrl Pts',(0.0645886152005097,2.30833217918201,
10.5477560148153));
#62782=CARTESIAN_POINT('Ctrl Pts',(-1.90424854748374,1.30684465150768,10.6588676653008));
#62783=CARTESIAN_POINT('Ctrl Pts',(-2.13049227679005,-0.891025387309722,
10.7699793157862));
#62784=CARTESIAN_POINT('Ctrl Pts',(-0.408214485225542,-2.27228942196666,
10.8810909662716));
#62785=CARTESIAN_POINT('Ctrl Pts',(1.68888461736298,-1.5772814986318,10.9922026167571));
#62786=CARTESIAN_POINT('Ctrl Pts',(2.23817187934597,0.566161966084782,11.1033142672425));
#62787=CARTESIAN_POINT('Ctrl Pts',(1.24300218570944,1.64165746435707,11.1773887008995));
#62788=CARTESIAN_POINT('Ctrl Pts',(0.627850911123727,1.850383536838,11.2144259177279));
#62789=CARTESIAN_POINT('Ctrl Pts',(1.05793541951254,-1.4823699524473,-0.153382721514713));
#62790=CARTESIAN_POINT('Ctrl Pts',(1.55074231467859,-1.13066431478549,-0.116345504686234));
#62791=CARTESIAN_POINT('Ctrl Pts',(2.14955001436596,0.0967274517879858,
-0.0422710710292769));
#62792=CARTESIAN_POINT('Ctrl Pts',(1.08290436090784,1.86174541551099,0.0688405794561606));
#62793=CARTESIAN_POINT('Ctrl Pts',(-0.975409307071879,1.91793784975909,
0.179952229941597));
#62794=CARTESIAN_POINT('Ctrl Pts',(-2.14083151712633,0.22213180716797,0.291063880427034));
#62795=CARTESIAN_POINT('Ctrl Pts',(-1.34782279118508,-1.67833716661673,
0.402175530912471));
#62796=CARTESIAN_POINT('Ctrl Pts',(0.678460972679723,-2.04251926348523,
0.513287181397908));
#62797=CARTESIAN_POINT('Ctrl Pts',(2.08394142450739,-0.538362390807298,
0.624398831883346));
#62798=CARTESIAN_POINT('Ctrl Pts',(1.58282747515632,1.45855746470163,0.735510482368781));
#62799=CARTESIAN_POINT('Ctrl Pts',(-0.366459012269607,2.12091168831785,
0.84662213285422));
#62800=CARTESIAN_POINT('Ctrl Pts',(-1.98045646054783,0.842867780077688,
0.957733783339656));
#62801=CARTESIAN_POINT('Ctrl Pts',(-1.78250862301028,-1.20635899339281,
1.06884543382509));
#62802=CARTESIAN_POINT('Ctrl Pts',(0.0462869228141735,-2.15185334908375,
1.17995708431053));
#62803=CARTESIAN_POINT('Ctrl Pts',(1.83273239545565,-1.12859176615955,1.29106873479597));
#62804=CARTESIAN_POINT('Ctrl Pts',(1.94238315681312,0.927240382098824,1.4021803852814));
#62805=CARTESIAN_POINT('Ctrl Pts',(0.274916856192995,2.13472355144377,1.51329203576684));
#62806=CARTESIAN_POINT('Ctrl Pts',(-1.64407495706399,1.38911602796551,1.62440368625228));
#62807=CARTESIAN_POINT('Ctrl Pts',(-2.0588770445336,-0.62741605808422,1.73551533673771));
#62808=CARTESIAN_POINT('Ctrl Pts',(-0.589980335104445,-2.06991507018771,
1.84662698722315));
#62809=CARTESIAN_POINT('Ctrl Pts',(1.41869855984326,-1.61861665507704,1.95773863770859));
#62810=CARTESIAN_POINT('Ctrl Pts',(2.1293880179812,0.313579489369987,2.06885028819403));
#62811=CARTESIAN_POINT('Ctrl Pts',(0.891867138635642,1.95887681727571,2.17996193867946));
#62812=CARTESIAN_POINT('Ctrl Pts',(-1.16163690001897,1.8119671998123,2.2910735891649));
#62813=CARTESIAN_POINT('Ctrl Pts',(-2.1523412125303,0.0072605002547781,
2.40218523965033));
#62814=CARTESIAN_POINT('Ctrl Pts',(-1.1738349588193,-1.80408893734178,2.51329689013577));
#62815=CARTESIAN_POINT('Ctrl Pts',(0.878631217069615,-1.96484925501419,
2.62440854062121));
#62816=CARTESIAN_POINT('Ctrl Pts',(2.12722398078527,-0.327938323711113,
2.73552019110664));
#62817=CARTESIAN_POINT('Ctrl Pts',(1.42958632662274,1.60900849678758,2.84663184159209));
#62818=CARTESIAN_POINT('Ctrl Pts',(-0.57600216794938,2.07384833374845,2.95774349207752));
#62819=CARTESIAN_POINT('Ctrl Pts',(-2.05459728996263,0.641291965189069,
3.06885514256296));
#62820=CARTESIAN_POINT('Ctrl Pts',(-1.65340928710165,-1.37799243024573,
3.17996679304839));
#62821=CARTESIAN_POINT('Ctrl Pts',(0.260508675794864,-2.13653004623031,
3.29107844353384));
#62822=CARTESIAN_POINT('Ctrl Pts',(1.93608318568785,-0.940322979965331,
3.40219009401926));
#62823=CARTESIAN_POINT('Ctrl Pts',(1.84030497427301,1.11620025542831,3.51330174450471));
#62824=CARTESIAN_POINT('Ctrl Pts',(0.0608030219043116,2.15149445760286,
3.62441339499014));
#62825=CARTESIAN_POINT('Ctrl Pts',(-1.77432856410404,1.21835280406139,3.73552504547559));
#62826=CARTESIAN_POINT('Ctrl Pts',(-1.98609925645444,-0.829478843655077,
3.84663669596101));
#62827=CARTESIAN_POINT('Ctrl Pts',(-0.380756743800589,-2.11840735237885,
3.95774834644646));
#62828=CARTESIAN_POINT('Ctrl Pts',(1.57294605588646,-1.4691719143219,4.06885999693188));
#62829=CARTESIAN_POINT('Ctrl Pts',(2.08753596148093,0.524231836199493,4.17997164741733));
#62830=CARTESIAN_POINT('Ctrl Pts',(0.692206637610257,2.03800769856489,4.29108329790276));
#62831=CARTESIAN_POINT('Ctrl Pts',(-1.33643334165982,1.68717851215016,4.4021949483882));
#62832=CARTESIAN_POINT('Ctrl Pts',(-2.1423496001257,-0.207276625316418,
4.51330659887364));
#62833=CARTESIAN_POINT('Ctrl Pts',(-0.988196775702872,-1.91209114350017,
4.62441824935908));
#62834=CARTESIAN_POINT('Ctrl Pts',(1.07007270071357,-1.86750363419964,4.73552989984451));
#62835=CARTESIAN_POINT('Ctrl Pts',(2.1493159635798,-0.11430790551128,4.84664155032995));
#62836=CARTESIAN_POINT('Ctrl Pts',(1.26211650891535,1.74346990983058,4.95775320081538));
#62837=CARTESIAN_POINT('Ctrl Pts',(-0.779813036479037,2.00611989589323,
5.06886485130082));
#62838=CARTESIAN_POINT('Ctrl Pts',(-2.1082794649543,0.433339481484583,5.17997650178626));
#62839=CARTESIAN_POINT('Ctrl Pts',(-1.50784810891129,-1.53590998727594,
5.29108815227169));
#62840=CARTESIAN_POINT('Ctrl Pts',(0.472137013611209,-2.09993143910453,
5.40219980275713));
#62841=CARTESIAN_POINT('Ctrl Pts',(2.02015661416081,-0.742692845544967,
5.51331145324257));
#62842=CARTESIAN_POINT('Ctrl Pts',(1.71990340163759,1.29404702294652,5.62442310372801));
#62843=CARTESIAN_POINT('Ctrl Pts',(-0.153916274037652,2.14684307510999,
5.73553475421344));
#62844=CARTESIAN_POINT('Ctrl Pts',(-1.88691554856225,1.03545889399597,5.84664640469888));
#62845=CARTESIAN_POINT('Ctrl Pts',(-1.89354634030427,-1.02328278871562,
5.95775805518432));
#62846=CARTESIAN_POINT('Ctrl Pts',(-0.167742034418123,-2.1458070785722,
6.06886970566975));
#62847=CARTESIAN_POINT('Ctrl Pts',(1.71153207655705,-1.30509898455162,6.1799813561552));
#62848=CARTESIAN_POINT('Ctrl Pts',(2.02489878034016,0.729664537947597,6.29109300664062));
#62849=CARTESIAN_POINT('Ctrl Pts',(0.485653989206222,2.09684658745684,6.40220465712607));
#62850=CARTESIAN_POINT('Ctrl Pts',(-1.49792321581985,1.54559097049293,6.5133163076115));
#62851=CARTESIAN_POINT('Ctrl Pts',(-2.11102709394471,-0.41974994603061,
6.62442795809694));
#62852=CARTESIAN_POINT('Ctrl Pts',(-0.79271933890819,-2.0010550862688,6.73553960858237));
#62853=CARTESIAN_POINT('Ctrl Pts',(1.25085971055702,-1.7515636994031,6.84665125906781));
#62854=CARTESIAN_POINT('Ctrl Pts',(2.15000768978506,0.100460651134341,6.95776290955325));
#62855=CARTESIAN_POINT('Ctrl Pts',(1.08208008038219,1.86057198414926,7.06887456003868));
#62856=CARTESIAN_POINT('Ctrl Pts',(-0.975859481618359,1.91841697258389,
7.17998621052413));
#62857=CARTESIAN_POINT('Ctrl Pts',(-2.14096997451993,0.221072333783236,
7.29109786100956));
#62858=CARTESIAN_POINT('Ctrl Pts',(-1.34727362553083,-1.67853483327237,
7.402209511495));
#62859=CARTESIAN_POINT('Ctrl Pts',(0.679064389152043,-2.04242428597833,
7.51332116198043));
#62860=CARTESIAN_POINT('Ctrl Pts',(2.08411579664662,-0.537667885148679,
7.62443281246587));
#62861=CARTESIAN_POINT('Ctrl Pts',(1.58237713686343,1.4590092546951,7.73554446295131));
#62862=CARTESIAN_POINT('Ctrl Pts',(-0.367103060190181,2.1208160579853,7.84665611343674));
#62863=CARTESIAN_POINT('Ctrl Pts',(-1.98071493840836,0.842255152109201,
7.95776776392219));
#62864=CARTESIAN_POINT('Ctrl Pts',(-1.78213980826558,-1.20689813668469,
8.0688794144076));
#62865=CARTESIAN_POINT('Ctrl Pts',(0.0469428447876819,-2.15184148537872,
8.17999106489306));
#62866=CARTESIAN_POINT('Ctrl Pts',(1.83307675642296,-1.12803147698245,8.29110271537848));
#62867=CARTESIAN_POINT('Ctrl Pts',(1.94210013665906,0.927832133403047,8.40221436586394));
#62868=CARTESIAN_POINT('Ctrl Pts',(0.274265792786954,2.13480764600607,8.51332601634936));
#62869=CARTESIAN_POINT('Ctrl Pts',(-1.64449860425235,1.38861432550488,8.6244376668348));
#62870=CARTESIAN_POINT('Ctrl Pts',(-2.05868556570727,-0.628043908949741,
8.73554931732024));
#62871=CARTESIAN_POINT('Ctrl Pts',(-0.589348971863656,-2.07009497609277,
8.84666096780567));
#62872=CARTESIAN_POINT('Ctrl Pts',(1.41919218774748,-1.61818383148359,8.95777261829112));
#62873=CARTESIAN_POINT('Ctrl Pts',(2.12929227820989,0.314228931244718,9.06888426877654));
#62874=CARTESIAN_POINT('Ctrl Pts',(0.891269611515884,1.95914878439144,9.179995919262));
#62875=CARTESIAN_POINT('Ctrl Pts',(-1.16218949038264,1.81161275719849,9.29110756974741));
#62876=CARTESIAN_POINT('Ctrl Pts',(-2.15234336950711,0.00660410388236847,
9.40221922023287));
#62877=CARTESIAN_POINT('Ctrl Pts',(-1.17328455934639,-1.80444704726821,
9.51333087071829));
#62878=CARTESIAN_POINT('Ctrl Pts',(0.879230317440182,-1.96458086313641,
9.62444252120374));
#62879=CARTESIAN_POINT('Ctrl Pts',(2.12732420202743,-0.327290075520782,
9.73555417168917));
#62880=CARTESIAN_POINT('Ctrl Pts',(1.42909493440969,1.60944558045319,9.8466658221746));
#62881=CARTESIAN_POINT('Ctrl Pts',(-0.576633610487541,2.07367041606005,
9.95777747266004));
#62882=CARTESIAN_POINT('Ctrl Pts',(-2.05479483697499,0.640669329675303,
10.0688891231455));
#62883=CARTESIAN_POINT('Ctrl Pts',(-1.65298502134104,-1.37850440914814,
10.1800007736309));
#62884=CARTESIAN_POINT('Ctrl Pts',(0.26115292159373,-2.13643575818697,10.2911124241164));
#62885=CARTESIAN_POINT('Ctrl Pts',(1.93638399542254,-0.939760456828254,
10.4022240746018));
#62886=CARTESIAN_POINT('Ctrl Pts',(1.83993760927049,1.11681489898982,10.5133357250872));
#62887=CARTESIAN_POINT('Ctrl Pts',(0.0601978674766102,2.15141126935532,
10.6244473755726));
#62888=CARTESIAN_POINT('Ctrl Pts',(-1.77479732841649,1.21800507565884,10.7355590260581));
#62889=CARTESIAN_POINT('Ctrl Pts',(-1.98566096114678,-0.830453293000129,
10.8466706765435));
#62890=CARTESIAN_POINT('Ctrl Pts',(-0.380463978169507,-2.11781870639967,
10.957782327029));
#62891=CARTESIAN_POINT('Ctrl Pts',(1.57407388382168,-1.47005756870945,11.0688939775144));
#62892=CARTESIAN_POINT('Ctrl Pts',(2.08602048154327,0.527674155869038,11.1800056279999));
#62893=CARTESIAN_POINT('Ctrl Pts',(1.15850263419028,1.53005724266717,11.2540800616568));
#62894=CARTESIAN_POINT('Ctrl Pts',(0.585169473375027,1.72459407258861,11.2911172784853));
#62895=CARTESIAN_POINT('Ctrl Pts',(0.980771099081375,-1.37424797458507,
-0.0766913607573581));
#62896=CARTESIAN_POINT('Ctrl Pts',(1.43763335295088,-1.04819525110066,-0.0396541439288791));
#62897=CARTESIAN_POINT('Ctrl Pts',(1.99276486185844,0.089672287600667,0.0344202897280782));
#62898=CARTESIAN_POINT('Ctrl Pts',(1.00391884103562,1.72595232535247,0.145531940213516));
#62899=CARTESIAN_POINT('Ctrl Pts',(-0.904264325124765,1.77804616253862,
0.256643590698952));
#62900=CARTESIAN_POINT('Ctrl Pts',(-1.98468227953599,0.20592982580867,0.36775524118439));
#62901=CARTESIAN_POINT('Ctrl Pts',(-1.24951449388714,-1.55592161598129,
0.478866891669827));
#62902=CARTESIAN_POINT('Ctrl Pts',(0.628974984281669,-1.89354078329874,
0.589978542155263));
#62903=CARTESIAN_POINT('Ctrl Pts',(1.93194167019859,-0.499094995779056,
0.7010901926407));
#62904=CARTESIAN_POINT('Ctrl Pts',(1.46737826698393,1.35217233617898,0.812201843126137));
#62905=CARTESIAN_POINT('Ctrl Pts',(-0.339730007714042,1.96621537500318,
0.923313493611574));
#62906=CARTESIAN_POINT('Ctrl Pts',(-1.8360047538528,0.7813901905543,1.03442514409701));
#62907=CARTESIAN_POINT('Ctrl Pts',(-1.65249495296916,-1.11836886639236,
1.14553679458245));
#62908=CARTESIAN_POINT('Ctrl Pts',(0.0429108198140191,-1.99490019458391,
1.25664844506789));
#62909=CARTESIAN_POINT('Ctrl Pts',(1.69905547414348,-1.04627387125433,1.36776009555332));
#62910=CARTESIAN_POINT('Ctrl Pts',(1.80070846330345,0.859608773740392,1.47887174603876));
#62911=CARTESIAN_POINT('Ctrl Pts',(0.254864807653961,1.97901982027321,1.5899833965242));
#62912=CARTESIAN_POINT('Ctrl Pts',(-1.52415844376849,1.28779586009797,1.70109504700963));
#62913=CARTESIAN_POINT('Ctrl Pts',(-1.90870545082139,-0.581653213909888,
1.81220669749507));
#62914=CARTESIAN_POINT('Ctrl Pts',(-0.546947999872595,-1.91893837842057,
1.92331834798051));
#62915=CARTESIAN_POINT('Ctrl Pts',(1.31522068373867,-1.50055703449532,2.03442999846594));
#62916=CARTESIAN_POINT('Ctrl Pts',(1.97407345311151,0.290707442785592,2.14554164895138));
#62917=CARTESIAN_POINT('Ctrl Pts',(0.826815604866742,1.81599909938712,2.25665329943681));
#62918=CARTESIAN_POINT('Ctrl Pts',(-1.07690873956185,1.67980486264285,2.36776494992226));
#62919=CARTESIAN_POINT('Ctrl Pts',(-1.99535247395734,0.00673092958549589,
2.47887660040769));
#62920=CARTESIAN_POINT('Ctrl Pts',(-1.0882170891223,-1.67250122954812,2.58998825089313));
#62921=CARTESIAN_POINT('Ctrl Pts',(0.814545092789914,-1.82153591592328,
2.70109990137857));
#62922=CARTESIAN_POINT('Ctrl Pts',(1.97206725774273,-0.304018963960226,
2.812211551864));
#62923=CARTESIAN_POINT('Ctrl Pts',(1.325314312134,1.49164968174781,2.92332320234944));
#62924=CARTESIAN_POINT('Ctrl Pts',(-0.533989380555266,1.92258475527334,
3.03443485283487));
#62925=CARTESIAN_POINT('Ctrl Pts',(-1.90473785552499,0.594517031881129,
3.14554650332031));
#62926=CARTESIAN_POINT('Ctrl Pts',(-1.53281194091147,-1.27748360193918,
3.25665815380575));
#62927=CARTESIAN_POINT('Ctrl Pts',(0.241507539654265,-1.98069455187271,
3.36776980429119));
#62928=CARTESIAN_POINT('Ctrl Pts',(1.79486800320472,-0.871737145332536,
3.47888145477662));
#62929=CARTESIAN_POINT('Ctrl Pts',(1.70607571972046,1.03478617987453,3.58999310526206));
#62930=CARTESIAN_POINT('Ctrl Pts',(0.0563681350682242,1.99456748014249,
3.7011047557475));
#62931=CARTESIAN_POINT('Ctrl Pts',(-1.64491153604594,1.1294878653923,3.81221640623293));
#62932=CARTESIAN_POINT('Ctrl Pts',(-1.84123597216834,-0.768977824309152,
3.92332805671837));
#62933=CARTESIAN_POINT('Ctrl Pts',(-0.352984882831497,-1.96389370180267,
4.03443970720381));
#62934=CARTESIAN_POINT('Ctrl Pts',(1.45821758452731,-1.36201258278399,4.14555135768924));
#62935=CARTESIAN_POINT('Ctrl Pts',(1.93527402670466,0.485995103935303,4.25666300817468));
#62936=CARTESIAN_POINT('Ctrl Pts',(0.641718059759468,1.88935828557357,4.36777465866012));
#62937=CARTESIAN_POINT('Ctrl Pts',(-1.23895577477937,1.56411808621589,4.47888630914555));
#62938=CARTESIAN_POINT('Ctrl Pts',(-1.98608963569812,-0.1921581600124,4.58999795963099));
#62939=CARTESIAN_POINT('Ctrl Pts',(-0.916119093792434,-1.77262590680487,
4.70110961011643));
#62940=CARTESIAN_POINT('Ctrl Pts',(0.992023104075105,-1.73129054767478,
4.81222126060186));
#62941=CARTESIAN_POINT('Ctrl Pts',(1.99254788240719,-0.105970447774237,
4.9233329110873));
#62942=CARTESIAN_POINT('Ctrl Pts',(1.17005950721263,1.61630366858093,5.03444456157274));
#62943=CARTESIAN_POINT('Ctrl Pts',(-0.722934571202785,1.85979633434597,
5.14555621205818));
#62944=CARTESIAN_POINT('Ctrl Pts',(-1.95450452823164,0.401732309640217,
5.25666786254361));
#62945=CARTESIAN_POINT('Ctrl Pts',(-1.39786779017765,-1.42388287463214,
5.36777951302905));
#62946=CARTESIAN_POINT('Ctrl Pts',(0.437700004381964,-1.9467653956373,5.47889116351449));
#62947=CARTESIAN_POINT('Ctrl Pts',(1.87280923414012,-0.688521874747905,
5.59000281399993));
#62948=CARTESIAN_POINT('Ctrl Pts',(1.59445606832513,1.19966105449332,5.70111446448536));
#62949=CARTESIAN_POINT('Ctrl Pts',(-0.142689837650004,1.99025536294172,
5.81222611497081));
#62950=CARTESIAN_POINT('Ctrl Pts',(-1.74928658432651,0.959933979699734,
5.92333776545623));
#62951=CARTESIAN_POINT('Ctrl Pts',(-1.75543373545183,-0.948645982400418,
6.03444941594168));
#62952=CARTESIAN_POINT('Ctrl Pts',(-0.155507166528361,-1.98929493053321,
6.1455610664271));
#62953=CARTESIAN_POINT('Ctrl Pts',(1.58669533591315,-1.20990690157479,6.25667271691256));
#62954=CARTESIAN_POINT('Ctrl Pts',(1.87720551339304,0.676443833569079,6.36778436739797));
#62955=CARTESIAN_POINT('Ctrl Pts',(0.450231070802491,1.94390554872681,6.47889601788343));
#62956=CARTESIAN_POINT('Ctrl Pts',(-1.38866680481881,1.43285774055946,6.59000766836885));
#62957=CARTESIAN_POINT('Ctrl Pts',(-1.95705174903083,-0.38913397577471,
6.7011193188543));
#62958=CARTESIAN_POINT('Ctrl Pts',(-0.734899506098636,-1.85510094480672,
6.81223096933973));
#62959=CARTESIAN_POINT('Ctrl Pts',(1.15962376388238,-1.62380710853421,6.92334261982516));
#62960=CARTESIAN_POINT('Ctrl Pts',(1.99318915507666,0.0931331926412601,
7.03445427031061));
#62961=CARTESIAN_POINT('Ctrl Pts',(1.00315468237132,1.72486448242263,7.14556592079604));
#62962=CARTESIAN_POINT('Ctrl Pts',(-0.904681664573454,1.77849033881895,
7.25667757128148));
#62963=CARTESIAN_POINT('Ctrl Pts',(-1.98481063804218,0.204947628921387,
7.36778922176691));
#62964=CARTESIAN_POINT('Ctrl Pts',(-1.24900538360275,-1.55610486510929,
7.47890087225236));
#62965=CARTESIAN_POINT('Ctrl Pts',(0.629534388405818,-1.89345273331751,
7.59001252273779));
#62966=CARTESIAN_POINT('Ctrl Pts',(1.93210332387941,-0.498451146385645,
7.70112417322323));
#62967=CARTESIAN_POINT('Ctrl Pts',(1.46696077573226,1.35259117324623,7.81223582370866));
#62968=CARTESIAN_POINT('Ctrl Pts',(-0.340327079685797,1.96612671981249,
7.9233474741941));
#62969=CARTESIAN_POINT('Ctrl Pts',(-1.836244378702,0.780822246807544,8.03445912467955));
#62970=CARTESIAN_POINT('Ctrl Pts',(-1.65215303905282,-1.11886868533138,
8.14557077516496));
#62971=CARTESIAN_POINT('Ctrl Pts',(0.0435188997620014,-1.99488919620082,
8.25668242565042));
#62972=CARTESIAN_POINT('Ctrl Pts',(1.69937471790653,-1.04575444878119,8.36779407613584));
#62973=CARTESIAN_POINT('Ctrl Pts',(1.80044608624107,0.860157363537389,8.47890572662129));
#62974=CARTESIAN_POINT('Ctrl Pts',(0.254261231896373,1.97909778109651,8.59001737710672));
#62975=CARTESIAN_POINT('Ctrl Pts',(-1.52455119072723,1.28733075110866,8.70112902759215));
#62976=CARTESIAN_POINT('Ctrl Pts',(-1.90852793819114,-0.58223527021699,
8.8122406780776));
#62977=CARTESIAN_POINT('Ctrl Pts',(-0.546362687377931,-1.91910516224214,
8.92335232856302));
#62978=CARTESIAN_POINT('Ctrl Pts',(1.31567830711834,-1.50015578044556,9.03446397904849));
#62979=CARTESIAN_POINT('Ctrl Pts',(1.97398469646436,0.291309515284085,9.14557562953389));
#62980=CARTESIAN_POINT('Ctrl Pts',(0.826261660534066,1.81625122960423,9.25668728001935));
#62981=CARTESIAN_POINT('Ctrl Pts',(-1.07742102476217,1.67947627257441,9.36779893050478));
#62982=CARTESIAN_POINT('Ctrl Pts',(-1.99535447360731,0.00612240984059651,
9.47891058099021));
#62983=CARTESIAN_POINT('Ctrl Pts',(-1.08770683501224,-1.67283321944057,
9.59002223147566));
#62984=CARTESIAN_POINT('Ctrl Pts',(0.815100495622697,-1.82128710017129,
9.70113388196108));
#62985=CARTESIAN_POINT('Ctrl Pts',(1.97216016898856,-0.303417998080474,
9.81224553244654));
#62986=CARTESIAN_POINT('Ctrl Pts',(1.32485876137733,1.49205488514605,9.92335718293196));
#62987=CARTESIAN_POINT('Ctrl Pts',(-0.534574766563464,1.9224198146507,10.0344688334174));
#62988=CARTESIAN_POINT('Ctrl Pts',(-1.90492099373632,0.593939810525364,
10.1455804839028));
#62989=CARTESIAN_POINT('Ctrl Pts',(-1.53241862049827,-1.27795823782107,
10.2566921343883));
#62990=CARTESIAN_POINT('Ctrl Pts',(0.242104795071353,-1.98060714106653,
10.3678037848737));
#62991=CARTESIAN_POINT('Ctrl Pts',(1.79514687230076,-0.871215651841315,
10.4789154353591));
#62992=CARTESIAN_POINT('Ctrl Pts',(1.70573514980415,1.03535599219979,10.5900270858446));
#62993=CARTESIAN_POINT('Ctrl Pts',(0.055807119752709,1.99449035952863,10.70113873633));
#62994=CARTESIAN_POINT('Ctrl Pts',(-1.64534610934924,1.12916549981001,10.8122503868155));
#62995=CARTESIAN_POINT('Ctrl Pts',(-1.84082964550351,-0.769881198690536,
10.9233620373009));
#62996=CARTESIAN_POINT('Ctrl Pts',(-0.352713471113472,-1.96334799083268,
11.0344736877863));
#62997=CARTESIAN_POINT('Ctrl Pts',(1.45926315028039,-1.36283363878709,11.1455853382718));
#62998=CARTESIAN_POINT('Ctrl Pts',(1.93386908374058,0.489186345653294,11.2566969887572));
#62999=CARTESIAN_POINT('Ctrl Pts',(1.07400308267113,1.41845702097726,11.3307714224142));
#63000=CARTESIAN_POINT('Ctrl Pts',(0.542488035626326,1.59880460833922,11.3678086392426));
#63001=CARTESIAN_POINT('Ctrl Pts',(0.903606778650208,-1.26612599672284,
-2.77555756156289E-15));
#63002=CARTESIAN_POINT('Ctrl Pts',(1.32452439122316,-0.965726187415828,
0.0370372168284762));
#63003=CARTESIAN_POINT('Ctrl Pts',(1.83597970935092,0.0826171234133487,
0.111111650485434));
#63004=CARTESIAN_POINT('Ctrl Pts',(0.924933321163406,1.59015923519395,0.222223300970871));
#63005=CARTESIAN_POINT('Ctrl Pts',(-0.833119343177651,1.63815447531815,
0.333334951456308));
#63006=CARTESIAN_POINT('Ctrl Pts',(-1.82853304194564,0.18972784444937,0.444446601941745));
#63007=CARTESIAN_POINT('Ctrl Pts',(-1.15120619658919,-1.43350606534586,
0.555558252427182));
#63008=CARTESIAN_POINT('Ctrl Pts',(0.579488995883613,-1.74456230311225,
0.666669902912619));
#63009=CARTESIAN_POINT('Ctrl Pts',(1.77994191588978,-0.459827600750814,
0.777781553398056));
#63010=CARTESIAN_POINT('Ctrl Pts',(1.35192905881154,1.24578720765632,0.888893203883492));
#63011=CARTESIAN_POINT('Ctrl Pts',(-0.313001003158473,1.81151906168851,
1.00000485436893));
#63012=CARTESIAN_POINT('Ctrl Pts',(-1.69155304715778,0.719912601030908,
1.11111650485437));
#63013=CARTESIAN_POINT('Ctrl Pts',(-1.52248128292804,-1.03037873939191,
1.2222281553398));
#63014=CARTESIAN_POINT('Ctrl Pts',(0.0395347168138628,-1.83794704008407,
1.33333980582524));
#63015=CARTESIAN_POINT('Ctrl Pts',(1.56537855283131,-0.963955976349113,
1.44445145631068));
#63016=CARTESIAN_POINT('Ctrl Pts',(1.65903376979378,0.791977165381959,1.55556310679611));
#63017=CARTESIAN_POINT('Ctrl Pts',(0.234812759114929,1.82331608910266,1.66667475728155));
#63018=CARTESIAN_POINT('Ctrl Pts',(-1.404241930473,1.18647569223042,1.77778640776699));
#63019=CARTESIAN_POINT('Ctrl Pts',(-1.75853385710917,-0.535890369735552,
1.88889805825242));
#63020=CARTESIAN_POINT('Ctrl Pts',(-0.503915664640746,-1.76796168665343,
2.00000970873786));
#63021=CARTESIAN_POINT('Ctrl Pts',(1.21174280763407,-1.38249741391359,2.1111213592233));
#63022=CARTESIAN_POINT('Ctrl Pts',(1.81875888824183,0.267835396201195,2.22223300970874));
#63023=CARTESIAN_POINT('Ctrl Pts',(0.761764071097843,1.67312138149853,2.33334466019417));
#63024=CARTESIAN_POINT('Ctrl Pts',(-0.992180579104728,1.54764252547341,
2.44445631067961));
#63025=CARTESIAN_POINT('Ctrl Pts',(-1.83836373538439,0.00620135891621234,
2.55556796116504));
#63026=CARTESIAN_POINT('Ctrl Pts',(-1.0025992194253,-1.54091352175446,2.66667961165049));
#63027=CARTESIAN_POINT('Ctrl Pts',(0.750458968510211,-1.67822257683237,
2.77779126213592));
#63028=CARTESIAN_POINT('Ctrl Pts',(1.81691053470019,-0.280099604209337,
2.88890291262136));
#63029=CARTESIAN_POINT('Ctrl Pts',(1.22104229764526,1.37429086670804,3.0000145631068));
#63030=CARTESIAN_POINT('Ctrl Pts',(-0.491976593161155,1.77132117679823,
3.11112621359223));
#63031=CARTESIAN_POINT('Ctrl Pts',(-1.75487842108734,0.547742098573187,
3.22223786407767));
#63032=CARTESIAN_POINT('Ctrl Pts',(-1.41221459472129,-1.17697477363263,
3.3333495145631));
#63033=CARTESIAN_POINT('Ctrl Pts',(0.222506403513669,-1.8248590575151,3.44446116504855));
#63034=CARTESIAN_POINT('Ctrl Pts',(1.65365282072159,-0.803151310699741,
3.55557281553397));
#63035=CARTESIAN_POINT('Ctrl Pts',(1.57184646516792,0.953372104320743,3.66668446601942));
#63036=CARTESIAN_POINT('Ctrl Pts',(0.0519332482321354,1.83764050268212,
3.77779611650485));
#63037=CARTESIAN_POINT('Ctrl Pts',(-1.51549450798785,1.04062292672322,3.88890776699029));
#63038=CARTESIAN_POINT('Ctrl Pts',(-1.69637268788223,-0.708476804963227,
4.00001941747572));
#63039=CARTESIAN_POINT('Ctrl Pts',(-0.325213021862407,-1.80938005122649,
4.11113106796117));
#63040=CARTESIAN_POINT('Ctrl Pts',(1.34348911316817,-1.25485325124609,4.2222427184466));
#63041=CARTESIAN_POINT('Ctrl Pts',(1.78301209192838,0.447758371671112,4.33335436893204));
#63042=CARTESIAN_POINT('Ctrl Pts',(0.591229481908682,1.74070887258225,4.44446601941748));
#63043=CARTESIAN_POINT('Ctrl Pts',(-1.14147820789891,1.44105766028162,4.55557766990291));
#63044=CARTESIAN_POINT('Ctrl Pts',(-1.82982967127054,-0.177039694708382,
4.66668932038835));
#63045=CARTESIAN_POINT('Ctrl Pts',(-0.844041411881997,-1.63316067010957,
4.77780097087378));
#63046=CARTESIAN_POINT('Ctrl Pts',(0.913973507436636,-1.59507746114991,
4.88891262135923));
#63047=CARTESIAN_POINT('Ctrl Pts',(1.83577980123458,-0.0976329900371924,
5.00002427184466));
#63048=CARTESIAN_POINT('Ctrl Pts',(1.0780025055099,1.48913742733129,5.1111359223301));
#63049=CARTESIAN_POINT('Ctrl Pts',(-0.666056105926533,1.7134727727987,5.22224757281553));
#63050=CARTESIAN_POINT('Ctrl Pts',(-1.80072959150898,0.37012513779585,5.33335922330097));
#63051=CARTESIAN_POINT('Ctrl Pts',(-1.28788747144402,-1.31185576198834,
5.44447087378641));
#63052=CARTESIAN_POINT('Ctrl Pts',(0.403262995152723,-1.79359935217008,
5.55558252427184));
#63053=CARTESIAN_POINT('Ctrl Pts',(1.72546185411942,-0.634350903950841,
5.66669417475728));
#63054=CARTESIAN_POINT('Ctrl Pts',(1.46900873501267,1.1052750860401,5.77780582524271));
#63055=CARTESIAN_POINT('Ctrl Pts',(-0.13146340126236,1.83366765077345,5.88891747572816));
#63056=CARTESIAN_POINT('Ctrl Pts',(-1.61165762009075,0.884409065403499,
6.00002912621358));
#63057=CARTESIAN_POINT('Ctrl Pts',(-1.6173211305994,-0.87400917608522,6.11114077669903));
#63058=CARTESIAN_POINT('Ctrl Pts',(-0.143272298638598,-1.83278278249422,
6.22225242718446));
#63059=CARTESIAN_POINT('Ctrl Pts',(1.46185859526926,-1.11471481859797,6.33336407766989));
#63060=CARTESIAN_POINT('Ctrl Pts',(1.72951224644592,0.623223129190563,6.44447572815534));
#63061=CARTESIAN_POINT('Ctrl Pts',(0.414808152398764,1.79096450999678,6.55558737864077));
#63062=CARTESIAN_POINT('Ctrl Pts',(-1.27941039381778,1.320124510626,6.66669902912621));
#63063=CARTESIAN_POINT('Ctrl Pts',(-1.80307640411694,-0.358518005518811,
6.77781067961165));
#63064=CARTESIAN_POINT('Ctrl Pts',(-0.677079673289082,-1.70914680334463,
6.8889223300971));
#63065=CARTESIAN_POINT('Ctrl Pts',(1.06838781720774,-1.49605051766532,7.00003398058251));
#63066=CARTESIAN_POINT('Ctrl Pts',(1.83637062036826,0.0858057341481814,
7.11114563106797));
#63067=CARTESIAN_POINT('Ctrl Pts',(0.924229284360448,1.589156980696,7.22225728155339));
#63068=CARTESIAN_POINT('Ctrl Pts',(-0.833503847528551,1.63856370505402,
7.33336893203883));
#63069=CARTESIAN_POINT('Ctrl Pts',(-1.82865130156443,0.188822924059537,
7.44448058252428));
#63070=CARTESIAN_POINT('Ctrl Pts',(-1.15073714167466,-1.43367489694622,
7.5555922330097));
#63071=CARTESIAN_POINT('Ctrl Pts',(0.580004387659595,-1.74448118065669,
7.66670388349515));
#63072=CARTESIAN_POINT('Ctrl Pts',(1.7800908511122,-0.459234407622611,7.77781553398057));
#63073=CARTESIAN_POINT('Ctrl Pts',(1.35154441460109,1.24617309179735,7.88892718446602));
#63074=CARTESIAN_POINT('Ctrl Pts',(-0.313551099181417,1.81143738163968,
8.00003883495145));
#63075=CARTESIAN_POINT('Ctrl Pts',(-1.69177381899564,0.719389341505889,
8.11115048543689));
#63076=CARTESIAN_POINT('Ctrl Pts',(-1.52216626984007,-1.03083923397808,
8.22226213592232));
#63077=CARTESIAN_POINT('Ctrl Pts',(0.0400949547363229,-1.83793690702293,
8.33337378640777));
#63078=CARTESIAN_POINT('Ctrl Pts',(1.56567267939011,-0.963477420579929,
8.44448543689319));
#63079=CARTESIAN_POINT('Ctrl Pts',(1.65879203582308,0.792482593671729,8.55559708737864));
#63080=CARTESIAN_POINT('Ctrl Pts',(0.234256671005791,1.82338791618694,8.66670873786407));
#63081=CARTESIAN_POINT('Ctrl Pts',(-1.40460377720211,1.18604717671243,8.77782038834951));
#63082=CARTESIAN_POINT('Ctrl Pts',(-1.75837031067501,-0.536426631484242,
8.88893203883495));
#63083=CARTESIAN_POINT('Ctrl Pts',(-0.503376402892206,-1.7681153483915,
9.00004368932038));
#63084=CARTESIAN_POINT('Ctrl Pts',(1.2121644264892,-1.38212772940753,9.11115533980582));
#63085=CARTESIAN_POINT('Ctrl Pts',(1.81867711471885,0.26839009932345,9.22226699029127));
#63086=CARTESIAN_POINT('Ctrl Pts',(0.761253709552246,1.67335367481701,9.33337864077668));
#63087=CARTESIAN_POINT('Ctrl Pts',(-0.99265255914171,1.54733978795034,9.44449029126215));
#63088=CARTESIAN_POINT('Ctrl Pts',(-1.8383655777075,0.00564071579882353,
9.55560194174756));
#63089=CARTESIAN_POINT('Ctrl Pts',(-1.00212911067809,-1.54121939161292,
9.66671359223301));
#63090=CARTESIAN_POINT('Ctrl Pts',(0.750970673805211,-1.67799333720618,
9.77782524271844));
#63091=CARTESIAN_POINT('Ctrl Pts',(1.81699613594968,-0.279545920640164,
9.88893689320389));
#63092=CARTESIAN_POINT('Ctrl Pts',(1.22062258834496,1.37466418983892,10.0000485436893));
#63093=CARTESIAN_POINT('Ctrl Pts',(-0.492515922639386,1.77116921324136,
10.1111601941748));
#63094=CARTESIAN_POINT('Ctrl Pts',(-1.75504715049764,0.547210291375423,
10.2222718446602));
#63095=CARTESIAN_POINT('Ctrl Pts',(-1.4118522196555,-1.177412066494,10.3333834951456));
#63096=CARTESIAN_POINT('Ctrl Pts',(0.223056668548975,-1.82477852394609,
10.4444951456311));
#63097=CARTESIAN_POINT('Ctrl Pts',(1.65390974917898,-0.802670846854376,
10.5556067961165));
#63098=CARTESIAN_POINT('Ctrl Pts',(1.57153269033781,0.953897085409752,10.6667184466019));
#63099=CARTESIAN_POINT('Ctrl Pts',(0.0514163720288116,1.83756944970195,
10.7778300970874));
#63100=CARTESIAN_POINT('Ctrl Pts',(-1.51589489028199,1.04032592396117,10.8889417475728));
#63101=CARTESIAN_POINT('Ctrl Pts',(-1.69599832986023,-0.709309104380943,
11.0000533980583));
#63102=CARTESIAN_POINT('Ctrl Pts',(-0.324962964057439,-1.80887727526569,
11.1111650485437));
#63103=CARTESIAN_POINT('Ctrl Pts',(1.34445241673909,-1.25560970886474,11.2222766990291));
#63104=CARTESIAN_POINT('Ctrl Pts',(1.78171768593789,0.450698535437549,11.3333883495146));
#63105=CARTESIAN_POINT('Ctrl Pts',(0.989503531151977,1.30685679928735,11.4074627831715));
#63106=CARTESIAN_POINT('Ctrl Pts',(0.499806597877626,1.47301514408983,11.4445));
#63107=CARTESIAN_POINT('',(0.903606778650206,-1.26612599672284,0.));
#63108=CARTESIAN_POINT('Ctrl Pts',(0.903606778650208,-1.26612599672284,
-2.77555756156289E-15));
#63109=CARTESIAN_POINT('Ctrl Pts',(1.32452439122316,-0.965726187415828,
0.0370372168284762));
#63110=CARTESIAN_POINT('Ctrl Pts',(1.83597970935092,0.0826171234133487,
0.111111650485434));
#63111=CARTESIAN_POINT('Ctrl Pts',(0.924933321163406,1.59015923519395,0.222223300970871));
#63112=CARTESIAN_POINT('Ctrl Pts',(-0.833119343177651,1.63815447531815,
0.333334951456308));
#63113=CARTESIAN_POINT('Ctrl Pts',(-1.5310616378989,0.622578531632503,0.411241775931451));
#63114=CARTESIAN_POINT('Ctrl Pts',(-1.55772922446558,0.0543356393242454,
0.452111383578116));
#63115=CARTESIAN_POINT('Ctrl Pts',(-1.55735926886437,0.00101346774827265,
0.455943774396301));
#63116=CARTESIAN_POINT('Ctrl Pts',(0.863567639152676,1.75641488315944,2.28983498828939E-16));
#63117=CARTESIAN_POINT('Ctrl Pts',(0.902605506355985,1.73244147111074,2.48310810971475E-16));
#63118=CARTESIAN_POINT('Ctrl Pts',(0.940681517855526,1.70703362163956,1.53446104133306E-16));
#63119=CARTESIAN_POINT('Ctrl Pts',(0.977705169885396,1.68018661523996,1.12757025938492E-16));
#63120=CARTESIAN_POINT('Ctrl Pts',(1.0358643592122,1.63801357064694,3.49621561433049E-17));
#63121=CARTESIAN_POINT('Ctrl Pts',(1.09142895154027,1.59229038852923,-3.14041157591089E-18));
#63122=CARTESIAN_POINT('Ctrl Pts',(1.14423757319707,1.54335784953327,-1.00613961606655E-16));
#63123=CARTESIAN_POINT('Ctrl Pts',(1.16947625472704,1.51997165369202,-1.47199231391008E-16));
#63124=CARTESIAN_POINT('Ctrl Pts',(1.19408480623982,1.49585194230134,-1.44940981238328E-16));
#63125=CARTESIAN_POINT('Ctrl Pts',(1.21804196717247,1.47103398018765,-1.04083408558608E-16));
#63126=CARTESIAN_POINT('Ctrl Pts',(1.23020142841566,1.45843761915368,-8.33461403619852E-17));
#63127=CARTESIAN_POINT('Ctrl Pts',(1.24219304748387,1.44566136836505,-3.17714931440926E-16));
#63128=CARTESIAN_POINT('Ctrl Pts',(1.25401379483509,1.43270976178997,-3.05311331771918E-16));
#63129=CARTESIAN_POINT('Ctrl Pts',(1.26389181876557,1.42188673377951,-2.94946246493115E-16));
#63130=CARTESIAN_POINT('Ctrl Pts',(1.27364380619492,1.41094858444086,-5.46603369369435E-16));
#63131=CARTESIAN_POINT('Ctrl Pts',(1.28326720497828,1.3998998522991,-5.34294830600857E-16));
#63132=CARTESIAN_POINT('Ctrl Pts',(1.330154786252,1.3460676940429,-4.74324582576826E-16));
#63133=CARTESIAN_POINT('Ctrl Pts',(1.37400431756963,1.2896005558432,-2.78813144032988E-17));
#63134=CARTESIAN_POINT('Ctrl Pts',(1.41465239664765,1.2308327382907,1.45716771982052E-16));
#63135=CARTESIAN_POINT('Ctrl Pts',(1.44369336478921,1.18884614615641,2.69743702909727E-16));
#63136=CARTESIAN_POINT('Ctrl Pts',(1.47109927736379,1.14568453076923,1.23340209484872E-16));
#63137=CARTESIAN_POINT('Ctrl Pts',(1.4967949674738,1.10146499100096,1.52655665885959E-16));
#63138=CARTESIAN_POINT('Ctrl Pts',(1.51164370962241,1.07591189080641,1.69596158676961E-16));
#63139=CARTESIAN_POINT('Ctrl Pts',(1.5259211042574,1.05000546373499,-2.47389032972511E-16));
#63140=CARTESIAN_POINT('Ctrl Pts',(1.53961051084784,1.0237681518455,-2.63677968348475E-16));
#63141=CARTESIAN_POINT('Ctrl Pts',(1.5453767175419,1.01271655786648,-2.70539139983884E-16));
#63142=CARTESIAN_POINT('Ctrl Pts',(1.55103417937643,1.00161467257822,6.72528652799515E-17));
#63143=CARTESIAN_POINT('Ctrl Pts',(1.55658137030158,0.990465869694384,6.24500451351651E-17));
#63144=CARTESIAN_POINT('Ctrl Pts',(1.58759523113096,0.928133884781808,3.5597896440648E-17));
#63145=CARTESIAN_POINT('Ctrl Pts',(1.61517455934254,0.864320573166324,-1.32844578099872E-16));
#63146=CARTESIAN_POINT('Ctrl Pts',(1.639165272121,0.799334213601843,-1.80411241501588E-16));
#63147=CARTESIAN_POINT('Ctrl Pts',(1.66256479067373,0.735949288762567,-2.26805737281603E-16));
#63148=CARTESIAN_POINT('Ctrl Pts',(1.68255047093124,0.671447445488438,-3.92048207771591E-16));
#63149=CARTESIAN_POINT('Ctrl Pts',(1.69893099532196,0.606109731061441,-4.30211422042248E-16));
#63150=CARTESIAN_POINT('Ctrl Pts',(1.70969999791506,0.563154939181291,-4.55300957861645E-16));
#63151=CARTESIAN_POINT('Ctrl Pts',(1.71890982821634,0.519838805550124,-3.77882014063636E-16));
#63152=CARTESIAN_POINT('Ctrl Pts',(1.72649398406889,0.476242912678102,-4.71844785465692E-16));
#63153=CARTESIAN_POINT('Ctrl Pts',(1.73287054571603,0.439588616027976,-5.50846247992205E-16));
#63154=CARTESIAN_POINT('Ctrl Pts',(1.73809775889755,0.402736552578244,-9.42921937940892E-17));
#63155=CARTESIAN_POINT('Ctrl Pts',(1.74213052178609,0.36573694696249,-1.2490009027033E-16));
#63156=CARTESIAN_POINT('Ctrl Pts',(1.74338539139703,0.354223827548557,-1.34424309820125E-16));
#63157=CARTESIAN_POINT('Ctrl Pts',(1.74452450777523,0.342696049837886,-3.03274465566551E-16));
#63158=CARTESIAN_POINT('Ctrl Pts',(1.74554535151306,0.331170337018761,-2.91433543964104E-16));
#63159=CARTESIAN_POINT('Ctrl Pts',(1.75129431083391,0.266262406759456,-2.24750491415529E-16));
#63160=CARTESIAN_POINT('Ctrl Pts',(1.75331011127704,0.201301920292928,9.80627071070611E-17));
#63161=CARTESIAN_POINT('Ctrl Pts',(1.75142561531544,0.136549272921142,2.77555756156289E-17));
#63162=CARTESIAN_POINT('Ctrl Pts',(1.75088296778463,0.11790351037964,7.510378979319E-18));
#63163=CARTESIAN_POINT('Ctrl Pts',(1.75001659332986,0.099275023041261,-5.08054903583662E-16));
#63164=CARTESIAN_POINT('Ctrl Pts',(1.74882170147482,0.0806701752180915,
-4.85722573273506E-16));
#63165=CARTESIAN_POINT('Ctrl Pts',(1.74442082328573,0.0121470962041962,
-4.16579971360731E-16));
#63166=CARTESIAN_POINT('Ctrl Pts',(1.73556771390717,-0.056057442313777,
-1.52368272571946E-16));
#63167=CARTESIAN_POINT('Ctrl Pts',(1.72245534586321,-0.123606275893366,
-5.55111512312578E-17));
#63168=CARTESIAN_POINT('Ctrl Pts',(1.71065390208195,-0.184401836184713,
3.16625666268892E-17));
#63169=CARTESIAN_POINT('Ctrl Pts',(1.69540107690307,-0.244666544752314,
-5.10914177950054E-16));
#63170=CARTESIAN_POINT('Ctrl Pts',(1.67680493801022,-0.304129401844208,
-5.82867087928207E-16));
#63171=CARTESIAN_POINT('Ctrl Pts',(1.67349552259788,-0.314711560692091,
-5.95672007842828E-16));
#63172=CARTESIAN_POINT('Ctrl Pts',(1.67008173945308,-0.325263020743978,
-2.82234476894323E-16));
#63173=CARTESIAN_POINT('Ctrl Pts',(1.66656691458475,-0.335775244456298,
-2.77555756156289E-16));
#63174=CARTESIAN_POINT('Ctrl Pts',(1.64601434320315,-0.39724437487395,-2.5019742521657E-16));
#63175=CARTESIAN_POINT('Ctrl Pts',(1.6219871213203,-0.457449913435399,-1.49651752513019E-16));
#63176=CARTESIAN_POINT('Ctrl Pts',(1.59467186427628,-0.5161179062652,-1.94289029309402E-16));
#63177=CARTESIAN_POINT('Ctrl Pts',(1.56746479951959,-0.57455352257637,-2.38749503483388E-16));
#63178=CARTESIAN_POINT('Ctrl Pts',(1.53699493854014,-0.631464584970275,
-4.11608014004163E-16));
#63179=CARTESIAN_POINT('Ctrl Pts',(1.50340708769257,-0.686547887629179,
-4.71844785465692E-16));
#63180=CARTESIAN_POINT('Ctrl Pts',(1.47050686756616,-0.740503491725204,
-5.30848353445754E-16));
#63181=CARTESIAN_POINT('Ctrl Pts',(1.43461427022078,-0.792706028859038,
8.26037042042841E-17));
#63182=CARTESIAN_POINT('Ctrl Pts',(1.39583852741916,-0.842828743497358,
1.94289029309402E-16));
#63183=CARTESIAN_POINT('Ctrl Pts',(1.38891448399703,-0.851778974428235,
2.14232271779286E-16));
#63184=CARTESIAN_POINT('Ctrl Pts',(1.38189845475662,-0.860662765012678,
1.05754276149716E-16));
#63185=CARTESIAN_POINT('Ctrl Pts',(1.3747909965488,-0.869478087839508,1.11022302462516E-16));
#63186=CARTESIAN_POINT('Ctrl Pts',(1.36801000346398,-0.877888498619479,
1.1604835382339E-16));
#63187=CARTESIAN_POINT('Ctrl Pts',(1.36114891147745,-0.8862326313589,4.78426519390645E-16));
#63188=CARTESIAN_POINT('Ctrl Pts',(1.35421355798306,-0.894502968665375,
4.71844785465692E-16));
#63189=CARTESIAN_POINT('Ctrl Pts',(1.3143417576089,-0.942049678199007,4.34005967100638E-16));
#63190=CARTESIAN_POINT('Ctrl Pts',(1.27196760499602,-0.987223303029092,
-4.84873724376989E-16));
#63191=CARTESIAN_POINT('Ctrl Pts',(1.22722986402911,-1.02975664627632,-3.05311331771918E-16));
#63192=CARTESIAN_POINT('Ctrl Pts',(1.18329662429212,-1.07152512911229,-1.2897793916942E-16));
#63193=CARTESIAN_POINT('Ctrl Pts',(1.13708333146208,-1.1107479710078,1.42267300457324E-16));
#63194=CARTESIAN_POINT('Ctrl Pts',(1.08869802628341,-1.14712822354107,1.94289029309402E-16));
#63195=CARTESIAN_POINT('Ctrl Pts',(1.04185702701945,-1.1823473334721,2.44650389103912E-16));
#63196=CARTESIAN_POINT('Ctrl Pts',(0.99297984330778,-1.21490270865201,1.66616011326585E-16));
#63197=CARTESIAN_POINT('Ctrl Pts',(0.942151955941521,-1.24447758118399,
1.11022302462516E-16));
#63198=CARTESIAN_POINT('Ctrl Pts',(0.929425469464971,-1.25188265416315,
9.71025308430195E-17));
#63199=CARTESIAN_POINT('Ctrl Pts',(0.916576650468056,-1.25910062269163,
1.9641793555709E-16));
#63200=CARTESIAN_POINT('Ctrl Pts',(0.903606778650242,-1.26612599672281,
1.94289029309402E-16));
#63201=CARTESIAN_POINT('Ctrl Pts',(1.88079991776263,-0.516378774142081,
11.046));
#63202=CARTESIAN_POINT('Ctrl Pts',(1.79754570390634,-0.821182550519846,
11.028067538919));
#63203=CARTESIAN_POINT('Ctrl Pts',(1.64446793279769,-1.10682480125595,11.010135077838));
#63204=CARTESIAN_POINT('Ctrl Pts',(1.43091597726206,-1.33587557506818,10.9922026167571));
#63205=CARTESIAN_POINT('Ctrl Pts',(0.9898515831668,-1.80895080641009,10.9551653999286));
#63206=CARTESIAN_POINT('Ctrl Pts',(0.290818548970629,-2.04062011418838,
10.9181281831001));
#63207=CARTESIAN_POINT('Ctrl Pts',(-0.345744266721549,-1.9262440956347,
10.8810909662716));
#63208=CARTESIAN_POINT('Ctrl Pts',(-0.982307082413709,-1.81186807708102,
10.8440537494431));
#63209=CARTESIAN_POINT('Ctrl Pts',(-1.55639967960188,-1.35144673219537,
10.8070165326147));
#63210=CARTESIAN_POINT('Ctrl Pts',(-1.80573868997825,-0.754924386616321,
10.7699793157862));
#63211=CARTESIAN_POINT('Ctrl Pts',(-1.90472245868201,-0.518114150655666,
10.7552761078989));
#63212=CARTESIAN_POINT('Ctrl Pts',(-1.95252608806662,-0.259854826956367,
10.7405729000116));
#63213=CARTESIAN_POINT('Ctrl Pts',(-1.95129684289216,-0.00113636086278679,
10.7258696921242));
#63214=CARTESIAN_POINT('Origin',(0.,0.,-1.29405622560369));
#63215=CARTESIAN_POINT('',(-0.903606778650172,-1.26612599672286,0.));
#63216=CARTESIAN_POINT('Ctrl Pts',(-0.905549614304886,-1.26792015305981,
1.24276674021151E-15));
#63217=CARTESIAN_POINT('Ctrl Pts',(-0.513706458239086,-1.54472437079514,
0.0344950590738082));
#63218=CARTESIAN_POINT('Ctrl Pts',(0.587535178885047,-1.72169358136003,
0.106052258091336));
#63219=CARTESIAN_POINT('Ctrl Pts',(1.77508460417327,-0.479721809770191,
0.214671597052585));
#63220=CARTESIAN_POINT('Ctrl Pts',(1.3650560094313,1.23222299189869,0.325858016883748));
#63221=CARTESIAN_POINT('Ctrl Pts',(-0.295638381403906,1.81478253869214,
0.43704443671491));
#63222=CARTESIAN_POINT('Ctrl Pts',(-1.41307745535963,0.946781319192958,
0.526443839621562));
#63223=CARTESIAN_POINT('Ctrl Pts',(-1.55414936746312,0.214718667413076,
0.578781102584494));
#63224=CARTESIAN_POINT('Ctrl Pts',(-1.55326046963413,0.000729270061605551,
0.594056225603705));
#63225=CARTESIAN_POINT('Origin',(0.,0.,0.));
#63226=CARTESIAN_POINT('Ctrl Pts',(-0.685825729128748,1.39614588036674,
-0.230074082272066));
#63227=CARTESIAN_POINT('Ctrl Pts',(-1.15028016933624,1.16799292759742,-0.193011942328345));
#63228=CARTESIAN_POINT('Ctrl Pts',(-1.82555218707277,0.215691441263552,
-0.118887662440903));
#63229=CARTESIAN_POINT('Ctrl Pts',(-1.16942936218886,-1.42059634545264,
-0.00770124260974049));
#63230=CARTESIAN_POINT('Ctrl Pts',(0.559468948314244,-1.75104601534012,
0.103485177221422));
#63231=CARTESIAN_POINT('Ctrl Pts',(1.77508460417327,-0.479721809770191,
0.214671597052585));
#63232=CARTESIAN_POINT('Ctrl Pts',(1.3650560094313,1.23222299189869,0.325858016883748));
#63233=CARTESIAN_POINT('Ctrl Pts',(-0.295638381403906,1.81478253869214,
0.43704443671491));
#63234=CARTESIAN_POINT('Ctrl Pts',(-1.68540213790592,0.735245708832444,
0.548230856546073));
#63235=CARTESIAN_POINT('Ctrl Pts',(-1.53132379752993,-1.01797781965797,
0.659417276377235));
#63236=CARTESIAN_POINT('Ctrl Pts',(0.0255447675030308,-1.83860034663711,
0.770603696208398));
#63237=CARTESIAN_POINT('Ctrl Pts',(1.55899683301632,-0.975032021788082,
0.881790116039561));
#63238=CARTESIAN_POINT('Ctrl Pts',(1.66434877052597,0.781732535368643,0.992976535870723));
#63239=CARTESIAN_POINT('Ctrl Pts',(0.245080507541896,1.82238325373942,1.10416295570189));
#63240=CARTESIAN_POINT('Ctrl Pts',(-1.39868975820189,1.19365863723167,1.21534937553305));
#63241=CARTESIAN_POINT('Ctrl Pts',(-1.76120077222934,-0.528512641939849,
1.32653579536421));
#63242=CARTESIAN_POINT('Ctrl Pts',(-0.510374815939226,-1.76654153931159,
1.43772221519537));
#63243=CARTESIAN_POINT('Ctrl Pts',(1.20797626960931,-1.38634273102519,1.54890863502654));
#63244=CARTESIAN_POINT('Ctrl Pts',(1.81976886629041,0.263806680570579,1.6600950548577));
#63245=CARTESIAN_POINT('Ctrl Pts',(0.764574137846417,1.67229745635935,1.77128147468886));
#63246=CARTESIAN_POINT('Ctrl Pts',(-0.991003621173195,1.54889135395602,
1.88246789452002));
#63247=CARTESIAN_POINT('Ctrl Pts',(-1.83877909581896,0.00663349951290586,
1.99365431435119));
#63248=CARTESIAN_POINT('Ctrl Pts',(-1.00215313155719,-1.54170088892816,
2.10484073418235));
#63249=CARTESIAN_POINT('Ctrl Pts',(0.752488571272716,-1.67777039880966,
2.21602715401351));
#63250=CARTESIAN_POINT('Ctrl Pts',(1.81781810074028,-0.276929424335053,
2.32721357384467));
#63251=CARTESIAN_POINT('Ctrl Pts',(1.21794738393109,1.37759091140133,2.43839999367584));
#63252=CARTESIAN_POINT('Ctrl Pts',(-0.497615974795104,1.77017821004958,
2.549586413507));
#63253=CARTESIAN_POINT('Ctrl Pts',(-1.75734151264734,0.541205469518692,
2.66077283333817));
#63254=CARTESIAN_POINT('Ctrl Pts',(-1.40726598433086,-1.1835349598584,2.77195925316932));
#63255=CARTESIAN_POINT('Ctrl Pts',(0.231926238140432,-1.82410602009977,
2.88314567300049));
#63256=CARTESIAN_POINT('Ctrl Pts',(1.65866396469461,-0.793716828903688,
2.99433209283165));
#63257=CARTESIAN_POINT('Ctrl Pts',(1.56599354026699,0.96375141196464,3.10551851266282));
#63258=CARTESIAN_POINT('Ctrl Pts',(0.0388050940998321,1.83838154825996,
3.21670493249398));
#63259=CARTESIAN_POINT('Ctrl Pts',(-1.52393050178991,1.02897443019027,3.32789135232514));
#63260=CARTESIAN_POINT('Ctrl Pts',(-1.69067964401488,-0.723017906820314,
3.4390777721563));
#63261=CARTESIAN_POINT('Ctrl Pts',(-0.308692884081366,-1.81269447386996,
3.55026419198746));
#63262=CARTESIAN_POINT('Ctrl Pts',(1.35606994996762,-1.24186426112907,3.66145061181863));
#63263=CARTESIAN_POINT('Ctrl Pts',(1.77861387826841,0.466567491694538,3.77263703164979));
#63264=CARTESIAN_POINT('Ctrl Pts',(0.571870330903418,1.74760318061885,3.88382345148095));
#63265=CARTESIAN_POINT('Ctrl Pts',(-1.15873124952358,1.42775853828764,3.99500987131212));
#63266=CARTESIAN_POINT('Ctrl Pts',(-1.82788473512851,-0.199974866820836,
4.10619629114327));
#63267=CARTESIAN_POINT('Ctrl Pts',(-0.822616502622442,-1.64452261823584,
4.21738271097444));
#63268=CARTESIAN_POINT('Ctrl Pts',(0.936204134582059,-1.58261630557358,
4.3285691308056));
#63269=CARTESIAN_POINT('Ctrl Pts',(1.83742116834086,-0.0709647969689106,
4.43975555063676));
#63270=CARTESIAN_POINT('Ctrl Pts',(1.0554806974386,1.50569354438759,4.55094197046793));
#63271=CARTESIAN_POINT('Ctrl Pts',(-0.693325883166112,1.70307127625589,
4.66212839029909));
#63272=CARTESIAN_POINT('Ctrl Pts',(-1.80701587562324,0.340361833232659,
4.77331481013025));
#63273=CARTESIAN_POINT('Ctrl Pts',(-1.26540093064824,-1.33413381524886,
4.88450122996142));
#63274=CARTESIAN_POINT('Ctrl Pts',(0.435376164803608,-1.7865050090601,4.99568764979258));
#63275=CARTESIAN_POINT('Ctrl Pts',(1.73732980498774,-0.602360109052031,
5.10687406962374));
#63276=CARTESIAN_POINT('Ctrl Pts',(1.44781397169404,1.13357278356683,5.21806048945491));
#63277=CARTESIAN_POINT('Ctrl Pts',(-0.167962271460079,1.83110382765203,
5.32924690928607));
#63278=CARTESIAN_POINT('Ctrl Pts',(-1.62987778710162,0.851264325217889,
5.44043332911723));
#63279=CARTESIAN_POINT('Ctrl Pts',(-1.59875453933454,-0.908370230265797,
5.55161974894839));
#63280=CARTESIAN_POINT('Ctrl Pts',(-0.103102773360761,-1.83589824620028,
5.66280616877956));
#63281=CARTESIAN_POINT('Ctrl Pts',(1.4869956060099,-1.08166382022474,5.77399258861071));
#63282=CARTESIAN_POINT('Ctrl Pts',(1.71494149863546,0.663421591850831,5.88517900844189));
#63283=CARTESIAN_POINT('Ctrl Pts',(0.371926577693494,1.80078404398782,5.99636542827304));
#63284=CARTESIAN_POINT('Ctrl Pts',(-1.311789224034,1.28855018683177,6.10755184810421));
#63285=CARTESIAN_POINT('Ctrl Pts',(-1.79384918603911,-0.404051543769803,
6.21873826793537));
#63286=CARTESIAN_POINT('Ctrl Pts',(-0.632665469493242,-1.72652453095426,
6.32992468776653));
#63287=CARTESIAN_POINT('Ctrl Pts',(1.10806726459172,-1.46742614445027,6.44111110759769));
#63288=CARTESIAN_POINT('Ctrl Pts',(1.83376231205259,0.135898253011021,6.55229752742886));
#63289=CARTESIAN_POINT('Ctrl Pts',(0.879651525947856,1.61473395492061,6.66348394726001));
#63290=CARTESIAN_POINT('Ctrl Pts',(-0.880258220622017,1.61440330069759,
6.77467036709119));
#63291=CARTESIAN_POINT('Ctrl Pts',(-1.83381324808445,0.13520918395534,6.88585678692234));
#63292=CARTESIAN_POINT('Ctrl Pts',(-1.1075157823663,-1.46784241118916,6.99704320675351));
#63293=CARTESIAN_POINT('Ctrl Pts',(0.633314188332071,-1.72628667698419,
7.10822962658467));
#63294=CARTESIAN_POINT('Ctrl Pts',(1.7940008868909,-0.403377453646542,7.21941604641583));
#63295=CARTESIAN_POINT('Ctrl Pts',(1.31130494233742,1.28904301731096,7.33060246624699));
#63296=CARTESIAN_POINT('Ctrl Pts',(-0.372603218894873,1.80064416072257,
7.44178888607816));
#63297=CARTESIAN_POINT('Ctrl Pts',(-1.71519066664489,0.662777133981789,
7.55297530590932));
#63298=CARTESIAN_POINT('Ctrl Pts',(-1.48658905212271,-1.08222250133236,
7.66416172574049));
#63299=CARTESIAN_POINT('Ctrl Pts',(0.103792628149562,-1.8358593744105,7.77534814557165));
#63300=CARTESIAN_POINT('Ctrl Pts',(1.59909575810308,-0.907769413831382,
7.8865345654028));
#63301=CARTESIAN_POINT('Ctrl Pts',(1.62955779866738,0.851876712390422,7.99772098523398));
#63302=CARTESIAN_POINT('Ctrl Pts',(0.167274199086701,1.83116681231986,8.10890740506512));
#63303=CARTESIAN_POINT('Ctrl Pts',(-1.44823982381472,1.1330286690894,8.2200938248963));
#63304=CARTESIAN_POINT('Ctrl Pts',(-1.73710333792674,-0.603012890298399,
8.33128024472746));
#63305=CARTESIAN_POINT('Ctrl Pts',(-0.434704832044991,-1.78666848096071,
8.44246666455862));
#63306=CARTESIAN_POINT('Ctrl Pts',(1.26590215885116,-1.33365823077974,8.55365308438979));
#63307=CARTESIAN_POINT('Ctrl Pts',(1.8068878531032,0.341040818691465,8.66483950422094));
#63308=CARTESIAN_POINT('Ctrl Pts',(0.69268588294083,1.70333168137465,8.77602592405212));
#63309=CARTESIAN_POINT('Ctrl Pts',(-1.05604640517969,1.5052968290502,8.88721234388326));
#63310=CARTESIAN_POINT('Ctrl Pts',(-1.83739437498563,-0.0716552286239433,
8.99839876371444));
#63311=CARTESIAN_POINT('Ctrl Pts',(-0.935609375970031,-1.5829679799695,
9.1095851835456));
#63312=CARTESIAN_POINT('Ctrl Pts',(0.823234386500799,-1.64421340203127,
9.22077160337675));
#63313=CARTESIAN_POINT('Ctrl Pts',(1.82795976495949,-0.199287985657338,
9.33195802320793));
#63314=CARTESIAN_POINT('Ctrl Pts',(1.15819463928053,1.42819381470141,9.44314444303908));
#63315=CARTESIAN_POINT('Ctrl Pts',(-0.572526917402423,1.74738822826618,
9.55433086287024));
#63316=CARTESIAN_POINT('Ctrl Pts',(-1.77878918025408,0.46589901053406,9.66551728270142));
#63317=CARTESIAN_POINT('Ctrl Pts',(-1.35560300066214,-1.24237352171324,
9.77670370253256));
#63318=CARTESIAN_POINT('Ctrl Pts',(0.309373610575528,-1.81257875466721,
9.88789012236375));
#63319=CARTESIAN_POINT('Ctrl Pts',(1.69095195914933,-0.722381792257861,
9.99907654219489));
#63320=CARTESIAN_POINT('Ctrl Pts',(1.52354231364944,1.0295455294481,10.1102629620261));
#63321=CARTESIAN_POINT('Ctrl Pts',(-0.0394931635484403,1.83836962465064,
10.2214493818572));
#63322=CARTESIAN_POINT('Ctrl Pts',(-1.56636075542215,0.963157594965877,
10.3326358016884));
#63323=CARTESIAN_POINT('Ctrl Pts',(-1.65835572967195,-0.794329933758677,
10.4438222215196));
#63324=CARTESIAN_POINT('Ctrl Pts',(-0.231259578302998,-1.82421227428175,
10.5550086413507));
#63325=CARTESIAN_POINT('Ctrl Pts',(1.40774638007895,-1.1829694620695,10.6661950611819));
#63326=CARTESIAN_POINT('Ctrl Pts',(1.75706993010233,0.541796064983141,10.7773814810131));
#63327=CARTESIAN_POINT('Ctrl Pts',(0.497080432048737,1.77049779856472,10.8885679008442));
#63328=CARTESIAN_POINT('Ctrl Pts',(-1.21871201614337,1.37688031013954,10.9997543206754));
#63329=CARTESIAN_POINT('Ctrl Pts',(-1.81724153253684,-0.27712968875509,
11.1109407405065));
#63330=CARTESIAN_POINT('Ctrl Pts',(-0.75277483453787,-1.67898453189698,
11.2221271603377));
#63331=CARTESIAN_POINT('Ctrl Pts',(1.00462758039806,-1.53944373403644,11.3333135801688));
#63332=CARTESIAN_POINT('Ctrl Pts',(1.55754888396286,-0.511266487217653,
11.4074378600563));
#63333=CARTESIAN_POINT('Ctrl Pts',(1.55548765964692,0.00619602180124784,
11.4445));
#63334=CARTESIAN_POINT('Ctrl Pts',(-0.74439243930934,1.51537102412034,-0.153382721514711));
#63335=CARTESIAN_POINT('Ctrl Pts',(-1.24850938769699,1.26773474301532,-0.11632058157099));
#63336=CARTESIAN_POINT('Ctrl Pts',(-1.98144687185762,0.234110607521693,
-0.042196301683548));
#63337=CARTESIAN_POINT('Ctrl Pts',(-1.26929384324154,-1.54190945884872,
0.0689901181476148));
#63338=CARTESIAN_POINT('Ctrl Pts',(0.607245306591998,-1.90057817801302,
0.180176537978778));
#63339=CARTESIAN_POINT('Ctrl Pts',(1.92666956394248,-0.520688088821623,
0.29136295780994));
#63340=CARTESIAN_POINT('Ctrl Pts',(1.48162620545796,1.33744979191402,0.402549377641103));
#63341=CARTESIAN_POINT('Ctrl Pts',(-0.320884689126903,1.9697575395855,0.513735797472264));
#63342=CARTESIAN_POINT('Ctrl Pts',(-1.82932858212653,0.798032683003624,
0.624922217303428));
#63343=CARTESIAN_POINT('Ctrl Pts',(-1.66209258212561,-1.10490895887015,
0.736108637134591));
#63344=CARTESIAN_POINT('Ctrl Pts',(0.0277261860929502,-1.99560929084259,
0.847295056965753));
#63345=CARTESIAN_POINT('Ctrl Pts',(1.69212878157669,-1.0582957656395,0.958481476796916));
#63346=CARTESIAN_POINT('Ctrl Pts',(1.80647734334385,0.848489294255244,1.06966789662808));
#63347=CARTESIAN_POINT('Ctrl Pts',(0.266009379770665,1.97800732458805,1.18085431645924));
#63348=CARTESIAN_POINT('Ctrl Pts',(-1.51813213871049,1.2955921992025,1.29204073629041));
#63349=CARTESIAN_POINT('Ctrl Pts',(-1.91160010957712,-0.573645458357494,
1.40322715612156));
#63350=CARTESIAN_POINT('Ctrl Pts',(-0.553958736254638,-1.91739695630841,
1.51441357595273));
#63351=CARTESIAN_POINT('Ctrl Pts',(1.31113249878304,-1.50473072594935,1.62559999578389));
#63352=CARTESIAN_POINT('Ctrl Pts',(1.9751696791516,0.286334691329668,1.73678641561505));
#63353=CARTESIAN_POINT('Ctrl Pts',(0.829865639814035,1.81510481441338,1.84797283544622));
#63354=CARTESIAN_POINT('Ctrl Pts',(-1.07563127424026,1.68116033596642,1.95915925527738));
#63355=CARTESIAN_POINT('Ctrl Pts',(-1.99580330447296,0.00719997322039096,
2.07034567510854));
#63356=CARTESIAN_POINT('Ctrl Pts',(-1.08773290717609,-1.67335583465575,
2.18153209493971));
#63357=CARTESIAN_POINT('Ctrl Pts',(0.816748015321165,-1.82104512374819,
2.29271851477087));
#63358=CARTESIAN_POINT('Ctrl Pts',(1.97305232620797,-0.300578063700233,
2.40390493460203));
#63359=CARTESIAN_POINT('Ctrl Pts',(1.32195510545613,1.49523153675082,2.51509135443319));
#63360=CARTESIAN_POINT('Ctrl Pts',(-0.54011034229875,1.92134418384253,2.62627777426435));
#63361=CARTESIAN_POINT('Ctrl Pts',(-1.90741128502276,0.587422201459822,
2.73746419409552));
#63362=CARTESIAN_POINT('Ctrl Pts',(-1.52744073944838,-1.28460400121777,
2.84865061392668));
#63363=CARTESIAN_POINT('Ctrl Pts',(0.251731789602741,-1.9798772081443,2.95983703375785));
#63364=CARTESIAN_POINT('Ctrl Pts',(1.80030707836241,-0.861496997406464,
3.071023453589));
#63365=CARTESIAN_POINT('Ctrl Pts',(1.69972297898904,1.04605183790867,3.18220987342017));
#63366=CARTESIAN_POINT('Ctrl Pts',(0.0421188903066005,1.99537180797957,
3.29339629325133));
#63367=CARTESIAN_POINT('Ctrl Pts',(-1.65406792919015,1.11684463493277,3.4045827130825));
#63368=CARTESIAN_POINT('Ctrl Pts',(-1.83505676565636,-0.784760676748056,
3.51576913291366));
#63369=CARTESIAN_POINT('Ctrl Pts',(-0.335053992900935,-1.96749116257395,
3.62695555274482));
#63370=CARTESIAN_POINT('Ctrl Pts',(1.47187277329603,-1.34791438607496,3.73814197257599));
#63371=CARTESIAN_POINT('Ctrl Pts',(1.93050022360002,0.506410445822938,3.84932839240714));
#63372=CARTESIAN_POINT('Ctrl Pts',(0.620705716495424,1.89684133929807,3.96051481223831));
#63373=CARTESIAN_POINT('Ctrl Pts',(-1.25768215554202,1.54968327363698,4.07170123206947));
#63374=CARTESIAN_POINT('Ctrl Pts',(-1.9839786099702,-0.217051901949521,
4.18288765190064));
#63375=CARTESIAN_POINT('Ctrl Pts',(-0.892864584974339,-1.78495811879663,
4.29407407173179));
#63376=CARTESIAN_POINT('Ctrl Pts',(1.01615213578872,-1.71776526041577,4.40526049156296));
#63377=CARTESIAN_POINT('Ctrl Pts',(1.99432941554622,-0.0770249001709277,
4.51644691139412));
#63378=CARTESIAN_POINT('Ctrl Pts',(1.14561442891388,1.6342736102696,4.62763333122529));
#63379=CARTESIAN_POINT('Ctrl Pts',(-0.752533075803338,1.84850659257176,
4.73881975105645));
#63380=CARTESIAN_POINT('Ctrl Pts',(-1.96132763527948,0.369427340688636,
4.85000617088761));
#63381=CARTESIAN_POINT('Ctrl Pts',(-1.3734609908354,-1.44806338245697,4.96119259071877));
#63382=CARTESIAN_POINT('Ctrl Pts',(0.472555507281729,-1.9390652246629,5.07237901054994));
#63383=CARTESIAN_POINT('Ctrl Pts',(1.88569065943703,-0.653799196903168,
5.1835654303811));
#63384=CARTESIAN_POINT('Ctrl Pts',(1.57145135896933,1.23037525956625,5.29475185021226));
#63385=CARTESIAN_POINT('Ctrl Pts',(-0.182305561972616,1.98747259981946,
5.40593827004342));
#63386=CARTESIAN_POINT('Ctrl Pts',(-1.76906267902489,0.923958814363803,
5.51712468987459));
#63387=CARTESIAN_POINT('Ctrl Pts',(-1.73528163328608,-0.985941329968107,
5.62831110970574));
#63388=CARTESIAN_POINT('Ctrl Pts',(-0.111907328205795,-1.99267644208816,
5.73949752953692));
#63389=CARTESIAN_POINT('Ctrl Pts',(1.61397894448518,-1.17403348321834,5.85068394936807));
#63390=CARTESIAN_POINT('Ctrl Pts',(1.86139048335769,0.720075080408093,5.96187036919923));
#63391=CARTESIAN_POINT('Ctrl Pts',(0.403687585131819,1.9545636307293,6.0730567890304));
#63392=CARTESIAN_POINT('Ctrl Pts',(-1.42381065460884,1.39858709874703,6.18424320886156));
#63393=CARTESIAN_POINT('Ctrl Pts',(-1.94703656429618,-0.438555891823412,
6.29542962869273));
#63394=CARTESIAN_POINT('Ctrl Pts',(-0.686692511086116,-1.87396265922711,
6.40661604852388));
#63395=CARTESIAN_POINT('Ctrl Pts',(1.20269167366484,-1.59273833100625,6.51780246835505));
#63396=CARTESIAN_POINT('Ctrl Pts',(1.99035810790665,0.147503407586138,6.62898888818621));
#63397=CARTESIAN_POINT('Ctrl Pts',(0.954770165847204,1.75262562555938,6.74017530801738));
#63398=CARTESIAN_POINT('Ctrl Pts',(-0.9554286697633,1.7522667348191,6.85136172784854));
#63399=CARTESIAN_POINT('Ctrl Pts',(-1.99041339366714,0.146755494853507,
6.9625481476797));
#63400=CARTESIAN_POINT('Ctrl Pts',(-1.20209309711463,-1.59319014522084,
7.07373456751086));
#63401=CARTESIAN_POINT('Ctrl Pts',(0.687396627858533,-1.87370449350154,
7.18492098734203));
#63402=CARTESIAN_POINT('Ctrl Pts',(1.94720121977979,-0.437824237162718,
7.29610740717318));
#63403=CARTESIAN_POINT('Ctrl Pts',(1.42328501723757,1.39912201493195,7.40729382700435));
#63404=CARTESIAN_POINT('Ctrl Pts',(-0.404422008722263,1.95441180200575,
7.51848024683551));
#63405=CARTESIAN_POINT('Ctrl Pts',(-1.86166092929526,0.719375588474842,
7.62966666666667));
#63406=CARTESIAN_POINT('Ctrl Pts',(-1.61353767256008,-1.17463987340584,
7.74085308649784));
#63407=CARTESIAN_POINT('Ctrl Pts',(0.112656093769942,-1.99263425080664,
7.852039506329));
#63408=CARTESIAN_POINT('Ctrl Pts',(1.73565199074082,-0.985289206269375,
7.96322592616017));
#63409=CARTESIAN_POINT('Ctrl Pts',(1.76871536488809,0.924623496894334,8.07441234599133));
#63410=CARTESIAN_POINT('Ctrl Pts',(0.181558731034875,1.98754096312013,8.18559876582249));
#63411=CARTESIAN_POINT('Ctrl Pts',(-1.57191357711808,1.22978467993954,8.29678518565365));
#63412=CARTESIAN_POINT('Ctrl Pts',(-1.88544485301595,-0.6545077229961,8.40797160548482));
#63413=CARTESIAN_POINT('Ctrl Pts',(-0.471826845453332,-1.93924265639472,
8.51915802531597));
#63414=CARTESIAN_POINT('Ctrl Pts',(1.37400502187529,-1.44754718502077,8.63034444514714));
#63415=CARTESIAN_POINT('Ctrl Pts',(1.96118868016023,0.370164308726493,8.7415308649783));
#63416=CARTESIAN_POINT('Ctrl Pts',(0.751838422178375,1.84878923522181,8.85271728480947));
#63417=CARTESIAN_POINT('Ctrl Pts',(-1.14622844578058,1.63384301706618,8.96390370464062));
#63418=CARTESIAN_POINT('Ctrl Pts',(-1.99430033414812,-0.077774291863319,
9.0750901244718));
#63419=CARTESIAN_POINT('Ctrl Pts',(-1.01550658722561,-1.71814696636568,
9.18627654430294));
#63420=CARTESIAN_POINT('Ctrl Pts',(0.893535233606871,-1.78462249679383,
9.29746296413412));
#63421=CARTESIAN_POINT('Ctrl Pts',(1.98406004704164,-0.216306363946107,
9.40864938396527));
#63422=CARTESIAN_POINT('Ctrl Pts',(1.2570997209806,1.55015572087487,9.51983580379645));
#63423=CARTESIAN_POINT('Ctrl Pts',(-0.621418372793996,1.8966080308943,9.63102222362759));
#63424=CARTESIAN_POINT('Ctrl Pts',(-1.93069049565776,0.50568487910749,9.74220864345877));
#63425=CARTESIAN_POINT('Ctrl Pts',(-1.47136594843111,-1.34846713542859,
9.85339506328992));
#63426=CARTESIAN_POINT('Ctrl Pts',(0.335792850651442,-1.96736556142493,
9.9645814831211));
#63427=CARTESIAN_POINT('Ctrl Pts',(1.83535233538869,-0.784070240605622,
10.0757679029522));
#63428=CARTESIAN_POINT('Ctrl Pts',(1.65364659137136,1.11746450372967,10.1869543227834));
#63429=CARTESIAN_POINT('Ctrl Pts',(-0.0428657180698079,1.99535886614283,
10.2981407426146));
#63430=CARTESIAN_POINT('Ctrl Pts',(-1.70012155281541,1.04540731136874,10.4093271624457));
#63431=CARTESIAN_POINT('Ctrl Pts',(-1.79997252133044,-0.862162458906591,
10.5205135822769));
#63432=CARTESIAN_POINT('Ctrl Pts',(-0.251008199743871,-1.97999253599851,
10.6317000021081));
#63433=CARTESIAN_POINT('Ctrl Pts',(1.52796215902707,-1.28399021223231,10.7428864219392));
#63434=CARTESIAN_POINT('Ctrl Pts',(1.90711651044001,0.588063231359589,10.8540728417704));
#63435=CARTESIAN_POINT('Ctrl Pts',(0.539529066393858,1.92169106390877,10.9652592616015));
#63436=CARTESIAN_POINT('Ctrl Pts',(-1.32278503412967,1.49446025304978,11.0764456814327));
#63437=CARTESIAN_POINT('Ctrl Pts',(-1.97242652143987,-0.300795429882017,
11.1876321012639));
#63438=CARTESIAN_POINT('Ctrl Pts',(-0.817058724297523,-1.82236293883171,
11.2988185210951));
#63439=CARTESIAN_POINT('Ctrl Pts',(1.09041866382002,-1.67090592797485,11.4100049409262));
#63440=CARTESIAN_POINT('Ctrl Pts',(1.69055718360052,-0.554926552610627,
11.4841292208136));
#63441=CARTESIAN_POINT('Ctrl Pts',(1.6883199391646,0.00672513670271936,
11.5211913607574));
#63442=CARTESIAN_POINT('Ctrl Pts',(-0.802959149489932,1.63459616787394,
-0.0766913607573554));
#63443=CARTESIAN_POINT('Ctrl Pts',(-1.34673860605774,1.36747655843322,-0.0396292208136346));
#63444=CARTESIAN_POINT('Ctrl Pts',(-2.13734155664247,0.252529773779836,
0.0344950590738073));
#63445=CARTESIAN_POINT('Ctrl Pts',(-1.36915832429422,-1.66322257224481,
0.14568147890497));
#63446=CARTESIAN_POINT('Ctrl Pts',(0.655021664869751,-2.05011034068591,
0.256867898736133));
#63447=CARTESIAN_POINT('Ctrl Pts',(2.0782545237117,-0.561654367873057,0.368054318567295));
#63448=CARTESIAN_POINT('Ctrl Pts',(1.59819640148463,1.44267659192936,0.479240738398458));
#63449=CARTESIAN_POINT('Ctrl Pts',(-0.346130996849898,2.12473254047885,
0.590427158229621));
#63450=CARTESIAN_POINT('Ctrl Pts',(-1.97325502634714,0.860819657174806,
0.701613578060782));
#63451=CARTESIAN_POINT('Ctrl Pts',(-1.79286136672128,-1.19184009808233,
0.812799997891947));
#63452=CARTESIAN_POINT('Ctrl Pts',(0.0299076046828686,-2.15261823504807,
0.923986417723108));
#63453=CARTESIAN_POINT('Ctrl Pts',(1.82526073013706,-1.14155950949091,1.03517283755427));
#63454=CARTESIAN_POINT('Ctrl Pts',(1.94860591616173,0.915246053141843,1.14635925738543));
#63455=CARTESIAN_POINT('Ctrl Pts',(0.286938251999433,2.13363139543668,1.2575456772166));
#63456=CARTESIAN_POINT('Ctrl Pts',(-1.63757451921909,1.39752576117334,1.36873209704776));
#63457=CARTESIAN_POINT('Ctrl Pts',(-2.0619994469249,-0.618778274775138,
1.47991851687892));
#63458=CARTESIAN_POINT('Ctrl Pts',(-0.597542656570052,-2.06825237330522,
1.59110493671008));
#63459=CARTESIAN_POINT('Ctrl Pts',(1.41428872795678,-1.62311872087351,1.70229135654125));
#63460=CARTESIAN_POINT('Ctrl Pts',(2.13057049201279,0.308862702088754,1.81347777637241));
#63461=CARTESIAN_POINT('Ctrl Pts',(0.895157141781652,1.95791217246742,1.92466419620357));
#63462=CARTESIAN_POINT('Ctrl Pts',(-1.16025892730732,1.81342931797682,2.03585061603473));
#63463=CARTESIAN_POINT('Ctrl Pts',(-2.15282751312695,0.00776644692787891,
2.1470370358659));
#63464=CARTESIAN_POINT('Ctrl Pts',(-1.173312682795,-1.80501078038335,2.25822345569706));
#63465=CARTESIAN_POINT('Ctrl Pts',(0.881007459369614,-1.96431984868673,
2.36940987552822));
#63466=CARTESIAN_POINT('Ctrl Pts',(2.12828655167567,-0.324226703065412,
2.48059629535939));
#63467=CARTESIAN_POINT('Ctrl Pts',(1.42596282698117,1.6128721621003,2.59178271519055));
#63468=CARTESIAN_POINT('Ctrl Pts',(-0.582604709802392,2.07251015763547,
2.70296913502171));
#63469=CARTESIAN_POINT('Ctrl Pts',(-2.05748105739819,0.633638933400953,
2.81415555485287));
#63470=CARTESIAN_POINT('Ctrl Pts',(-1.6476154945659,-1.38567304257714,2.92534197468403));
#63471=CARTESIAN_POINT('Ctrl Pts',(0.271537341065049,-2.13564839618882,
3.0365283945152));
#63472=CARTESIAN_POINT('Ctrl Pts',(1.9419501920302,-0.92927716590924,3.14771481434636));
#63473=CARTESIAN_POINT('Ctrl Pts',(1.83345241771109,1.12835226385271,3.25890123417753));
#63474=CARTESIAN_POINT('Ctrl Pts',(0.045432686513366,2.15236206769919,3.37008765400868));
#63475=CARTESIAN_POINT('Ctrl Pts',(-1.78420535659039,1.20471483967528,3.48127407383985));
#63476=CARTESIAN_POINT('Ctrl Pts',(-1.97943388729784,-0.8465034466758,3.59246049367101));
#63477=CARTESIAN_POINT('Ctrl Pts',(-0.361415101720502,-2.12228785127793,
3.70364691350217));
#63478=CARTESIAN_POINT('Ctrl Pts',(1.58767559662444,-1.45396451102085,3.81483333333334));
#63479=CARTESIAN_POINT('Ctrl Pts',(2.08238656893164,0.546253399951339,3.9260197531645));
#63480=CARTESIAN_POINT('Ctrl Pts',(0.669541102087431,2.04607949797729,4.03720617299566));
#63481=CARTESIAN_POINT('Ctrl Pts',(-1.35663306156047,1.67160800898631,4.14839259282683));
#63482=CARTESIAN_POINT('Ctrl Pts',(-2.14007248481188,-0.234128937078206,
4.25957901265799));
#63483=CARTESIAN_POINT('Ctrl Pts',(-0.963112667326238,-1.92539361935742,
4.37076543248915));
#63484=CARTESIAN_POINT('Ctrl Pts',(1.09610013699538,-1.85291421525797,4.48195185232032));
#63485=CARTESIAN_POINT('Ctrl Pts',(2.15123766275159,-0.0830850033729405,
4.59313827215147));
#63486=CARTESIAN_POINT('Ctrl Pts',(1.23574816038915,1.76285367615161,4.70432469198265));
#63487=CARTESIAN_POINT('Ctrl Pts',(-0.811740268440561,1.99394190888763,
4.8155111118138));
#63488=CARTESIAN_POINT('Ctrl Pts',(-2.11563939493572,0.398492848144611,
4.92669753164497));
#63489=CARTESIAN_POINT('Ctrl Pts',(-1.48152105102257,-1.56199294966507,
5.03788395147612));
#63490=CARTESIAN_POINT('Ctrl Pts',(0.509734849759847,-2.0916254402657,5.1490703713073));
#63491=CARTESIAN_POINT('Ctrl Pts',(2.03405151388631,-0.705238284754304,
5.26025679113844));
#63492=CARTESIAN_POINT('Ctrl Pts',(1.69508874624462,1.32717773556567,5.37144321096963));
#63493=CARTESIAN_POINT('Ctrl Pts',(-0.19664885248515,2.1438413719869,5.48262963080077));
#63494=CARTESIAN_POINT('Ctrl Pts',(-1.90824757094816,0.996653303509719,
5.59381605063195));
#63495=CARTESIAN_POINT('Ctrl Pts',(-1.87180872723762,-1.06351242967042,
5.70500247046309));
#63496=CARTESIAN_POINT('Ctrl Pts',(-0.12071188305083,-2.14945463797604,
5.81618889029427));
#63497=CARTESIAN_POINT('Ctrl Pts',(1.74096228296046,-1.26640314621194,5.92737531012542));
#63498=CARTESIAN_POINT('Ctrl Pts',(2.00783946807991,0.776728568965356,6.0385617299566));
#63499=CARTESIAN_POINT('Ctrl Pts',(0.435448592570146,2.10834321747079,6.14974814978775));
#63500=CARTESIAN_POINT('Ctrl Pts',(-1.53583208518367,1.50862401066228,6.26093456961893));
#63501=CARTESIAN_POINT('Ctrl Pts',(-2.10022394255324,-0.473060239877022,
6.37212098945007));
#63502=CARTESIAN_POINT('Ctrl Pts',(-0.74071955267899,-2.02140078749996,
6.48330740928124));
#63503=CARTESIAN_POINT('Ctrl Pts',(1.29731608273796,-1.71805051756223,6.5944938291124));
#63504=CARTESIAN_POINT('Ctrl Pts',(2.14695390376071,0.15910856216126,6.70568024894357));
#63505=CARTESIAN_POINT('Ctrl Pts',(1.02988880574655,1.89051729619815,6.81686666877473));
#63506=CARTESIAN_POINT('Ctrl Pts',(-1.03059911890458,1.89013016894061,6.92805308860589));
#63507=CARTESIAN_POINT('Ctrl Pts',(-2.14701353924984,0.158301805751674,
7.03923950843705));
#63508=CARTESIAN_POINT('Ctrl Pts',(-1.29667041186295,-1.71853787925252,
7.15042592826822));
#63509=CARTESIAN_POINT('Ctrl Pts',(0.741479067384996,-2.0211223100189,7.26161234809938));
#63510=CARTESIAN_POINT('Ctrl Pts',(2.10040155266868,-0.472271020678894,
7.37279876793055));
#63511=CARTESIAN_POINT('Ctrl Pts',(1.53526509213771,1.50920101255294,7.48398518776171));
#63512=CARTESIAN_POINT('Ctrl Pts',(-0.436240798549652,2.10817944328893,
7.59517160759286));
#63513=CARTESIAN_POINT('Ctrl Pts',(-2.00813119194563,0.775974042967894,
7.70635802742404));
#63514=CARTESIAN_POINT('Ctrl Pts',(-1.74048629299744,-1.26705724547931,
7.81754444725519));
#63515=CARTESIAN_POINT('Ctrl Pts',(0.121519559390324,-2.14940912720278,
7.92873086708636));
#63516=CARTESIAN_POINT('Ctrl Pts',(1.87220822337856,-1.06280899870737,8.03991728691751));
#63517=CARTESIAN_POINT('Ctrl Pts',(1.90787293110882,0.997370281398245,8.15110370674869));
#63518=CARTESIAN_POINT('Ctrl Pts',(0.195843262983046,2.1439151139204,8.26229012657984));
#63519=CARTESIAN_POINT('Ctrl Pts',(-1.69558733042143,1.32654069078969,8.37347654641101));
#63520=CARTESIAN_POINT('Ctrl Pts',(-2.03378636810517,-0.706002555693802,
8.48466296624217));
#63521=CARTESIAN_POINT('Ctrl Pts',(-0.508948858861673,-2.09181683182873,
8.59584938607333));
#63522=CARTESIAN_POINT('Ctrl Pts',(1.48210788489943,-1.56143613926181,8.70703580590451));
#63523=CARTESIAN_POINT('Ctrl Pts',(2.11548950721726,0.399287798761521,8.81822222573564));
#63524=CARTESIAN_POINT('Ctrl Pts',(0.810990961415923,1.99424678906897,8.92940864556684));
#63525=CARTESIAN_POINT('Ctrl Pts',(-1.23641048638147,1.76238920508216,9.04059506539797));
#63526=CARTESIAN_POINT('Ctrl Pts',(-2.15120629331062,-0.0838933551026959,
9.15178148522916));
#63527=CARTESIAN_POINT('Ctrl Pts',(-1.09540379848118,-1.85332595276186,
9.26296790506031));
#63528=CARTESIAN_POINT('Ctrl Pts',(0.963836080712942,-1.9250315915564,9.37415432489147));
#63529=CARTESIAN_POINT('Ctrl Pts',(2.14016032912378,-0.233324742234878,
9.48534074472264));
#63530=CARTESIAN_POINT('Ctrl Pts',(1.35600480268067,1.67211762704833,9.5965271645538));
#63531=CARTESIAN_POINT('Ctrl Pts',(-0.67030982818557,2.04582783352242,9.70771358438496));
#63532=CARTESIAN_POINT('Ctrl Pts',(-2.08259181106143,0.545470747680921,
9.81890000421612));
#63533=CARTESIAN_POINT('Ctrl Pts',(-1.58712889620009,-1.45456074914393,
9.93008642404728));
#63534=CARTESIAN_POINT('Ctrl Pts',(0.362212090727357,-2.12215236818265,
10.0412728438785));
#63535=CARTESIAN_POINT('Ctrl Pts',(1.97975271162804,-0.845758688953388,
10.1524592637096));
#63536=CARTESIAN_POINT('Ctrl Pts',(1.78375086909329,1.20538347801125,10.2636456835408));
#63537=CARTESIAN_POINT('Ctrl Pts',(-0.0462382725911752,2.15234810763501,
10.3748321033719));
#63538=CARTESIAN_POINT('Ctrl Pts',(-1.83388235020868,1.12765702777161,10.4860185232031));
#63539=CARTESIAN_POINT('Ctrl Pts',(-1.94158931298892,-0.929994984054507,
10.5972049430343));
#63540=CARTESIAN_POINT('Ctrl Pts',(-0.270756821184746,-2.13577279771527,
10.7083913628654));
#63541=CARTESIAN_POINT('Ctrl Pts',(1.64817793797518,-1.38501096239512,10.8195777826966));
#63542=CARTESIAN_POINT('Ctrl Pts',(2.0571630907777,0.634330397736036,10.9307642025277));
#63543=CARTESIAN_POINT('Ctrl Pts',(0.58197770073898,2.07288432925282,11.0419506223589));
#63544=CARTESIAN_POINT('Ctrl Pts',(-1.42685805211597,1.61204019596003,11.1531370421901));
#63545=CARTESIAN_POINT('Ctrl Pts',(-2.12761151034289,-0.324461171008946,
11.2643234620212));
#63546=CARTESIAN_POINT('Ctrl Pts',(-0.881342614057178,-1.96574134576644,
11.3755098818524));
#63547=CARTESIAN_POINT('Ctrl Pts',(1.17620974724197,-1.80236812191326,11.4866963016836));
#63548=CARTESIAN_POINT('Ctrl Pts',(1.82356548323819,-0.598586618003602,
11.560820581571));
#63549=CARTESIAN_POINT('Ctrl Pts',(1.82115221868229,0.00725425160419088,
11.5978827215147));
#63550=CARTESIAN_POINT('Ctrl Pts',(-0.861525859670525,1.75382131162755,
-1.38777878078145E-16));
#63551=CARTESIAN_POINT('Ctrl Pts',(-1.44496782441849,1.46721837385112,0.0370621399437207));
#63552=CARTESIAN_POINT('Ctrl Pts',(-2.29323624142731,0.270948940037977,
0.111186419831162));
#63553=CARTESIAN_POINT('Ctrl Pts',(-1.4690228053469,-1.78453568564088,0.222372839662325));
#63554=CARTESIAN_POINT('Ctrl Pts',(0.702798023147504,-2.19964250335881,
0.333559259493488));
#63555=CARTESIAN_POINT('Ctrl Pts',(2.22983948348091,-0.602620646924488,
0.44474567932465));
#63556=CARTESIAN_POINT('Ctrl Pts',(1.71476659751129,1.54790339194469,0.555932099155814));
#63557=CARTESIAN_POINT('Ctrl Pts',(-0.371377304572895,2.2797075413722,0.667118518986976));
#63558=CARTESIAN_POINT('Ctrl Pts',(-2.11718147056775,0.923606631345987,
0.778304938818138));
#63559=CARTESIAN_POINT('Ctrl Pts',(-1.92363015131696,-1.2787712372945,0.889491358649302));
#63560=CARTESIAN_POINT('Ctrl Pts',(0.0320890232727887,-2.30962717925356,
1.00067777848046));
#63561=CARTESIAN_POINT('Ctrl Pts',(1.95839267869742,-1.22482325334233,1.11186419831163));
#63562=CARTESIAN_POINT('Ctrl Pts',(2.09073448897961,0.982002812028443,1.22305061814279));
#63563=CARTESIAN_POINT('Ctrl Pts',(0.3078671242282,2.28925546628532,1.33423703797395));
#63564=CARTESIAN_POINT('Ctrl Pts',(-1.75701689972769,1.49945932314417,1.44542345780511));
#63565=CARTESIAN_POINT('Ctrl Pts',(-2.21239878427269,-0.663911091192784,
1.55660987763628));
#63566=CARTESIAN_POINT('Ctrl Pts',(-0.641126576885465,-2.21910779030204,
1.66779629746744));
#63567=CARTESIAN_POINT('Ctrl Pts',(1.51744495713052,-1.74150671579767,1.7789827172986));
#63568=CARTESIAN_POINT('Ctrl Pts',(2.28597130487397,0.331390712847842,1.89016913712977));
#63569=CARTESIAN_POINT('Ctrl Pts',(0.960448643749269,2.10071953052146,2.00135555696093));
#63570=CARTESIAN_POINT('Ctrl Pts',(-1.24488658037438,1.94569829998722,2.11254197679209));
#63571=CARTESIAN_POINT('Ctrl Pts',(-2.30985172178094,0.00833292063536468,
2.22372839662325));
#63572=CARTESIAN_POINT('Ctrl Pts',(-1.2588924584139,-1.93666572611094,2.33491481645442));
#63573=CARTESIAN_POINT('Ctrl Pts',(0.945266903418065,-2.10759457362527,
2.44610123628558));
#63574=CARTESIAN_POINT('Ctrl Pts',(2.28352077714336,-0.347875342430591,
2.55728765611674));
#63575=CARTESIAN_POINT('Ctrl Pts',(1.52997054850621,1.73051278744978,2.6684740759479));
#63576=CARTESIAN_POINT('Ctrl Pts',(-0.625099077306038,2.22367613142842,
2.77966049577907));
#63577=CARTESIAN_POINT('Ctrl Pts',(-2.20755082977362,0.679855665342084,
2.89084691561023));
#63578=CARTESIAN_POINT('Ctrl Pts',(-1.76779024968342,-1.48674208393651,
3.00203333544139));
#63579=CARTESIAN_POINT('Ctrl Pts',(0.291342892527361,-2.29141958423335,
3.11321975527256));
#63580=CARTESIAN_POINT('Ctrl Pts',(2.08359330569799,-0.997057334412016,
3.22440617510372));
#63581=CARTESIAN_POINT('Ctrl Pts',(1.96718185643314,1.21065268979674,3.33559259493488));
#63582=CARTESIAN_POINT('Ctrl Pts',(0.0487464827201324,2.30935232741881,
3.44677901476604));
#63583=CARTESIAN_POINT('Ctrl Pts',(-1.91434278399063,1.29258504441778,3.55796543459721));
#63584=CARTESIAN_POINT('Ctrl Pts',(-2.12381100893932,-0.908246216603541,
3.66915185442837));
#63585=CARTESIAN_POINT('Ctrl Pts',(-0.38777621054007,-2.27708453998192,
3.78033827425954));
#63586=CARTESIAN_POINT('Ctrl Pts',(1.70347841995286,-1.56001463596674,3.89152469409069));
#63587=CARTESIAN_POINT('Ctrl Pts',(2.23427291426326,0.58609635407974,4.00271111392186));
#63588=CARTESIAN_POINT('Ctrl Pts',(0.718376487679439,2.19531765665651,4.11389753375301));
#63589=CARTESIAN_POINT('Ctrl Pts',(-1.45558396757891,1.79353274433565,4.22508395358419));
#63590=CARTESIAN_POINT('Ctrl Pts',(-2.29616635965357,-0.251205972206891,
4.33627037341534));
#63591=CARTESIAN_POINT('Ctrl Pts',(-1.03336074967814,-2.06582911991821,
4.44745679324651));
#63592=CARTESIAN_POINT('Ctrl Pts',(1.17604813820203,-1.98806317010017,4.55864321307767));
#63593=CARTESIAN_POINT('Ctrl Pts',(2.30814590995695,-0.0891451065749571,
4.66982963290884));
#63594=CARTESIAN_POINT('Ctrl Pts',(1.32588189186442,1.89143374203362,4.78101605273999));
#63595=CARTESIAN_POINT('Ctrl Pts',(-0.870947461077787,2.1393772252035,4.89220247257116));
#63596=CARTESIAN_POINT('Ctrl Pts',(-2.26995115459196,0.427558355600586,
5.00338889240232));
#63597=CARTESIAN_POINT('Ctrl Pts',(-1.58958111120973,-1.67592251687317,
5.11457531223348));
#63598=CARTESIAN_POINT('Ctrl Pts',(0.546914192237968,-2.24418565586851,
5.22576173206465));
#63599=CARTESIAN_POINT('Ctrl Pts',(2.1824123683356,-0.756677372605439,5.33694815189581));
#63600=CARTESIAN_POINT('Ctrl Pts',(1.81872613351991,1.4239802115651,5.44813457172697));
#63601=CARTESIAN_POINT('Ctrl Pts',(-0.210992142997687,2.30021014415434,
5.55932099155813));
#63602=CARTESIAN_POINT('Ctrl Pts',(-2.04743246287144,1.06934779265563,5.67050741138931));
#63603=CARTESIAN_POINT('Ctrl Pts',(-2.00833582118916,-1.14108352937273,
5.78169383122044));
#63604=CARTESIAN_POINT('Ctrl Pts',(-0.129516437895867,-2.30623283386393,
5.89288025105164));
#63605=CARTESIAN_POINT('Ctrl Pts',(1.86794562143574,-1.35877280920554,6.00406667088277));
#63606=CARTESIAN_POINT('Ctrl Pts',(2.15428845280213,0.83338205752262,6.11525309071395));
#63607=CARTESIAN_POINT('Ctrl Pts',(0.467209600008474,2.26212280421227,6.22643951054511));
#63608=CARTESIAN_POINT('Ctrl Pts',(-1.64785351575852,1.61866092257753,6.33762593037627));
#63609=CARTESIAN_POINT('Ctrl Pts',(-2.25341132081031,-0.507564587930634,
6.44881235020743));
#63610=CARTESIAN_POINT('Ctrl Pts',(-0.794746594271866,-2.1688389157728,
6.55999877003859));
#63611=CARTESIAN_POINT('Ctrl Pts',(1.39194049181108,-1.84336270411821,6.67118518986976));
#63612=CARTESIAN_POINT('Ctrl Pts',(2.30354969961477,0.170713716736379,6.78237160970093));
#63613=CARTESIAN_POINT('Ctrl Pts',(1.1050074456459,2.02840896683692,6.89355802953208));
#63614=CARTESIAN_POINT('Ctrl Pts',(-1.10576956804586,2.02799360306213,7.00474444936325));
#63615=CARTESIAN_POINT('Ctrl Pts',(-2.30361368483253,0.169848116649841,
7.11593086919441));
#63616=CARTESIAN_POINT('Ctrl Pts',(-1.39124772661127,-1.84388561328419,
7.22711728902557));
#63617=CARTESIAN_POINT('Ctrl Pts',(0.795561506911461,-2.16854012653626,
7.33830370885674));
#63618=CARTESIAN_POINT('Ctrl Pts',(2.25360188555757,-0.506717804195071,
7.44949012868789));
#63619=CARTESIAN_POINT('Ctrl Pts',(1.64724516703786,1.61928001017393,7.56067654851907));
#63620=CARTESIAN_POINT('Ctrl Pts',(-0.468059588377044,2.26194708457211,
7.67186296835021));
#63621=CARTESIAN_POINT('Ctrl Pts',(-2.154601454596,0.832572497460946,7.78304938818139));
#63622=CARTESIAN_POINT('Ctrl Pts',(-1.8674349134348,-1.35947461755279,7.89423580801255));
#63623=CARTESIAN_POINT('Ctrl Pts',(0.130383025010703,-2.30618400359892,
8.00542222784371));
#63624=CARTESIAN_POINT('Ctrl Pts',(2.00876445601631,-1.14032879114536,8.11660864767487));
#63625=CARTESIAN_POINT('Ctrl Pts',(2.04703049732954,1.07011706590215,8.22779506750604));
#63626=CARTESIAN_POINT('Ctrl Pts',(0.210127794931219,2.30028926472067,8.3389814873372));
#63627=CARTESIAN_POINT('Ctrl Pts',(-1.81926108372479,1.42329670163983,8.45016790716836));
#63628=CARTESIAN_POINT('Ctrl Pts',(-2.18212788319439,-0.757497388391501,
8.56135432699953));
#63629=CARTESIAN_POINT('Ctrl Pts',(-0.546070872270014,-2.24439100726275,
8.67254074683069));
#63630=CARTESIAN_POINT('Ctrl Pts',(1.59021074792356,-1.67532509350284,8.78372716666185));
#63631=CARTESIAN_POINT('Ctrl Pts',(2.26979033427429,0.428411288796547,8.89491358649301));
#63632=CARTESIAN_POINT('Ctrl Pts',(0.870143500653468,2.13970434291613,9.00610000632417));
#63633=CARTESIAN_POINT('Ctrl Pts',(-1.32659252698235,1.89093539309814,9.11728642615534));
#63634=CARTESIAN_POINT('Ctrl Pts',(-2.30811225247311,-0.0900124183420705,
9.2284728459865));
#63635=CARTESIAN_POINT('Ctrl Pts',(-1.17530100973675,-1.98850493915805,
9.33965926581767));
#63636=CARTESIAN_POINT('Ctrl Pts',(1.03413692781901,-2.06544068631896,9.45084568564882));
#63637=CARTESIAN_POINT('Ctrl Pts',(2.29626061120593,-0.250343120523647,
9.56203210547999));
#63638=CARTESIAN_POINT('Ctrl Pts',(1.45490988438074,1.79407953322179,9.67321852531115));
#63639=CARTESIAN_POINT('Ctrl Pts',(-0.719201283577143,2.19504763615053,
9.78440494514231));
#63640=CARTESIAN_POINT('Ctrl Pts',(-2.2344931264651,0.585256616254353,9.89559136497349));
#63641=CARTESIAN_POINT('Ctrl Pts',(-1.70289184396906,-1.56065436285928,
10.0067777848046));
#63642=CARTESIAN_POINT('Ctrl Pts',(0.388631330803272,-2.27693917494037,
10.1179642046358));
#63643=CARTESIAN_POINT('Ctrl Pts',(2.1241530878674,-0.907447137301155,10.229150624467));
#63644=CARTESIAN_POINT('Ctrl Pts',(1.91385514681521,1.29330245229283,10.3403370442981));
#63645=CARTESIAN_POINT('Ctrl Pts',(-0.0496108271125438,2.30933734912719,
10.4515234641293));
#63646=CARTESIAN_POINT('Ctrl Pts',(-1.96764314760194,1.20990674417448,10.5627098839605));
#63647=CARTESIAN_POINT('Ctrl Pts',(-2.08320610464741,-0.997827509202423,
10.6738963037916));
#63648=CARTESIAN_POINT('Ctrl Pts',(-0.290505442625618,-2.29155305943203,
10.7850827236228));
#63649=CARTESIAN_POINT('Ctrl Pts',(1.7683937169233,-1.48603171255794,10.8962691434539));
#63650=CARTESIAN_POINT('Ctrl Pts',(2.20720967111538,0.680597564112484,11.0074555632851));
#63651=CARTESIAN_POINT('Ctrl Pts',(0.624426335084105,2.22407759459687,11.1186419831163));
#63652=CARTESIAN_POINT('Ctrl Pts',(-1.53093107010227,1.72962013887028,11.2298284029474));
#63653=CARTESIAN_POINT('Ctrl Pts',(-2.28279649924591,-0.348126912135875,
11.3410148227786));
#63654=CARTESIAN_POINT('Ctrl Pts',(-0.945626503816835,-2.10911975270116,
11.4522012426097));
#63655=CARTESIAN_POINT('Ctrl Pts',(1.26200083066393,-1.93383031585166,11.5633876624409));
#63656=CARTESIAN_POINT('Ctrl Pts',(1.95657378287586,-0.642246683396576,
11.6375119423284));
#63657=CARTESIAN_POINT('Ctrl Pts',(1.95398449819998,0.0077833665056624,
11.6745740822721));
#63658=CARTESIAN_POINT('Ctrl Pts',(-1.95093054978418,-0.000550606481354719,
10.6241303078758));
#63659=CARTESIAN_POINT('Ctrl Pts',(-1.95166977968097,-0.292567552961119,
10.640718973181));
#63660=CARTESIAN_POINT('Ctrl Pts',(-1.89027401228485,-0.584289311968449,
10.6573076384863));
#63661=CARTESIAN_POINT('Ctrl Pts',(-1.7651621681362,-0.845492725344543,
10.6738963037916));
#63662=CARTESIAN_POINT('Ctrl Pts',(-1.48563921730681,-1.42906935927896,
10.7109584437353));
#63663=CARTESIAN_POINT('Ctrl Pts',(-0.888072329966215,-1.8603112093555,
10.7480205836791));
#63664=CARTESIAN_POINT('Ctrl Pts',(-0.246139026371096,-1.94167857658142,
10.7850827236228));
#63665=CARTESIAN_POINT('Ctrl Pts',(0.395794277224022,-2.02304594380734,
10.8221448635665));
#63666=CARTESIAN_POINT('Ctrl Pts',(1.08209399707366,-1.75453882818264,10.8592070035102));
#63667=CARTESIAN_POINT('Ctrl Pts',(1.49837984936383,-1.25918039092522,10.8962691434539));
#63668=CARTESIAN_POINT('Ctrl Pts',(1.91466570165399,-0.763821953667804,
10.9333312833977));
#63669=CARTESIAN_POINT('Ctrl Pts',(2.06093768638468,-0.041612194777677,
10.9703934233414));
#63670=CARTESIAN_POINT('Ctrl Pts',(1.87027645607817,0.576739356414784,11.0074555632851));
#63671=CARTESIAN_POINT('Ctrl Pts',(1.80418088670294,0.791100177355746,11.0203037088567));
#63672=CARTESIAN_POINT('Ctrl Pts',(1.69759382901609,0.992979671982257,11.0331518544284));
#63673=CARTESIAN_POINT('Ctrl Pts',(1.56057659382855,1.17255425406022,11.046));
#63674=CARTESIAN_POINT('Ctrl Pts',(-0.9055496143049,-1.2679201530598,4.59701721133854E-17));
#63675=CARTESIAN_POINT('Ctrl Pts',(-0.937460871048188,-1.25085822491965,
4.11134559556874E-17));
#63676=CARTESIAN_POINT('Ctrl Pts',(-0.968677330061127,-1.23263760516135,
2.44937731663795E-16));
#63677=CARTESIAN_POINT('Ctrl Pts',(-0.999128467894991,-1.21327242330634,
1.95156391047391E-16));
#63678=CARTESIAN_POINT('Ctrl Pts',(-1.04916478169554,-1.18145218981002,
1.19833509668E-16));
#63679=CARTESIAN_POINT('Ctrl Pts',(-1.09713600671012,-1.14654455097205,
1.20483738925504E-16));
#63680=CARTESIAN_POINT('Ctrl Pts',(-1.14296368523792,-1.10887020140839,
3.46944695195361E-17));
#63681=CARTESIAN_POINT('Ctrl Pts',(-1.1691715546085,-1.08732504652154,-1.4366579135275E-17));
#63682=CARTESIAN_POINT('Ctrl Pts',(-1.19467812556179,-1.06487409533188,
1.54611493479508E-16));
#63683=CARTESIAN_POINT('Ctrl Pts',(-1.21946596262297,-1.04157045589269,
1.28369537222284E-16));
#63684=CARTESIAN_POINT('Ctrl Pts',(-1.23288807387334,-1.02895200756582,
1.14160049906282E-16));
#63685=CARTESIAN_POINT('Ctrl Pts',(-1.24610308792281,-1.01607950194371,
2.35779340588765E-16));
#63686=CARTESIAN_POINT('Ctrl Pts',(-1.25908578368524,-1.0029839550804,2.28983498828939E-16));
#63687=CARTESIAN_POINT('Ctrl Pts',(-1.30296735026586,-0.95872095130156,
2.06013524941215E-16));
#63688=CARTESIAN_POINT('Ctrl Pts',(-1.34424080059494,-0.911874911049719,
3.41092537496216E-16));
#63689=CARTESIAN_POINT('Ctrl Pts',(-1.3828175432908,-0.862794893107178,
2.15105711021124E-16));
#63690=CARTESIAN_POINT('Ctrl Pts',(-1.41246270387874,-0.825078255778903,
1.18288316865636E-16));
#63691=CARTESIAN_POINT('Ctrl Pts',(-1.44051505756546,-0.786041114269597,
-3.41744083773187E-17));
#63692=CARTESIAN_POINT('Ctrl Pts',(-1.46692433972057,-0.745823635123971,
-2.77555756156289E-17));
#63693=CARTESIAN_POINT('Ctrl Pts',(-1.479951210132,-0.725985614308893,-2.45893667770833E-17));
#63694=CARTESIAN_POINT('Ctrl Pts',(-1.49257814628919,-0.705860181165347,
1.12314029669873E-16));
#63695=CARTESIAN_POINT('Ctrl Pts',(-1.50479813274716,-0.685463000140721,
1.31838984174237E-16));
#63696=CARTESIAN_POINT('Ctrl Pts',(-1.51107691151866,-0.674982678607113,
1.41871145034493E-16));
#63697=CARTESIAN_POINT('Ctrl Pts',(-1.51724344631134,-0.664438579506566,
2.39743182585592E-16));
#63698=CARTESIAN_POINT('Ctrl Pts',(-1.52329612440982,-0.653835068968427,
2.42861286636753E-16));
#63699=CARTESIAN_POINT('Ctrl Pts',(-1.55541704658302,-0.597563360607725,
2.59408734877987E-16));
#63700=CARTESIAN_POINT('Ctrl Pts',(-1.58434358367058,-0.539605423501723,
2.32306933354682E-17));
#63701=CARTESIAN_POINT('Ctrl Pts',(-1.60998194797531,-0.480314579840224,
1.38777878078145E-17));
#63702=CARTESIAN_POINT('Ctrl Pts',(-1.63611695660561,-0.419875204988797,
4.34370584461709E-18));
#63703=CARTESIAN_POINT('Ctrl Pts',(-1.65883591999594,-0.358049987819819,
-3.99522282745635E-16));
#63704=CARTESIAN_POINT('Ctrl Pts',(-1.67800508733892,-0.295172269836945,
-4.02455846426619E-16));
#63705=CARTESIAN_POINT('Ctrl Pts',(-1.69036857863681,-0.254618180804147,
-4.04347899868101E-16));
#63706=CARTESIAN_POINT('Ctrl Pts',(-1.70125468815875,-0.21362546632645,
2.10692284276142E-16));
#63707=CARTESIAN_POINT('Ctrl Pts',(-1.71061789501208,-0.172277279535232,
2.22044604925031E-16));
#63708=CARTESIAN_POINT('Ctrl Pts',(-1.71585060492304,-0.149169484288187,
2.28388948449886E-16));
#63709=CARTESIAN_POINT('Ctrl Pts',(-1.72060753217063,-0.125950592727189,
-7.81124113857471E-17));
#63710=CARTESIAN_POINT('Ctrl Pts',(-1.72487954070067,-0.102634681883505,
-6.93889390390723E-17));
#63711=CARTESIAN_POINT('Ctrl Pts',(-1.72700542719079,-0.0910319475914671,
-6.50478634353357E-17));
#63712=CARTESIAN_POINT('Ctrl Pts',(-1.7290114810898,-0.0794035343790101,
3.2530658909822E-16));
#63713=CARTESIAN_POINT('Ctrl Pts',(-1.73089565945358,-0.0677563287869385,
3.05311331771918E-16));
#63714=CARTESIAN_POINT('Ctrl Pts',(-1.74172479313661,-0.000815136373784872,
1.90390516006322E-16));
#63715=CARTESIAN_POINT('Ctrl Pts',(-1.74848828323664,0.0664709663887247,
1.66332759660732E-17));
#63716=CARTESIAN_POINT('Ctrl Pts',(-1.75106678678907,0.133744024330042,
0.));
#63717=CARTESIAN_POINT('Ctrl Pts',(-1.75197767455289,0.157509050853062,
-5.87590718476407E-18));
#63718=CARTESIAN_POINT('Ctrl Pts',(-1.75236592486458,0.181272742240003,
-1.43574718418596E-16));
#63719=CARTESIAN_POINT('Ctrl Pts',(-1.75222496230419,0.20502014676713,-1.52655665885959E-16));
#63720=CARTESIAN_POINT('Ctrl Pts',(-1.75184009030703,0.269858008556557,
-1.89868827307373E-16));
#63721=CARTESIAN_POINT('Ctrl Pts',(-1.74751402866387,0.334573792851957,
-3.30194805135327E-16));
#63722=CARTESIAN_POINT('Ctrl Pts',(-1.7394637798186,0.398932034828451,-3.60822483003176E-16));
#63723=CARTESIAN_POINT('Ctrl Pts',(-1.73512917103287,0.433585348839861,
-3.77313774654407E-16));
#63724=CARTESIAN_POINT('Ctrl Pts',(-1.72971393872322,0.468135193807322,
-2.30290250750647E-16));
#63725=CARTESIAN_POINT('Ctrl Pts',(-1.72324590502527,0.502545438383202,
-2.22044604925031E-16));
#63726=CARTESIAN_POINT('Ctrl Pts',(-1.71875224847293,0.526451903350239,
-2.16315955056648E-16));
#63727=CARTESIAN_POINT('Ctrl Pts',(-1.71375034317529,0.550290993458765,
-1.09112752506388E-16));
#63728=CARTESIAN_POINT('Ctrl Pts',(-1.70824837476028,0.574050543226345,
-1.11022302462516E-16));
#63729=CARTESIAN_POINT('Ctrl Pts',(-1.70556019910987,0.585659087356796,
-1.11955278682682E-16));
#63730=CARTESIAN_POINT('Ctrl Pts',(-1.70275214211861,0.597250589985584,
-1.86923780482983E-17));
#63731=CARTESIAN_POINT('Ctrl Pts',(-1.69982665236451,0.608817432227434,
-2.77555756156289E-17));
#63732=CARTESIAN_POINT('Ctrl Pts',(-1.68323412399998,0.674421202576402,
-7.91594003935956E-17));
#63733=CARTESIAN_POINT('Ctrl Pts',(-1.6629277813761,0.739001412074313,-4.05964646411352E-16));
#63734=CARTESIAN_POINT('Ctrl Pts',(-1.63916833994428,0.802303176749866,
-3.88578058618805E-16));
#63735=CARTESIAN_POINT('Ctrl Pts',(-1.61488642929252,0.866996944840365,
-3.70809140417215E-16));
#63736=CARTESIAN_POINT('Ctrl Pts',(-1.58699772603761,0.930356288581554,
-4.09457680297508E-17));
#63737=CARTESIAN_POINT('Ctrl Pts',(-1.55572518982035,0.992113582996803,
0.));
#63738=CARTESIAN_POINT('Ctrl Pts',(-1.52416508821539,1.05443876420538,4.13222832434933E-17));
#63739=CARTESIAN_POINT('Ctrl Pts',(-1.48915832892389,1.11513327578217,-2.91589739144645E-16));
#63740=CARTESIAN_POINT('Ctrl Pts',(-1.45088203376165,1.17391247934435,-2.77555756156289E-16));
#63741=CARTESIAN_POINT('Ctrl Pts',(-1.43586030613212,1.19698067814596,-2.72048047818399E-16));
#63742=CARTESIAN_POINT('Ctrl Pts',(-1.42033446520901,1.21975369583959,-2.46829292445535E-16));
#63743=CARTESIAN_POINT('Ctrl Pts',(-1.40431321996707,1.24221341255695,-2.22044604925031E-16));
#63744=CARTESIAN_POINT('Ctrl Pts',(-1.39827097600966,1.25068385824148,-2.12697320981403E-16));
#63745=CARTESIAN_POINT('Ctrl Pts',(-1.39215941512485,1.25910802930607,-2.5395452896005E-16));
#63746=CARTESIAN_POINT('Ctrl Pts',(-1.38598454691313,1.26747777400967,-2.4980018054066E-16));
#63747=CARTESIAN_POINT('Ctrl Pts',(-1.3431243018081,1.32557282918544,-2.20964521964367E-16));
#63748=CARTESIAN_POINT('Ctrl Pts',(-1.29714727100707,1.38114651172693,8.67497813555755E-17));
#63749=CARTESIAN_POINT('Ctrl Pts',(-1.24829449348075,1.43391808714502,5.55111512312578E-17));
#63750=CARTESIAN_POINT('Ctrl Pts',(-1.19933005104754,1.48681028483588,2.42011176187261E-17));
#63751=CARTESIAN_POINT('Ctrl Pts',(-1.14747626839011,1.53688856046327,-1.29713890200027E-16));
#63752=CARTESIAN_POINT('Ctrl Pts',(-1.09292624810297,1.58385401467225,-2.77555756156289E-17));
#63753=CARTESIAN_POINT('Ctrl Pts',(-1.03954323648884,1.62981471962349,7.20215071969156E-17));
#63754=CARTESIAN_POINT('Ctrl Pts',(-0.983577547054738,1.67279522220595,
1.33536308196711E-16));
#63755=CARTESIAN_POINT('Ctrl Pts',(-0.92517040004714,1.71248622994896,1.66533453693773E-16));
#63756=CARTESIAN_POINT('Ctrl Pts',(-0.904266808925204,1.72669141954621,
1.78342947445829E-16));
#63757=CARTESIAN_POINT('Ctrl Pts',(-0.883050159709791,1.74047492561567,
-1.31748417511445E-16));
#63758=CARTESIAN_POINT('Ctrl Pts',(-0.861525859670525,1.75382131162755,
-1.38777878078145E-16));
#63759=CARTESIAN_POINT('Origin',(0.,0.,0.));
#63760=CARTESIAN_POINT('Origin',(-0.866025403784439,-1.5,-4.));
#63761=CARTESIAN_POINT('',(-0.866025403784439,-1.5,-4.));
#63762=CARTESIAN_POINT('',(0.866025403784439,-1.5,-4.));
#63763=CARTESIAN_POINT('',(-0.43301270189222,-1.5,-4.));
#63764=CARTESIAN_POINT('',(-0.866025403784439,-1.5,-2.));
#63765=CARTESIAN_POINT('',(-0.866025403784439,-1.5,-4.));
#63766=CARTESIAN_POINT('',(0.866025403784439,-1.5,-2.));
#63767=CARTESIAN_POINT('',(-0.866025403784439,-1.5,-2.));
#63768=CARTESIAN_POINT('',(0.866025403784439,-1.5,-4.));
#63769=CARTESIAN_POINT('Origin',(-1.73205080756888,2.12115047744981E-16,
-4.));
#63770=CARTESIAN_POINT('',(-1.73205080756888,2.12115047744981E-16,-4.));
#63771=CARTESIAN_POINT('',(-1.51554445662277,-0.375,-4.));
#63772=CARTESIAN_POINT('',(-1.73205080756888,2.77555756156289E-16,-2.));
#63773=CARTESIAN_POINT('',(-1.73205080756888,2.12115047744981E-16,-4.));
#63774=CARTESIAN_POINT('',(-1.73205080756888,2.12115047744981E-16,-2.));
#63775=CARTESIAN_POINT('Origin',(-0.866025403784438,1.5,-4.));
#63776=CARTESIAN_POINT('',(-0.866025403784438,1.5,-4.));
#63777=CARTESIAN_POINT('',(-1.08253175473055,1.125,-4.));
#63778=CARTESIAN_POINT('',(-0.866025403784438,1.5,-2.));
#63779=CARTESIAN_POINT('',(-0.866025403784438,1.5,-4.));
#63780=CARTESIAN_POINT('',(-0.866025403784438,1.5,-2.));
#63781=CARTESIAN_POINT('Origin',(0.866025403784439,1.5,-4.));
#63782=CARTESIAN_POINT('',(0.866025403784439,1.5,-4.));
#63783=CARTESIAN_POINT('',(0.43301270189222,1.5,-4.));
#63784=CARTESIAN_POINT('',(0.866025403784439,1.5,-2.));
#63785=CARTESIAN_POINT('',(0.866025403784439,1.5,-4.));
#63786=CARTESIAN_POINT('',(0.866025403784439,1.5,-2.));
#63787=CARTESIAN_POINT('Origin',(1.73205080756888,0.,-4.));
#63788=CARTESIAN_POINT('',(1.73205080756888,0.,-4.));
#63789=CARTESIAN_POINT('',(1.51554445662277,0.375,-4.));
#63790=CARTESIAN_POINT('',(1.73205080756888,0.,-2.));
#63791=CARTESIAN_POINT('',(1.73205080756888,0.,-4.));
#63792=CARTESIAN_POINT('',(1.73205080756888,0.,-2.));
#63793=CARTESIAN_POINT('Origin',(0.866025403784439,-1.5,-4.));
#63794=CARTESIAN_POINT('',(1.08253175473055,-1.125,-4.));
#63795=CARTESIAN_POINT('',(0.866025403784439,-1.5,-2.));
#63796=CARTESIAN_POINT('Origin',(0.,2.77555756156289E-16,-2.));
#63797=CARTESIAN_POINT('Origin',(0.,0.,0.));
#63798=CARTESIAN_POINT('',(-3.5,-4.28626379701574E-16,0.));
#63799=CARTESIAN_POINT('Origin',(0.,0.,0.));
#63800=CARTESIAN_POINT('Origin',(0.,0.,-4.));
#63801=CARTESIAN_POINT('',(-3.5,-4.28626379701574E-16,-4.));
#63802=CARTESIAN_POINT('',(-3.5,-4.28626379701574E-16,-4.));
#63803=CARTESIAN_POINT('Origin',(0.,0.,-4.));
#63804=CARTESIAN_POINT('Origin',(0.,0.,-4.));
#63805=CARTESIAN_POINT('Origin',(0.,0.,12.));
#63877=UNCERTAINTY_MEASURE_WITH_UNIT(LENGTH_MEASURE(0.01),#63899,
'DISTANCE_ACCURACY_VALUE',
'Maximum model space distance between geometric entities at asserted c
onnectivities');
#63878=UNCERTAINTY_MEASURE_WITH_UNIT(LENGTH_MEASURE(0.01),#63899,
'DISTANCE_ACCURACY_VALUE',
'Maximum model space distance between geometric entities at asserted c
onnectivities');
#63897=(
GEOMETRIC_REPRESENTATION_CONTEXT(3)
GLOBAL_UNCERTAINTY_ASSIGNED_CONTEXT((#63877))
GLOBAL_UNIT_ASSIGNED_CONTEXT((#63899,#63901,#63902))
REPRESENTATION_CONTEXT('','3D')
);
#63898=(
GEOMETRIC_REPRESENTATION_CONTEXT(3)
GLOBAL_UNCERTAINTY_ASSIGNED_CONTEXT((#63878))
GLOBAL_UNIT_ASSIGNED_CONTEXT((#63899,#63901,#63902))
REPRESENTATION_CONTEXT('','3D')
);
#63899=(
LENGTH_UNIT()
NAMED_UNIT(*)
SI_UNIT(.MILLI.,.METRE.)
);
#63901=(
NAMED_UNIT(*)
PLANE_ANGLE_UNIT()
SI_UNIT($,.RADIAN.)
);
#63902=(
NAMED_UNIT(*)
SI_UNIT($,.STERADIAN.)
SOLID_ANGLE_UNIT()
);
#63921=SHAPE_DEFINITION_REPRESENTATION(#63940,#64012);
#63940=PRODUCT_DEFINITION_SHAPE('',$,#64032);
#64012=SHAPE_REPRESENTATION('',(#16752),#63897);
#64013=PRODUCT_DEFINITION_CONTEXT('part definition',#64072,'design');
#64032=PRODUCT_DEFINITION('Socket head cap screw M4x12',
'Socket head cap screw M4x12',#64051,#64013);
#64051=PRODUCT_DEFINITION_FORMATION('',$,#64092);
#64072=APPLICATION_CONTEXT(
'Core Data for Automotive Mechanical Design Process');
#64073=PRODUCT_CONTEXT('part definition',#64072,'mechanical');
#64092=PRODUCT('Socket head cap screw M4x12',
'Socket head cap screw M4x12',$,(#64073));
#64099=PRESENTATION_STYLE_ASSIGNMENT((#64112));
#64112=SURFACE_STYLE_USAGE(.BOTH.,#64125);
#64125=SURFACE_SIDE_STYLE('',(#64138));
#64138=SURFACE_STYLE_FILL_AREA(#64151);
#64151=FILL_AREA_STYLE('Dark gray',(#64164));
#64164=FILL_AREA_STYLE_COLOUR('Dark gray',#64177);
#64177=COLOUR_RGB('Dark gray',0.250980392156863,0.282352941176471,0.32156862745098);
ENDSEC;
END-ISO-10303-21;
